ISO-10303-21;
HEADER;
FILE_DESCRIPTION (('STEP AP214'),
    '1' );
FILE_NAME ('7. Upper Jaw.step',
    '2026-10-09T08:13:37',
    ( '' ),
    ( '' ),
    'SwSTEP 2.0',
    'SolidWorks 2021',
    '' );
FILE_SCHEMA (( 'AUTOMOTIVE_DESIGN' ));
ENDSEC;

DATA;
#11=LINE ( 'NONE', #27826, #25683 ) ;
#23=VECTOR ( 'NONE', #7321, 1000.000000000000000 ) ;
#31=DIRECTION ( 'NONE',  ( -9.376883653928687363E-17, -1.000000000000000000, 0.000000000000000000 ) ) ;
#34=FACE_OUTER_BOUND ( 'NONE', #29836, .T. ) ;
#43=ORIENTED_EDGE ( 'NONE', *, *, #36163, .F. ) ;
#62=AXIS2_PLACEMENT_3D ( 'NONE', #27613, #39267, #7568 ) ;
#92=DIRECTION ( 'NONE',  ( 0.000000000000000000, 0.000000000000000000, -1.000000000000000000 ) ) ;
#94=DIRECTION ( 'NONE',  ( 1.000000000000000000, 0.000000000000000000, 0.000000000000000000 ) ) ;
#141=ORIENTED_EDGE ( 'NONE', *, *, #12867, .F. ) ;
#144=AXIS2_PLACEMENT_3D ( 'NONE', #47269, #4995, #63405 ) ;
#162=EDGE_CURVE ( 'NONE', #36655, #50552, #43525, .T. ) ;
#166=ORIENTED_EDGE ( 'NONE', *, *, #34857, .T. ) ;
#180=PLANE ( 'NONE',  #48189 ) ;
#209=AXIS2_PLACEMENT_3D ( 'NONE', #26533, #25492, #41365 ) ;
#227=ORIENTED_EDGE ( 'NONE', *, *, #43634, .F. ) ;
#266=CARTESIAN_POINT ( 'NONE',  ( -9.250000000000003553, 25.24999999999998934, -4.000000000000000000 ) ) ;
#303=CARTESIAN_POINT ( 'NONE',  ( 9.250000000000003553, 27.99999999999998934, -3.750000000000000000 ) ) ;
#337=LINE ( 'NONE', #47253, #45614 ) ;
#339=CARTESIAN_POINT ( 'NONE',  ( -22.75000000000000711, 37.00000000000000000, -3.750000000000000000 ) ) ;
#345=EDGE_CURVE ( 'NONE', #35189, #45655, #41362, .T. ) ;
#414=DIRECTION ( 'NONE',  ( -1.000000000000000000, 0.000000000000000000, 0.000000000000000000 ) ) ;
#419=ADVANCED_FACE ( 'NONE', ( #59216 ), #27553, .F. ) ;
#445=AXIS2_PLACEMENT_3D ( 'NONE', #1315, #50606, #28423 ) ;
#451=ORIENTED_EDGE ( 'NONE', *, *, #12857, .T. ) ;
#454=VERTEX_POINT ( 'NONE', #6800 ) ;
#472=DIRECTION ( 'NONE',  ( 0.000000000000000000, 0.000000000000000000, -1.000000000000000000 ) ) ;
#491=CARTESIAN_POINT ( 'NONE',  ( 4.250000000000001776, 21.99999999999998579, -3.750000000000000000 ) ) ;
#504=DIRECTION ( 'NONE',  ( -0.000000000000000000, 1.000000000000000000, -0.000000000000000000 ) ) ;
#529=VERTEX_POINT ( 'NONE', #11740 ) ;
#531=DIRECTION ( 'NONE',  ( 0.000000000000000000, 1.000000000000000000, 0.000000000000000000 ) ) ;
#549=DIRECTION ( 'NONE',  ( -1.000000000000000000, 0.000000000000000000, 0.000000000000000000 ) ) ;
#554=ORIENTED_EDGE ( 'NONE', *, *, #7703, .F. ) ;
#573=ORIENTED_EDGE ( 'NONE', *, *, #64148, .T. ) ;
#585=ADVANCED_FACE ( 'NONE', ( #60599 ), #66238, .T. ) ;
#593=CIRCLE ( 'NONE', #44497, 0.2500000000000002220 ) ;
#600=( GEOMETRIC_REPRESENTATION_CONTEXT ( 3 ) GLOBAL_UNCERTAINTY_ASSIGNED_CONTEXT ( ( #58099 ) ) GLOBAL_UNIT_ASSIGNED_CONTEXT ( ( #44153, #38168, #38862 ) ) REPRESENTATION_CONTEXT ( 'NONE', 'WORKASPACE' ) );
#607=DIRECTION ( 'NONE',  ( 0.000000000000000000, 0.000000000000000000, -1.000000000000000000 ) ) ;
#612=CARTESIAN_POINT ( 'NONE',  ( -22.25000000000000711, 33.74999999999999289, -3.750000000000000000 ) ) ;
#617=DIRECTION ( 'NONE',  ( 1.000000000000000000, 0.000000000000000000, 0.000000000000000000 ) ) ;
#628=DIRECTION ( 'NONE',  ( 0.000000000000000000, 0.000000000000000000, 1.000000000000000000 ) ) ;
#645=PLANE ( 'NONE',  #55065 ) ;
#654=CARTESIAN_POINT ( 'NONE',  ( -13.50000000000000355, 28.24999999999998934, -4.000000000000000000 ) ) ;
#686=CARTESIAN_POINT ( 'NONE',  ( 8.750000000000001776, 24.74999999999998579, -3.750000000000000000 ) ) ;
#716=CARTESIAN_POINT ( 'NONE',  ( -4.250000000000001776, 21.99999999999998579, 3.750000000000000000 ) ) ;
#743=CARTESIAN_POINT ( 'NONE',  ( -25.00000000000000355, 36.75000000000000000, -3.000000000000000000 ) ) ;
#749=DIRECTION ( 'NONE',  ( 0.000000000000000000, -1.000000000000000000, 0.000000000000000000 ) ) ;
#791=EDGE_CURVE ( 'NONE', #1837, #31530, #38921, .T. ) ;
#816=CIRCLE ( 'NONE', #58197, 1.000000000000000888 ) ;
#876=AXIS2_PLACEMENT_3D ( 'NONE', #62738, #3624, #19840 ) ;
#879=VECTOR ( 'NONE', #31549, 1000.000000000000000 ) ;
#884=AXIS2_PLACEMENT_3D ( 'NONE', #23527, #66093, #8054 ) ;
#898=ORIENTED_EDGE ( 'NONE', *, *, #4253, .T. ) ;
#900=ORIENTED_EDGE ( 'NONE', *, *, #28247, .T. ) ;
#918=LINE ( 'NONE', #66052, #53474 ) ;
#922=ORIENTED_EDGE ( 'NONE', *, *, #54460, .T. ) ;
#925=EDGE_LOOP ( 'NONE', ( #34844, #14529, #43213, #21160 ) ) ;
#932=ADVANCED_FACE ( 'NONE', ( #19253 ), #67118, .F. ) ;
#933=DIRECTION ( 'NONE',  ( -0.000000000000000000, -0.000000000000000000, -1.000000000000000000 ) ) ;
#934=ORIENTED_EDGE ( 'NONE', *, *, #5792, .T. ) ;
#951=ORIENTED_EDGE ( 'NONE', *, *, #31614, .F. ) ;
#988=CARTESIAN_POINT ( 'NONE',  ( 4.500000000000002665, 22.24999999999998579, 4.000000000000000000 ) ) ;
#990=ORIENTED_EDGE ( 'NONE', *, *, #25548, .F. ) ;
#1038=EDGE_CURVE ( 'NONE', #30672, #41120, #15077, .T. ) ;
#1074=VECTOR ( 'NONE', #4879, 1000.000000000000000 ) ;
#1078=DIRECTION ( 'NONE',  ( 0.000000000000000000, 1.000000000000000000, 0.000000000000000000 ) ) ;
#1085=EDGE_CURVE ( 'NONE', #61213, #35189, #33302, .T. ) ;
#1108=FILL_AREA_STYLE ('',( #53945 ) ) ;
#1148=STYLED_ITEM ( 'NONE', ( #50817 ), #55567 ) ;
#1163=CIRCLE ( 'NONE', #40576, 0.2500000000000002220 ) ;
#1182=FACE_OUTER_BOUND ( 'NONE', #23963, .T. ) ;
#1195=MECHANICAL_DESIGN_GEOMETRIC_PRESENTATION_REPRESENTATION('',(#1148),#28191);
#1215=DIRECTION ( 'NONE',  ( 0.000000000000000000, 0.000000000000000000, 1.000000000000000000 ) ) ;
#1217=EDGE_CURVE ( 'NONE', #56763, #41176, #14618, .T. ) ;
#1262=ORIENTED_EDGE ( 'NONE', *, *, #38969, .F. ) ;
#1290=DIRECTION ( 'NONE',  ( 0.000000000000000000, 0.000000000000000000, -1.000000000000000000 ) ) ;
#1300=CARTESIAN_POINT ( 'NONE',  ( 22.75000000000000711, 36.75000000000000000, -3.750000000000000000 ) ) ;
#1315=CARTESIAN_POINT ( 'NONE',  ( -15.00000000000000000, 8.000000000000000000, -4.000000000000000000 ) ) ;
#1324=VERTEX_POINT ( 'NONE', #9349 ) ;
#1348=DIRECTION ( 'NONE',  ( -0.000000000000000000, -0.000000000000000000, 1.000000000000000000 ) ) ;
#1350=DIRECTION ( 'NONE',  ( -1.000000000000000000, 0.000000000000000000, 0.000000000000000000 ) ) ;
#1370=FACE_BOUND ( 'NONE', #12312, .T. ) ;
#1435=VECTOR ( 'NONE', #40829, 1000.000000000000000 ) ;
#1454=VERTEX_POINT ( 'NONE', #13840 ) ;
#1495=DIRECTION ( 'NONE',  ( -1.000000000000000000, 0.000000000000000000, 0.000000000000000000 ) ) ;
#1556=EDGE_CURVE ( 'NONE', #50331, #65395, #9628, .T. ) ;
#1565=DIRECTION ( 'NONE',  ( -1.000000000000000000, 0.000000000000000000, 0.000000000000000000 ) ) ;
#1594=DIRECTION ( 'NONE',  ( 0.000000000000000000, 0.000000000000000000, -1.000000000000000000 ) ) ;
#1595=VERTEX_POINT ( 'NONE', #46600 ) ;
#1597=DIRECTION ( 'NONE',  ( 1.000000000000000000, -0.000000000000000000, -0.000000000000000000 ) ) ;
#1662=DIRECTION ( 'NONE',  ( 0.000000000000000000, 0.000000000000000000, -1.000000000000000000 ) ) ;
#1665=DIRECTION ( 'NONE',  ( 0.000000000000000000, 0.000000000000000000, -1.000000000000000000 ) ) ;
#1706=CYLINDRICAL_SURFACE ( 'NONE', #4736, 0.2500000000000002220 ) ;
#1729=ORIENTED_EDGE ( 'NONE', *, *, #50153, .T. ) ;
#1752=DIRECTION ( 'NONE',  ( 0.000000000000000000, -1.000000000000000000, 0.000000000000000000 ) ) ;
#1768=DIRECTION ( 'NONE',  ( 0.7071067811865474617, 0.000000000000000000, 0.7071067811865474617 ) ) ;
#1803=ORIENTED_EDGE ( 'NONE', *, *, #14374, .T. ) ;
#1806=DIRECTION ( 'NONE',  ( -1.000000000000000000, 0.000000000000000000, 0.000000000000000000 ) ) ;
#1837=VERTEX_POINT ( 'NONE', #17677 ) ;
#1852=CARTESIAN_POINT ( 'NONE',  ( -9.250000000000003553, 25.24999999999998934, 4.000000000000000000 ) ) ;
#1881=DIRECTION ( 'NONE',  ( 0.000000000000000000, 0.000000000000000000, -1.000000000000000000 ) ) ;
#1902=ORIENTED_EDGE ( 'NONE', *, *, #30713, .F. ) ;
#1905=VECTOR ( 'NONE', #66420, 1000.000000000000000 ) ;
#1912=CARTESIAN_POINT ( 'NONE',  ( 13.75000000000000533, 30.99999999999999289, 3.750000000000000000 ) ) ;
#1927=EDGE_CURVE ( 'NONE', #35855, #21095, #41033, .T. ) ;
#1929=EDGE_LOOP ( 'NONE', ( #2352, #3010, #34974, #11079 ) ) ;
#1959=ORIENTED_EDGE ( 'NONE', *, *, #16549, .F. ) ;
#1980=EDGE_CURVE ( 'NONE', #66411, #2325, #36526, .T. ) ;
#2016=AXIS2_PLACEMENT_3D ( 'NONE', #63589, #36894, #58653 ) ;
#2037=AXIS2_PLACEMENT_3D ( 'NONE', #5373, #11359, #16676 ) ;
#2038=ORIENTED_EDGE ( 'NONE', *, *, #18513, .F. ) ;
#2058=ORIENTED_EDGE ( 'NONE', *, *, #41906, .T. ) ;
#2070=DIRECTION ( 'NONE',  ( 0.000000000000000000, 0.000000000000000000, 1.000000000000000000 ) ) ;
#2091=LINE ( 'NONE', #62625, #46288 ) ;
#2108=CARTESIAN_POINT ( 'NONE',  ( 0.000000000000000000, 33.74999999999999289, 3.750000000000000000 ) ) ;
#2115=ORIENTED_EDGE ( 'NONE', *, *, #27930, .F. ) ;
#2130=EDGE_CURVE ( 'NONE', #64410, #66883, #18163, .T. ) ;
#2136=ADVANCED_FACE ( 'NONE', ( #45963 ), #8321, .F. ) ;
#2146=DIRECTION ( 'NONE',  ( 0.000000000000000000, 0.000000000000000000, 1.000000000000000000 ) ) ;
#2158=CONICAL_SURFACE ( 'NONE', #40418, 4.000000000000000000, 0.7853981633974482790 ) ;
#2168=DIRECTION ( 'NONE',  ( 0.000000000000000000, 0.000000000000000000, -1.000000000000000000 ) ) ;
#2200=VECTOR ( 'NONE', #4405, 1000.000000000000000 ) ;
#2211=AXIS2_PLACEMENT_3D ( 'NONE', #39533, #13811, #7830 ) ;
#2224=LINE ( 'NONE', #8289, #34988 ) ;
#2227=VECTOR ( 'NONE', #29351, 1000.000000000000000 ) ;
#2228=LINE ( 'NONE', #6884, #11765 ) ;
#2234=ADVANCED_FACE ( 'NONE', ( #8659 ), #45638, .T. ) ;
#2246=DIRECTION ( 'NONE',  ( 1.000000000000000000, -5.782411586589331015E-16, 0.000000000000000000 ) ) ;
#2264=PLANE ( 'NONE',  #31213 ) ;
#2287=DIRECTION ( 'NONE',  ( -1.000000000000000000, 0.000000000000000000, 0.000000000000000000 ) ) ;
#2293=EDGE_CURVE ( 'NONE', #27282, #51168, #34561, .T. ) ;
#2296=ORIENTED_EDGE ( 'NONE', *, *, #43191, .F. ) ;
#2306=DIRECTION ( 'NONE',  ( 0.000000000000000000, 0.000000000000000000, -1.000000000000000000 ) ) ;
#2323=ORIENTED_EDGE ( 'NONE', *, *, #64532, .T. ) ;
#2325=VERTEX_POINT ( 'NONE', #8204 ) ;
#2344=FACE_OUTER_BOUND ( 'NONE', #23122, .T. ) ;
#2352=ORIENTED_EDGE ( 'NONE', *, *, #23333, .T. ) ;
#2357=FACE_OUTER_BOUND ( 'NONE', #8309, .T. ) ;
#2373=VECTOR ( 'NONE', #25912, 1000.000000000000000 ) ;
#2387=VERTEX_POINT ( 'NONE', #18410 ) ;
#2391=VECTOR ( 'NONE', #35253, 1000.000000000000000 ) ;
#2405=DIRECTION ( 'NONE',  ( 1.000000000000000000, 0.000000000000000000, 0.000000000000000000 ) ) ;
#2437=ORIENTED_EDGE ( 'NONE', *, *, #30727, .T. ) ;
#2441=DIRECTION ( 'NONE',  ( 0.000000000000000000, -1.000000000000000000, 0.000000000000000000 ) ) ;
#2465=DIRECTION ( 'NONE',  ( -0.000000000000000000, -0.000000000000000000, 1.000000000000000000 ) ) ;
#2521=DIRECTION ( 'NONE',  ( -1.000000000000000000, 0.000000000000000000, 0.000000000000000000 ) ) ;
#2540=EDGE_LOOP ( 'NONE', ( #19733, #39653, #35537, #69008 ) ) ;
#2586=LINE ( 'NONE', #18480, #2227 ) ;
#2602=SPHERICAL_SURFACE ( 'NONE', #46627, 1.000000000000000000 ) ;
#2608=CYLINDRICAL_SURFACE ( 'NONE', #20971, 0.2500000000000002220 ) ;
#2620=ORIENTED_EDGE ( 'NONE', *, *, #36828, .T. ) ;
#2633=DIRECTION ( 'NONE',  ( 0.000000000000000000, -0.000000000000000000, -1.000000000000000000 ) ) ;
#2641=FACE_OUTER_BOUND ( 'NONE', #31961, .T. ) ;
#2653=DIRECTION ( 'NONE',  ( 0.000000000000000000, 0.000000000000000000, -1.000000000000000000 ) ) ;
#2666=FACE_OUTER_BOUND ( 'NONE', #24215, .T. ) ;
#2683=ORIENTED_EDGE ( 'NONE', *, *, #22324, .T. ) ;
#2706=AXIS2_PLACEMENT_3D ( 'NONE', #61530, #13358, #56272 ) ;
#2720=LINE ( 'NONE', #7685, #14959 ) ;
#2726=DIRECTION ( 'NONE',  ( 1.000000000000000000, 0.000000000000000000, 0.000000000000000000 ) ) ;
#2729=ORIENTED_EDGE ( 'NONE', *, *, #162, .F. ) ;
#2756=CARTESIAN_POINT ( 'NONE',  ( 22.75000000000000711, 34.24999999999999289, -3.750000000000000000 ) ) ;
#2762=TOROIDAL_SURFACE ( 'NONE', #42179, 0.7500000000000000000, 0.2500000000000000000 ) ;
#2779=AXIS2_PLACEMENT_3D ( 'NONE', #48093, #16068, #16753 ) ;
#2782=VERTEX_POINT ( 'NONE', #35190 ) ;
#2787=DIRECTION ( 'NONE',  ( -0.000000000000000000, -0.000000000000000000, 1.000000000000000000 ) ) ;
#2803=FACE_OUTER_BOUND ( 'NONE', #44040, .T. ) ;
#2811=VECTOR ( 'NONE', #8473, 1000.000000000000000 ) ;
#2816=DIRECTION ( 'NONE',  ( 0.000000000000000000, 0.000000000000000000, -1.000000000000000000 ) ) ;
#2834=EDGE_CURVE ( 'NONE', #55052, #54990, #66869, .T. ) ;
#2835=VECTOR ( 'NONE', #68851, 1000.000000000000000 ) ;
#2855=DIRECTION ( 'NONE',  ( -0.000000000000000000, 0.000000000000000000, -1.000000000000000000 ) ) ;
#2864=ORIENTED_EDGE ( 'NONE', *, *, #23515, .F. ) ;
#2866=CYLINDRICAL_SURFACE ( 'NONE', #18162, 0.2500000000000002220 ) ;
#2898=PLANE ( 'NONE',  #53034 ) ;
#2925=PRODUCT_DEFINITION_CONTEXT ( 'detailed design', #24878, 'design' ) ;
#2930=CARTESIAN_POINT ( 'NONE',  ( 9.250000000000003553, 27.74999999999998934, 3.750000000000000000 ) ) ;
#2940=EDGE_CURVE ( 'NONE', #40236, #53491, #32997, .T. ) ;
#2945=VERTEX_POINT ( 'NONE', #48207 ) ;
#2950=DIRECTION ( 'NONE',  ( 0.000000000000000000, 1.000000000000000000, 0.000000000000000000 ) ) ;
#2958=DIRECTION ( 'NONE',  ( 1.000000000000000000, 0.000000000000000000, 0.000000000000000000 ) ) ;
#2975=CARTESIAN_POINT ( 'NONE',  ( 22.25000000000000711, 33.99999999999999289, 3.750000000000000000 ) ) ;
#3009=EDGE_LOOP ( 'NONE', ( #30945, #2323, #43, #57017 ) ) ;
#3010=ORIENTED_EDGE ( 'NONE', *, *, #4675, .F. ) ;
#3015=ORIENTED_EDGE ( 'NONE', *, *, #20735, .F. ) ;
#3018=AXIS2_PLACEMENT_3D ( 'NONE', #1300, #11569, #22478 ) ;
#3022=ADVANCED_FACE ( 'NONE', ( #11915 ), #26353, .F. ) ;
#3050=DIRECTION ( 'NONE',  ( 0.000000000000000000, 0.000000000000000000, -1.000000000000000000 ) ) ;
#3125=CARTESIAN_POINT ( 'NONE',  ( -22.75000000000000711, 34.24999999999999289, 4.000000000000000000 ) ) ;
#3130=CARTESIAN_POINT ( 'NONE',  ( -24.75000000000000355, 36.75000000000000000, 3.000000000000000000 ) ) ;
#3173=CARTESIAN_POINT ( 'NONE',  ( 0.000000000000000000, 27.74999999999998934, 4.000000000000000000 ) ) ;
#3176=DIRECTION ( 'NONE',  ( -0.000000000000000000, -0.000000000000000000, 1.000000000000000000 ) ) ;
#3180=LINE ( 'NONE', #8540, #68655 ) ;
#3191=EDGE_CURVE ( 'NONE', #35189, #66039, #65888, .T. ) ;
#3252=AXIS2_PLACEMENT_3D ( 'NONE', #46347, #2653, #61418 ) ;
#3265=CARTESIAN_POINT ( 'NONE',  ( 15.00000000000000000, 8.000000000000000000, 4.000000000000000000 ) ) ;
#3339=CARTESIAN_POINT ( 'NONE',  ( 24.00000000000000000, 1.000000000000000888, -3.000000000000000000 ) ) ;
#3344=CARTESIAN_POINT ( 'NONE',  ( -22.75000000000000711, 0.000000000000000000, 3.750000000000000000 ) ) ;
#3361=EDGE_LOOP ( 'NONE', ( #20498, #19017, #55925, #27193, #17474, #37527 ) ) ;
#3366=DIRECTION ( 'NONE',  ( 0.000000000000000000, 0.000000000000000000, 1.000000000000000000 ) ) ;
#3407=FACE_OUTER_BOUND ( 'NONE', #39060, .T. ) ;
#3423=ORIENTED_EDGE ( 'NONE', *, *, #43191, .T. ) ;
#3455=LINE ( 'NONE', #29542, #15883 ) ;
#3466=ORIENTED_EDGE ( 'NONE', *, *, #46283, .T. ) ;
#3477=ORIENTED_EDGE ( 'NONE', *, *, #1217, .F. ) ;
#3485=EDGE_CURVE ( 'NONE', #51168, #66608, #5270, .T. ) ;
#3486=EDGE_LOOP ( 'NONE', ( #17034, #32502, #990, #4722 ) ) ;
#3487=LINE ( 'NONE', #51043, #43080 ) ;
#3508=TOROIDAL_SURFACE ( 'NONE', #11429, 0.5000000000000000000, 0.2500000000000000000 ) ;
#3511=EDGE_LOOP ( 'NONE', ( #54066, #9067, #54459, #54187 ) ) ;
#3520=AXIS2_PLACEMENT_3D ( 'NONE', #18700, #29229, #55972 ) ;
#3523=DIRECTION ( 'NONE',  ( -1.000000000000000000, 0.000000000000000000, 0.000000000000000000 ) ) ;
#3537=ORIENTED_EDGE ( 'NONE', *, *, #16397, .F. ) ;
#3571=CARTESIAN_POINT ( 'NONE',  ( -13.25000000000000355, 28.24999999999998934, 4.000000000000000000 ) ) ;
#3579=DIRECTION ( 'NONE',  ( -1.000000000000000000, 0.000000000000000000, 0.000000000000000000 ) ) ;
#3582=ORIENTED_EDGE ( 'NONE', *, *, #14094, .F. ) ;
#3597=DIRECTION ( 'NONE',  ( 0.000000000000000000, 0.000000000000000000, -1.000000000000000000 ) ) ;
#3617=FILL_AREA_STYLE ('',( #46971 ) ) ;
#3624=DIRECTION ( 'NONE',  ( 0.000000000000000000, 0.000000000000000000, 1.000000000000000000 ) ) ;
#3739=DIRECTION ( 'NONE',  ( -1.000000000000000000, 0.000000000000000000, 0.000000000000000000 ) ) ;
#3754=ORIENTED_EDGE ( 'NONE', *, *, #51669, .F. ) ;
#3763=FACE_OUTER_BOUND ( 'NONE', #925, .T. ) ;
#3806=DIRECTION ( 'NONE',  ( 0.000000000000000000, 0.000000000000000000, -1.000000000000000000 ) ) ;
#3809=EDGE_CURVE ( 'NONE', #38442, #68484, #41316, .T. ) ;
#3870=ADVANCED_FACE ( 'NONE', ( #69628 ), #33387, .T. ) ;
#3939=EDGE_LOOP ( 'NONE', ( #14966, #12743, #26301, #13717 ) ) ;
#3959=CARTESIAN_POINT ( 'NONE',  ( 13.75000000000000533, 30.74999999999999289, 3.750000000000000000 ) ) ;
#3966=AXIS2_PLACEMENT_3D ( 'NONE', #21681, #9418, #63214 ) ;
#3976=EDGE_CURVE ( 'NONE', #65417, #61564, #61491, .T. ) ;
#4025=ORIENTED_EDGE ( 'NONE', *, *, #2940, .T. ) ;
#4036=ADVANCED_FACE ( 'NONE', ( #24533 ), #12960, .F. ) ;
#4063=DIRECTION ( 'NONE',  ( 0.000000000000000000, 0.000000000000000000, 1.000000000000000000 ) ) ;
#4084=CARTESIAN_POINT ( 'NONE',  ( 9.250000000000003553, 25.24999999999998934, -3.750000000000000000 ) ) ;
#4090=ORIENTED_EDGE ( 'NONE', *, *, #35258, .F. ) ;
#4093=ORIENTED_EDGE ( 'NONE', *, *, #62014, .F. ) ;
#4095=LINE ( 'NONE', #14694, #2373 ) ;
#4109=EDGE_CURVE ( 'NONE', #68484, #454, #28991, .T. ) ;
#4127=DIRECTION ( 'NONE',  ( -0.000000000000000000, -0.000000000000000000, 1.000000000000000000 ) ) ;
#4188=DIRECTION ( 'NONE',  ( -1.000000000000000000, 0.000000000000000000, 0.000000000000000000 ) ) ;
#4192=CARTESIAN_POINT ( 'NONE',  ( 24.00000000000000355, 37.00000000000000000, -3.000000000000000000 ) ) ;
#4212=AXIS2_PLACEMENT_3D ( 'NONE', #54806, #6990, #18237 ) ;
#4221=LINE ( 'NONE', #63690, #60754 ) ;
#4237=CYLINDRICAL_SURFACE ( 'NONE', #28074, 0.2500000000000002220 ) ;
#4253=EDGE_CURVE ( 'NONE', #6972, #9166, #11496, .T. ) ;
#4299=CARTESIAN_POINT ( 'NONE',  ( 24.00000000000000000, 1.000000000000000000, -4.000000000000000000 ) ) ;
#4317=CIRCLE ( 'NONE', #2016, 0.2500000000000002220 ) ;
#4319=ADVANCED_FACE ( 'NONE', ( #16116 ), #180, .F. ) ;
#4322=DIRECTION ( 'NONE',  ( 0.000000000000000000, 0.000000000000000000, 1.000000000000000000 ) ) ;
#4332=DIRECTION ( 'NONE',  ( 0.000000000000000000, 0.000000000000000000, 1.000000000000000000 ) ) ;
#4345=CARTESIAN_POINT ( 'NONE',  ( 25.00000000000000000, 1.000000000000000888, 3.000000000000000000 ) ) ;
#4354=CARTESIAN_POINT ( 'NONE',  ( 10.50000000000002309, 8.000000000000000000, -4.000000000000000000 ) ) ;
#4355=EDGE_LOOP ( 'NONE', ( #20650, #24455, #17466, #45196 ) ) ;
#4360=DIRECTION ( 'NONE',  ( -0.000000000000000000, -0.000000000000000000, 1.000000000000000000 ) ) ;
#4377=CARTESIAN_POINT ( 'NONE',  ( 15.00000000000000000, 8.000000000000000000, 4.000000000000000000 ) ) ;
#4400=CYLINDRICAL_SURFACE ( 'NONE', #14552, 0.2500000000000002220 ) ;
#4405=DIRECTION ( 'NONE',  ( -5.782411586589351722E-16, 1.000000000000000000, 0.000000000000000000 ) ) ;
#4409=AXIS2_PLACEMENT_3D ( 'NONE', #41376, #68429, #10395 ) ;
#4438=VERTEX_POINT ( 'NONE', #61734 ) ;
#4471=ORIENTED_EDGE ( 'NONE', *, *, #21273, .F. ) ;
#4473=DIRECTION ( 'NONE',  ( 0.000000000000000000, 0.000000000000000000, -1.000000000000000000 ) ) ;
#4511=FACE_OUTER_BOUND ( 'NONE', #28390, .T. ) ;
#4516=EDGE_CURVE ( 'NONE', #64993, #46369, #51557, .T. ) ;
#4522=DIRECTION ( 'NONE',  ( 1.000000000000000000, -0.000000000000000000, 0.000000000000000000 ) ) ;
#4545=ORIENTED_EDGE ( 'NONE', *, *, #69589, .T. ) ;
#4585=EDGE_LOOP ( 'NONE', ( #55170, #13122, #24697, #17376 ) ) ;
#4661=DIRECTION ( 'NONE',  ( -1.000000000000000000, 0.000000000000000000, 0.000000000000000000 ) ) ;
#4675=EDGE_CURVE ( 'NONE', #46607, #16845, #27927, .T. ) ;
#4678=VECTOR ( 'NONE', #1348, 1000.000000000000000 ) ;
#4694=EDGE_CURVE ( 'NONE', #66883, #50598, #68441, .T. ) ;
#4698=ADVANCED_FACE ( 'NONE', ( #54997 ), #55367, .T. ) ;
#4700=CARTESIAN_POINT ( 'NONE',  ( 18.25000000000000711, 31.24999999999999289, -3.750000000000000000 ) ) ;
#4717=DIRECTION ( 'NONE',  ( 0.000000000000000000, 8.673617379884035472E-16, -1.000000000000000000 ) ) ;
#4722=ORIENTED_EDGE ( 'NONE', *, *, #36084, .T. ) ;
#4736=AXIS2_PLACEMENT_3D ( 'NONE', #44717, #66108, #6335 ) ;
#4747=CARTESIAN_POINT ( 'NONE',  ( 17.75000000000000711, 31.24999999999999289, 4.000000000000000000 ) ) ;
#4753=AXIS2_PLACEMENT_3D ( 'NONE', #38353, #28408, #607 ) ;
#4757=CARTESIAN_POINT ( 'NONE',  ( 9.000000000000003553, 24.74999999999998579, -3.750000000000000000 ) ) ;
#4786=CARTESIAN_POINT ( 'NONE',  ( -10.50000000000002309, 8.000000000000000000, -4.000000000000000000 ) ) ;
#4821=CARTESIAN_POINT ( 'NONE',  ( -13.75000000000000533, 30.74999999999999289, -4.000000000000000000 ) ) ;
#4824=ADVANCED_FACE ( 'NONE', ( #13482 ), #40377, .T. ) ;
#4831=CIRCLE ( 'NONE', #40771, 0.2500000000000002220 ) ;
#4853=AXIS2_PLACEMENT_3D ( 'NONE', #64360, #12252, #6626 ) ;
#4879=DIRECTION ( 'NONE',  ( -0.000000000000000000, -0.000000000000000000, 1.000000000000000000 ) ) ;
#4881=AXIS2_PLACEMENT_3D ( 'NONE', #62106, #66004, #23433 ) ;
#4886=CARTESIAN_POINT ( 'NONE',  ( 4.750000000000002665, 22.24999999999998579, -3.750000000000000000 ) ) ;
#4888=CARTESIAN_POINT ( 'NONE',  ( 9.000000000000003553, 24.99999999999998579, 4.000000000000000000 ) ) ;
#4915=ORIENTED_EDGE ( 'NONE', *, *, #39621, .F. ) ;
#4929=DIRECTION ( 'NONE',  ( 0.000000000000000000, 0.000000000000000000, -1.000000000000000000 ) ) ;
#4943=CIRCLE ( 'NONE', #53263, 1.000000000000000000 ) ;
#4957=CIRCLE ( 'NONE', #47704, 0.2500000000000002220 ) ;
#4995=DIRECTION ( 'NONE',  ( 0.000000000000000000, 1.000000000000000000, 0.000000000000000000 ) ) ;
#5002=AXIS2_PLACEMENT_3D ( 'NONE', #60979, #7526, #34594 ) ;
#5041=CARTESIAN_POINT ( 'NONE',  ( 18.00000000000000711, 33.99999999999999289, 4.000000000000000000 ) ) ;
#5046=AXIS2_PLACEMENT_3D ( 'NONE', #47564, #67939, #53139 ) ;
#5051=VERTEX_POINT ( 'NONE', #29500 ) ;
#5053=AXIS2_PLACEMENT_3D ( 'NONE', #44819, #23663, #39535 ) ;
#5059=CARTESIAN_POINT ( 'NONE',  ( -24.00000000000000000, 1.000000000000000000, -4.000000000000000000 ) ) ;
#5062=PLANE ( 'NONE',  #17437 ) ;
#5074=DIRECTION ( 'NONE',  ( -1.000000000000000000, 0.000000000000000000, 0.000000000000000000 ) ) ;
#5143=DIRECTION ( 'NONE',  ( 0.000000000000000000, -1.000000000000000000, 0.000000000000000000 ) ) ;
#5153=DIRECTION ( 'NONE',  ( 1.000000000000000000, 0.000000000000000000, 0.000000000000000000 ) ) ;
#5159=EDGE_CURVE ( 'NONE', #27999, #6972, #26419, .T. ) ;
#5198=CARTESIAN_POINT ( 'NONE',  ( -15.00000000000000000, 8.000000000000000000, 3.500000000000003997 ) ) ;
#5210=AXIS2_PLACEMENT_3D ( 'NONE', #20300, #9073, #20666 ) ;
#5215=ORIENTED_EDGE ( 'NONE', *, *, #55313, .F. ) ;
#5267=DIRECTION ( 'NONE',  ( -1.000000000000000000, 0.000000000000000000, 0.000000000000000000 ) ) ;
#5269=DIRECTION ( 'NONE',  ( -1.000000000000000000, 0.000000000000000000, -0.000000000000000000 ) ) ;
#5270=CIRCLE ( 'NONE', #31077, 0.2500000000000002220 ) ;
#5274=DIRECTION ( 'NONE',  ( 0.000000000000000000, 1.000000000000000000, 0.000000000000000000 ) ) ;
#5292=EDGE_CURVE ( 'NONE', #34410, #12869, #11853, .T. ) ;
#5295=ORIENTED_EDGE ( 'NONE', *, *, #26733, .F. ) ;
#5301=CIRCLE ( 'NONE', #52556, 4.499999999999997335 ) ;
#5321=EDGE_CURVE ( 'NONE', #58314, #2782, #32055, .T. ) ;
#5335=ORIENTED_EDGE ( 'NONE', *, *, #56471, .F. ) ;
#5366=VERTEX_POINT ( 'NONE', #38637 ) ;
#5373=CARTESIAN_POINT ( 'NONE',  ( -18.25000000000000711, 33.99999999999999289, -3.750000000000000000 ) ) ;
#5377=CARTESIAN_POINT ( 'NONE',  ( 19.49999999999999645, 8.000000000000000000, 4.000000000000000000 ) ) ;
#5413=VERTEX_POINT ( 'NONE', #19189 ) ;
#5434=DIRECTION ( 'NONE',  ( -1.000000000000000000, 0.000000000000000000, 0.000000000000000000 ) ) ;
#5437=VECTOR ( 'NONE', #2855, 1000.000000000000000 ) ;
#5459=EDGE_CURVE ( 'NONE', #12723, #15255, #57976, .T. ) ;
#5464=EDGE_CURVE ( 'NONE', #12869, #66608, #69170, .T. ) ;
#5513=LINE ( 'NONE', #53722, #61043 ) ;
#5548=LINE ( 'NONE', #49454, #60671 ) ;
#5560=ORIENTED_EDGE ( 'NONE', *, *, #21616, .F. ) ;
#5564=CARTESIAN_POINT ( 'NONE',  ( -8.750000000000001776, 24.99999999999998579, 3.750000000000000000 ) ) ;
#5580=VERTEX_POINT ( 'NONE', #5564 ) ;
#5588=LINE ( 'NONE', #36976, #59886 ) ;
#5615=DIRECTION ( 'NONE',  ( -1.000000000000000000, 0.000000000000000000, 0.000000000000000000 ) ) ;
#5635=AXIS2_PLACEMENT_3D ( 'NONE', #47921, #9556, #26036 ) ;
#5641=CARTESIAN_POINT ( 'NONE',  ( -13.25000000000000355, 28.24999999999998934, 3.750000000000000000 ) ) ;
#5652=LINE ( 'NONE', #68673, #67230 ) ;
#5675=DIRECTION ( 'NONE',  ( 0.000000000000000000, 0.000000000000000000, -1.000000000000000000 ) ) ;
#5688=LINE ( 'NONE', #23280, #66484 ) ;
#5697=DIRECTION ( 'NONE',  ( 0.000000000000000000, 0.000000000000000000, -1.000000000000000000 ) ) ;
#5711=ADVANCED_FACE ( 'NONE', ( #28758 ), #59060, .T. ) ;
#5721=ORIENTED_EDGE ( 'NONE', *, *, #66820, .F. ) ;
#5753=VERTEX_POINT ( 'NONE', #12228 ) ;
#5758=ORIENTED_EDGE ( 'NONE', *, *, #24437, .T. ) ;
#5771=FACE_OUTER_BOUND ( 'NONE', #67341, .T. ) ;
#5792=EDGE_CURVE ( 'NONE', #65139, #55052, #25226, .T. ) ;
#5807=CARTESIAN_POINT ( 'NONE',  ( 24.00000000000000355, 36.75000000000000000, -3.000000000000000000 ) ) ;
#5837=DIRECTION ( 'NONE',  ( -0.000000000000000000, -0.000000000000000000, 1.000000000000000000 ) ) ;
#5878=ADVANCED_FACE ( 'NONE', ( #37916 ), #62330, .T. ) ;
#5889=DIRECTION ( 'NONE',  ( -1.000000000000000000, 0.000000000000000000, 0.000000000000000000 ) ) ;
#5943=ORIENTED_EDGE ( 'NONE', *, *, #12857, .F. ) ;
#5972=EDGE_CURVE ( 'NONE', #5413, #57180, #50767, .T. ) ;
#5978=EDGE_CURVE ( 'NONE', #46369, #33026, #11767, .T. ) ;
#5981=FACE_OUTER_BOUND ( 'NONE', #29803, .T. ) ;
#6009=LINE ( 'NONE', #59825, #41755 ) ;
#6033=DIRECTION ( 'NONE',  ( 1.000000000000000000, -0.000000000000000000, 0.000000000000000000 ) ) ;
#6056=EDGE_CURVE ( 'NONE', #24031, #5051, #47783, .T. ) ;
#6088=ORIENTED_EDGE ( 'NONE', *, *, #66135, .T. ) ;
#6102=CARTESIAN_POINT ( 'NONE',  ( -24.00000000000000355, 36.75000000000000000, -3.750000000000000000 ) ) ;
#6122=DIRECTION ( 'NONE',  ( 0.000000000000000000, 0.000000000000000000, 1.000000000000000000 ) ) ;
#6137=CIRCLE ( 'NONE', #33111, 0.2500000000000002220 ) ;
#6153=AXIS2_PLACEMENT_3D ( 'NONE', #36986, #58399, #4929 ) ;
#6207=AXIS2_PLACEMENT_3D ( 'NONE', #62595, #14409, #24970 ) ;
#6260=FACE_OUTER_BOUND ( 'NONE', #27726, .T. ) ;
#6267=EDGE_CURVE ( 'NONE', #58659, #65395, #22858, .T. ) ;
#6291=CARTESIAN_POINT ( 'NONE',  ( 18.00000000000000711, 33.99999999999999289, 3.750000000000000000 ) ) ;
#6298=SPHERICAL_SURFACE ( 'NONE', #4853, 0.2500000000000000000 ) ;
#6304=VECTOR ( 'NONE', #42769, 1000.000000000000000 ) ;
#6335=DIRECTION ( 'NONE',  ( 0.000000000000000000, 0.000000000000000000, -1.000000000000000000 ) ) ;
#6343=AXIS2_PLACEMENT_3D ( 'NONE', #43881, #5837, #32570 ) ;
#6353=FACE_BOUND ( 'NONE', #52622, .T. ) ;
#6357=ORIENTED_EDGE ( 'NONE', *, *, #33765, .T. ) ;
#6378=CIRCLE ( 'NONE', #68153, 4.499999999999997335 ) ;
#6382=CARTESIAN_POINT ( 'NONE',  ( 13.50000000000000533, 30.74999999999999289, -3.750000000000000000 ) ) ;
#6395=DIRECTION ( 'NONE',  ( -0.000000000000000000, -0.000000000000000000, 1.000000000000000000 ) ) ;
#6420=EDGE_CURVE ( 'NONE', #61213, #65002, #30708, .T. ) ;
#6425=VERTEX_POINT ( 'NONE', #39816 ) ;
#6430=CARTESIAN_POINT ( 'NONE',  ( 15.00000000000000000, 8.000000000000000000, -4.000000000000000000 ) ) ;
#6434=CARTESIAN_POINT ( 'NONE',  ( -13.75000000000000533, 30.74999999999999289, -3.750000000000000000 ) ) ;
#6447=ORIENTED_EDGE ( 'NONE', *, *, #24307, .T. ) ;
#6456=ORIENTED_EDGE ( 'NONE', *, *, #64984, .T. ) ;
#6463=AXIS2_PLACEMENT_3D ( 'NONE', #35485, #34767, #14357 ) ;
#6479=DIRECTION ( 'NONE',  ( 0.000000000000000000, 0.000000000000000000, -1.000000000000000000 ) ) ;
#6504=ADVANCED_FACE ( 'NONE', ( #25326 ), #56579, .T. ) ;
#6509=ORIENTED_EDGE ( 'NONE', *, *, #19367, .F. ) ;
#6532=DIRECTION ( 'NONE',  ( 0.000000000000000000, 1.000000000000000000, -0.000000000000000000 ) ) ;
#6544=VECTOR ( 'NONE', #531, 1000.000000000000000 ) ;
#6561=AXIS2_PLACEMENT_3D ( 'NONE', #23854, #18595, #9080 ) ;
#6620=DIRECTION ( 'NONE',  ( 0.000000000000000000, 0.000000000000000000, -1.000000000000000000 ) ) ;
#6626=DIRECTION ( 'NONE',  ( -1.000000000000000000, 0.000000000000000000, 0.000000000000000000 ) ) ;
#6634=LINE ( 'NONE', #60793, #63116 ) ;
#6638=DIRECTION ( 'NONE',  ( -0.000000000000000000, -0.000000000000000000, 1.000000000000000000 ) ) ;
#6646=EDGE_CURVE ( 'NONE', #24031, #35855, #58854, .T. ) ;
#6652=VERTEX_POINT ( 'NONE', #63655 ) ;
#6699=ORIENTED_EDGE ( 'NONE', *, *, #69661, .F. ) ;
#6715=DIRECTION ( 'NONE',  ( 0.000000000000000000, 0.000000000000000000, 1.000000000000000000 ) ) ;
#6750=DIRECTION ( 'NONE',  ( -1.000000000000000000, 0.000000000000000000, 0.000000000000000000 ) ) ;
#6800=CARTESIAN_POINT ( 'NONE',  ( 13.25000000000000355, 27.74999999999998934, 4.000000000000000000 ) ) ;
#6838=ADVANCED_FACE ( 'NONE', ( #23850 ), #30855, .T. ) ;
#6873=EDGE_LOOP ( 'NONE', ( #59411, #18653, #45529, #52071, #19636, #63820, #39133, #42843, #35291, #42896, #20298, #40169, #15137, #47208, #58021, #54180, #55801, #44993, #8857, #11785, #68496, #14007, #12956, #19187, #3423, #11631, #35076, #61315, #48548, #23159, #57346, #22367, #2058, #21614 ) ) ;
#6874=CIRCLE ( 'NONE', #13597, 1.000000000000000888 ) ;
#6884=CARTESIAN_POINT ( 'NONE',  ( 25.00000000000000355, 36.75000000000000000, 4.000000000000000000 ) ) ;
#6902=VECTOR ( 'NONE', #40611, 1000.000000000000000 ) ;
#6927=LINE ( 'NONE', #7968, #9464 ) ;
#6933=CYLINDRICAL_SURFACE ( 'NONE', #18948, 4.000000000000000000 ) ;
#6951=VECTOR ( 'NONE', #40988, 1000.000000000000000 ) ;
#6953=AXIS2_PLACEMENT_3D ( 'NONE', #65979, #1565, #12155 ) ;
#6966=DIRECTION ( 'NONE',  ( 0.000000000000000000, -1.000000000000000000, 0.000000000000000000 ) ) ;
#6972=VERTEX_POINT ( 'NONE', #35101 ) ;
#6985=CYLINDRICAL_SURFACE ( 'NONE', #12570, 0.2500000000000002220 ) ;
#6990=DIRECTION ( 'NONE',  ( 0.000000000000000000, 1.000000000000000000, 0.000000000000000000 ) ) ;
#7029=CIRCLE ( 'NONE', #28333, 0.2500000000000002220 ) ;
#7142=ORIENTED_EDGE ( 'NONE', *, *, #1217, .T. ) ;
#7148=CARTESIAN_POINT ( 'NONE',  ( -9.000000000000003553, 27.99999999999998934, 3.750000000000000000 ) ) ;
#7151=CIRCLE ( 'NONE', #10527, 0.2500000000000002220 ) ;
#7174=CARTESIAN_POINT ( 'NONE',  ( -25.00000000000000000, -9.376883653928695991E-17, -3.000000000000000000 ) ) ;
#7192=DIRECTION ( 'NONE',  ( 0.000000000000000000, 0.000000000000000000, -1.000000000000000000 ) ) ;
#7203=AXIS2_PLACEMENT_3D ( 'NONE', #56130, #7956, #19886 ) ;
#7217=DIRECTION ( 'NONE',  ( 0.000000000000000000, 0.000000000000000000, 1.000000000000000000 ) ) ;
#7220=CARTESIAN_POINT ( 'NONE',  ( -9.000000000000003553, 25.24999999999998934, 3.750000000000000000 ) ) ;
#7223=LINE ( 'NONE', #43521, #60397 ) ;
#7236=ORIENTED_EDGE ( 'NONE', *, *, #26668, .F. ) ;
#7239=CIRCLE ( 'NONE', #65628, 0.2500000000000002220 ) ;
#7240=VECTOR ( 'NONE', #34753, 1000.000000000000000 ) ;
#7253=AXIS2_PLACEMENT_3D ( 'NONE', #43469, #22291, #16016 ) ;
#7265=VERTEX_POINT ( 'NONE', #47731 ) ;
#7278=VECTOR ( 'NONE', #46445, 1000.000000000000000 ) ;
#7280=ORIENTED_EDGE ( 'NONE', *, *, #60652, .T. ) ;
#7291=ORIENTED_EDGE ( 'NONE', *, *, #6420, .T. ) ;
#7294=AXIS2_PLACEMENT_3D ( 'NONE', #7896, #34981, #51174 ) ;
#7321=DIRECTION ( 'NONE',  ( 0.000000000000000000, 0.000000000000000000, -1.000000000000000000 ) ) ;
#7335=CARTESIAN_POINT ( 'NONE',  ( -9.000000000000003553, 27.74999999999998934, -3.750000000000000000 ) ) ;
#7340=CARTESIAN_POINT ( 'NONE',  ( -13.75000000000000533, 30.74999999999999289, 4.000000000000000000 ) ) ;
#7349=CARTESIAN_POINT ( 'NONE',  ( -24.00000000000000000, 0.000000000000000000, 3.000000000000000000 ) ) ;
#7362=ORIENTED_EDGE ( 'NONE', *, *, #21038, .T. ) ;
#7366=ORIENTED_EDGE ( 'NONE', *, *, #66820, .T. ) ;
#7384=DIRECTION ( 'NONE',  ( -1.000000000000000000, 9.376883653928687363E-17, 0.000000000000000000 ) ) ;
#7394=CIRCLE ( 'NONE', #68061, 0.2500000000000002220 ) ;
#7426=DIRECTION ( 'NONE',  ( 0.000000000000000000, 0.000000000000000000, -1.000000000000000000 ) ) ;
#7431=ORIENTED_EDGE ( 'NONE', *, *, #65749, .T. ) ;
#7441=FACE_OUTER_BOUND ( 'NONE', #53953, .T. ) ;
#7475=ADVANCED_FACE ( 'NONE', ( #50781 ), #40952, .F. ) ;
#7478=DIRECTION ( 'NONE',  ( 0.000000000000000000, 0.000000000000000000, -1.000000000000000000 ) ) ;
#7526=DIRECTION ( 'NONE',  ( -0.000000000000000000, -0.000000000000000000, 1.000000000000000000 ) ) ;
#7538=DIRECTION ( 'NONE',  ( 0.000000000000000000, -1.000000000000000000, 0.000000000000000000 ) ) ;
#7556=DIRECTION ( 'NONE',  ( 0.000000000000000000, 0.000000000000000000, 1.000000000000000000 ) ) ;
#7562=CARTESIAN_POINT ( 'NONE',  ( 15.00000000000000000, 8.000000000000000000, -3.500000000000017764 ) ) ;
#7568=DIRECTION ( 'NONE',  ( 1.000000000000000000, 0.000000000000000000, 0.000000000000000000 ) ) ;
#7585=DIRECTION ( 'NONE',  ( 0.000000000000000000, 1.000000000000000000, -0.000000000000000000 ) ) ;
#7594=AXIS2_PLACEMENT_3D ( 'NONE', #65730, #49568, #1662 ) ;
#7603=DIRECTION ( 'NONE',  ( 0.000000000000000000, 0.000000000000000000, -1.000000000000000000 ) ) ;
#7609=CARTESIAN_POINT ( 'NONE',  ( -24.00000000000000355, 37.00000000000000000, -3.000000000000000000 ) ) ;
#7645=CARTESIAN_POINT ( 'NONE',  ( -9.250000000000003553, 25.24999999999998934, -3.750000000000000000 ) ) ;
#7661=EDGE_CURVE ( 'NONE', #64274, #47479, #26352, .T. ) ;
#7666=ORIENTED_EDGE ( 'NONE', *, *, #24363, .T. ) ;
#7685=CARTESIAN_POINT ( 'NONE',  ( 22.50000000000000711, 34.24999999999999289, -3.750000000000000000 ) ) ;
#7687=ORIENTED_EDGE ( 'NONE', *, *, #11696, .T. ) ;
#7696=ADVANCED_FACE ( 'NONE', ( #2344 ), #30822, .F. ) ;
#7703=EDGE_CURVE ( 'NONE', #19696, #2945, #23191, .T. ) ;
#7723=ORIENTED_EDGE ( 'NONE', *, *, #32096, .T. ) ;
#7732=VECTOR ( 'NONE', #45974, 1000.000000000000000 ) ;
#7733=ORIENTED_EDGE ( 'NONE', *, *, #39187, .F. ) ;
#7740=EDGE_LOOP ( 'NONE', ( #48842, #5721, #50466, #69691 ) ) ;
#7776=LINE ( 'NONE', #40172, #43850 ) ;
#7788=LINE ( 'NONE', #29237, #62274 ) ;
#7830=DIRECTION ( 'NONE',  ( 1.000000000000000000, 0.000000000000000000, 0.000000000000000000 ) ) ;
#7896=CARTESIAN_POINT ( 'NONE',  ( 9.250000000000003553, 27.74999999999998934, -3.750000000000000000 ) ) ;
#7901=CIRCLE ( 'NONE', #21402, 0.2500000000000002220 ) ;
#7946=ADVANCED_FACE ( 'NONE', ( #54055 ), #36508, .T. ) ;
#7956=DIRECTION ( 'NONE',  ( 0.000000000000000000, 0.000000000000000000, -1.000000000000000000 ) ) ;
#7961=VECTOR ( 'NONE', #54841, 999.9999999999998863 ) ;
#7964=CARTESIAN_POINT ( 'NONE',  ( 15.00000000000000000, 8.000000000000000000, 4.000000000000000000 ) ) ;
#7965=CARTESIAN_POINT ( 'NONE',  ( 13.75000000000000533, 30.74999999999999289, -3.750000000000000000 ) ) ;
#7968=CARTESIAN_POINT ( 'NONE',  ( 25.00000000000000355, 37.00000000000000000, -3.000000000000000000 ) ) ;
#8003=TOROIDAL_SURFACE ( 'NONE', #59723, 0.7500000000000000000, 0.2500000000000000000 ) ;
#8007=EDGE_CURVE ( 'NONE', #12301, #37934, #49987, .T. ) ;
#8030=AXIS2_PLACEMENT_3D ( 'NONE', #19376, #24637, #2816 ) ;
#8054=DIRECTION ( 'NONE',  ( 0.000000000000000000, 0.000000000000000000, -1.000000000000000000 ) ) ;
#8062=CARTESIAN_POINT ( 'NONE',  ( 24.00000000000000355, 36.75000000000000000, -4.000000000000000000 ) ) ;
#8077=EDGE_CURVE ( 'NONE', #31383, #12003, #53392, .T. ) ;
#8163=CARTESIAN_POINT ( 'NONE',  ( -13.25000000000000355, 28.24999999999998934, 4.000000000000000000 ) ) ;
#8177=FACE_OUTER_BOUND ( 'NONE', #10625, .T. ) ;
#8180=ORIENTED_EDGE ( 'NONE', *, *, #50153, .F. ) ;
#8184=CIRCLE ( 'NONE', #65466, 0.2500000000000002220 ) ;
#8193=ORIENTED_EDGE ( 'NONE', *, *, #50823, .T. ) ;
#8204=CARTESIAN_POINT ( 'NONE',  ( -4.500000000000002665, 22.24999999999998579, -3.750000000000000000 ) ) ;
#8213=CARTESIAN_POINT ( 'NONE',  ( -4.500000000000002665, 24.99999999999998579, 4.000000000000000000 ) ) ;
#8243=VECTOR ( 'NONE', #933, 1000.000000000000000 ) ;
#8281=EDGE_LOOP ( 'NONE', ( #2437, #63920, #67103, #56614 ) ) ;
#8289=CARTESIAN_POINT ( 'NONE',  ( 0.000000000000000000, 24.74999999999998579, 4.000000000000000000 ) ) ;
#8297=CIRCLE ( 'NONE', #45386, 0.2500000000000002220 ) ;
#8299=CARTESIAN_POINT ( 'NONE',  ( 0.000000000000000000, 21.74999999999998579, 3.750000000000000000 ) ) ;
#8309=EDGE_LOOP ( 'NONE', ( #9633, #22822, #60974, #46385 ) ) ;
#8321=PLANE ( 'NONE',  #34219 ) ;
#8343=LINE ( 'NONE', #35760, #2200 ) ;
#8358=CIRCLE ( 'NONE', #65634, 0.2500000000000002220 ) ;
#8367=VECTOR ( 'NONE', #45257, 1000.000000000000000 ) ;
#8370=CARTESIAN_POINT ( 'NONE',  ( 4.750000000000002665, 24.99999999999998579, -3.750000000000000000 ) ) ;
#8380=VERTEX_POINT ( 'NONE', #37609 ) ;
#8401=DIRECTION ( 'NONE',  ( 0.000000000000000000, 0.000000000000000000, 1.000000000000000000 ) ) ;
#8409=ORIENTED_EDGE ( 'NONE', *, *, #60364, .F. ) ;
#8411=CYLINDRICAL_SURFACE ( 'NONE', #35672, 0.2500000000000002220 ) ;
#8426=CARTESIAN_POINT ( 'NONE',  ( -22.25000000000000711, 33.74999999999999289, 4.000000000000000000 ) ) ;
#8460=LINE ( 'NONE', #45083, #1435 ) ;
#8467=ORIENTED_EDGE ( 'NONE', *, *, #32025, .F. ) ;
#8473=DIRECTION ( 'NONE',  ( -0.000000000000000000, -0.000000000000000000, 1.000000000000000000 ) ) ;
#8491=DIRECTION ( 'NONE',  ( -1.000000000000000000, 0.000000000000000000, 0.000000000000000000 ) ) ;
#8507=ORIENTED_EDGE ( 'NONE', *, *, #53483, .F. ) ;
#8516=ADVANCED_FACE ( 'NONE', ( #17837 ), #12893, .T. ) ;
#8538=CIRCLE ( 'NONE', #47911, 0.2500000000000002220 ) ;
#8540=CARTESIAN_POINT ( 'NONE',  ( -18.00000000000000711, 33.74999999999999289, 4.000000000000000000 ) ) ;
#8554=FACE_OUTER_BOUND ( 'NONE', #50185, .T. ) ;
#8573=DIRECTION ( 'NONE',  ( 0.000000000000000000, 0.000000000000000000, 1.000000000000000000 ) ) ;
#8575=FACE_OUTER_BOUND ( 'NONE', #31739, .T. ) ;
#8587=EDGE_CURVE ( 'NONE', #50288, #37037, #7394, .T. ) ;
#8591=DIRECTION ( 'NONE',  ( -0.000000000000000000, 1.000000000000000000, -0.000000000000000000 ) ) ;
#8630=EDGE_LOOP ( 'NONE', ( #41716, #67374, #51357, #51942 ) ) ;
#8644=DIRECTION ( 'NONE',  ( 0.000000000000000000, 0.000000000000000000, -1.000000000000000000 ) ) ;
#8647=ORIENTED_EDGE ( 'NONE', *, *, #7661, .F. ) ;
#8648=CARTESIAN_POINT ( 'NONE',  ( -24.00000000000000355, 36.75000000000000000, 3.750000000000000000 ) ) ;
#8659=FACE_OUTER_BOUND ( 'NONE', #43764, .T. ) ;
#8679=VERTEX_POINT ( 'NONE', #43153 ) ;
#8765=CIRCLE ( 'NONE', #14373, 4.000000000000000000 ) ;
#8789=CARTESIAN_POINT ( 'NONE',  ( 4.750000000000002665, 24.99999999999998579, -3.750000000000000000 ) ) ;
#8815=ORIENTED_EDGE ( 'NONE', *, *, #8007, .F. ) ;
#8820=ORIENTED_EDGE ( 'NONE', *, *, #28203, .T. ) ;
#8831=EDGE_CURVE ( 'NONE', #33741, #23152, #62831, .T. ) ;
#8857=ORIENTED_EDGE ( 'NONE', *, *, #53226, .T. ) ;
#8911=CARTESIAN_POINT ( 'NONE',  ( 8.750000000000001776, 24.99999999999998579, -4.000000000000000000 ) ) ;
#8915=EDGE_LOOP ( 'NONE', ( #67991, #22548, #48808, #21997 ) ) ;
#8925=ORIENTED_EDGE ( 'NONE', *, *, #18364, .T. ) ;
#8936=VECTOR ( 'NONE', #69131, 1000.000000000000000 ) ;
#8948=AXIS2_PLACEMENT_3D ( 'NONE', #43265, #10167, #31603 ) ;
#8958=EDGE_CURVE ( 'NONE', #9871, #69641, #43147, .T. ) ;
#8963=LINE ( 'NONE', #40647, #35038 ) ;
#8967=ORIENTED_EDGE ( 'NONE', *, *, #15768, .T. ) ;
#8986=DIRECTION ( 'NONE',  ( 0.000000000000000000, 0.000000000000000000, 1.000000000000000000 ) ) ;
#8989=ORIENTED_EDGE ( 'NONE', *, *, #34142, .F. ) ;
#9014=DIRECTION ( 'NONE',  ( 0.000000000000000000, 0.000000000000000000, -1.000000000000000000 ) ) ;
#9022=AXIS2_PLACEMENT_3D ( 'NONE', #46414, #56576, #35124 ) ;
#9047=DIRECTION ( 'NONE',  ( -1.000000000000000000, 0.000000000000000000, 0.000000000000000000 ) ) ;
#9067=ORIENTED_EDGE ( 'NONE', *, *, #12306, .T. ) ;
#9073=DIRECTION ( 'NONE',  ( -0.000000000000000000, -0.000000000000000000, -1.000000000000000000 ) ) ;
#9080=DIRECTION ( 'NONE',  ( 1.000000000000000000, 0.000000000000000000, 0.000000000000000000 ) ) ;
#9113=CARTESIAN_POINT ( 'NONE',  ( -18.25000000000000711, 31.24999999999999289, 3.750000000000000000 ) ) ;
#9125=LINE ( 'NONE', #41491, #7278 ) ;
#9137=DIRECTION ( 'NONE',  ( 0.000000000000000000, -1.000000000000000000, 0.000000000000000000 ) ) ;
#9142=ORIENTED_EDGE ( 'NONE', *, *, #10702, .T. ) ;
#9166=VERTEX_POINT ( 'NONE', #24424 ) ;
#9192=ORIENTED_EDGE ( 'NONE', *, *, #34306, .T. ) ;
#9221=AXIS2_PLACEMENT_3D ( 'NONE', #10718, #37505, #44164 ) ;
#9232=CARTESIAN_POINT ( 'NONE',  ( -9.250000000000003553, 27.74999999999998934, 3.750000000000000000 ) ) ;
#9249=AXIS2_PLACEMENT_3D ( 'NONE', #3571, #68009, #19796 ) ;
#9250=VERTEX_POINT ( 'NONE', #41695 ) ;
#9266=CARTESIAN_POINT ( 'NONE',  ( -13.75000000000000355, 28.24999999999998934, 4.000000000000000000 ) ) ;
#9277=DIRECTION ( 'NONE',  ( -1.000000000000000000, 0.000000000000000000, 0.000000000000000000 ) ) ;
#9286=AXIS2_PLACEMENT_3D ( 'NONE', #25840, #9342, #20574 ) ;
#9342=DIRECTION ( 'NONE',  ( 0.000000000000000000, 0.000000000000000000, 1.000000000000000000 ) ) ;
#9349=CARTESIAN_POINT ( 'NONE',  ( -22.75000000000000711, 36.75000000000000000, -4.000000000000000000 ) ) ;
#9354=EDGE_LOOP ( 'NONE', ( #69301, #33099, #48990, #68768 ) ) ;
#9357=EDGE_LOOP ( 'NONE', ( #3466, #14358, #9142, #33731, #59320, #166 ) ) ;
#9360=CARTESIAN_POINT ( 'NONE',  ( 18.00000000000000711, 33.74999999999999289, 3.750000000000000000 ) ) ;
#9369=DIRECTION ( 'NONE',  ( 1.000000000000000000, 0.000000000000000000, 0.000000000000000000 ) ) ;
#9405=AXIS2_PLACEMENT_3D ( 'NONE', #54888, #6715, #13376 ) ;
#9414=EDGE_CURVE ( 'NONE', #64993, #10966, #10056, .T. ) ;
#9416=EDGE_LOOP ( 'NONE', ( #63013, #21097, #69019 ) ) ;
#9418=DIRECTION ( 'NONE',  ( 0.000000000000000000, 0.000000000000000000, 1.000000000000000000 ) ) ;
#9464=VECTOR ( 'NONE', #34003, 1000.000000000000000 ) ;
#9476=EDGE_CURVE ( 'NONE', #23152, #61204, #68490, .T. ) ;
#9482=CARTESIAN_POINT ( 'NONE',  ( 24.00000000000000355, 37.00000000000000000, -3.750000000000000000 ) ) ;
#9494=LINE ( 'NONE', #57664, #35200 ) ;
#9495=CARTESIAN_POINT ( 'NONE',  ( -4.250000000000001776, 22.24999999999998579, -4.000000000000000000 ) ) ;
#9497=ORIENTED_EDGE ( 'NONE', *, *, #50438, .T. ) ;
#9509=VERTEX_POINT ( 'NONE', #44140 ) ;
#9517=EDGE_CURVE ( 'NONE', #56729, #61204, #39189, .T. ) ;
#9521=TOROIDAL_SURFACE ( 'NONE', #66797, 0.5000000000000000000, 0.2500000000000000000 ) ;
#9532=CARTESIAN_POINT ( 'NONE',  ( 22.75000000000000711, 36.75000000000000000, 4.000000000000000000 ) ) ;
#9541=CARTESIAN_POINT ( 'NONE',  ( -15.00000000000000000, 8.000000000000000000, -4.000000000000000000 ) ) ;
#9553=FACE_OUTER_BOUND ( 'NONE', #43614, .T. ) ;
#9556=DIRECTION ( 'NONE',  ( 0.000000000000000000, -1.000000000000000000, 0.000000000000000000 ) ) ;
#9557=DIRECTION ( 'NONE',  ( 0.000000000000000000, 0.000000000000000000, -1.000000000000000000 ) ) ;
#9587=ORIENTED_EDGE ( 'NONE', *, *, #5459, .F. ) ;
#9598=VECTOR ( 'NONE', #68325, 1000.000000000000000 ) ;
#9619=CARTESIAN_POINT ( 'NONE',  ( -9.250000000000003553, 25.24999999999998934, 3.750000000000000000 ) ) ;
#9621=CARTESIAN_POINT ( 'NONE',  ( -22.50000000000000711, 36.75000000000000000, 3.750000000000000000 ) ) ;
#9628=LINE ( 'NONE', #8911, #13032 ) ;
#9633=ORIENTED_EDGE ( 'NONE', *, *, #18741, .F. ) ;
#9644=DIRECTION ( 'NONE',  ( 0.000000000000000000, -1.000000000000000000, 0.000000000000000000 ) ) ;
#9655=EDGE_CURVE ( 'NONE', #46540, #40174, #52167, .T. ) ;
#9656=FACE_OUTER_BOUND ( 'NONE', #30338, .T. ) ;
#9664=VECTOR ( 'NONE', #28903, 1000.000000000000000 ) ;
#9706=CARTESIAN_POINT ( 'NONE',  ( -4.250000000000001776, 21.99999999999998579, -3.750000000000000000 ) ) ;
#9711=DIRECTION ( 'NONE',  ( -1.000000000000000000, 0.000000000000000000, 0.000000000000000000 ) ) ;
#9722=EDGE_CURVE ( 'NONE', #51168, #5413, #31351, .T. ) ;
#9783=AXIS2_PLACEMENT_3D ( 'NONE', #45455, #65827, #23594 ) ;
#9785=EDGE_CURVE ( 'NONE', #58314, #11393, #5652, .T. ) ;
#9790=DIRECTION ( 'NONE',  ( -1.000000000000000000, 0.000000000000000000, 0.000000000000000000 ) ) ;
#9799=LINE ( 'NONE', #69226, #59353 ) ;
#9817=DIRECTION ( 'NONE',  ( 0.000000000000000000, 0.000000000000000000, -1.000000000000000000 ) ) ;
#9871=VERTEX_POINT ( 'NONE', #39455 ) ;
#9900=ORIENTED_EDGE ( 'NONE', *, *, #1556, .T. ) ;
#9911=EDGE_LOOP ( 'NONE', ( #26834, #53017, #28155, #10091 ) ) ;
#9924=DIRECTION ( 'NONE',  ( -1.000000000000000000, 0.000000000000000000, 0.000000000000000000 ) ) ;
#9938=EDGE_CURVE ( 'NONE', #60418, #36018, #61577, .T. ) ;
#9955=ORIENTED_EDGE ( 'NONE', *, *, #24307, .F. ) ;
#9962=DIRECTION ( 'NONE',  ( -1.000000000000000000, 0.000000000000000000, 0.000000000000000000 ) ) ;
#10013=CARTESIAN_POINT ( 'NONE',  ( 24.00000000000000000, 1.000000000000000888, 3.000000000000000000 ) ) ;
#10022=DIRECTION ( 'NONE',  ( 0.000000000000000000, 0.000000000000000000, -1.000000000000000000 ) ) ;
#10056=CIRCLE ( 'NONE', #63955, 0.2500000000000002220 ) ;
#10091=ORIENTED_EDGE ( 'NONE', *, *, #39186, .F. ) ;
#10093=CIRCLE ( 'NONE', #25843, 0.2500000000000002220 ) ;
#10096=EDGE_CURVE ( 'NONE', #41120, #56763, #22341, .T. ) ;
#10150=LINE ( 'NONE', #68545, #23463 ) ;
#10167=DIRECTION ( 'NONE',  ( 0.000000000000000000, 0.000000000000000000, -1.000000000000000000 ) ) ;
#10186=EDGE_LOOP ( 'NONE', ( #69136, #53449, #46753, #58357 ) ) ;
#10209=ORIENTED_EDGE ( 'NONE', *, *, #1038, .F. ) ;
#10234=AXIS2_PLACEMENT_3D ( 'NONE', #64135, #69426, #42738 ) ;
#10245=AXIS2_PLACEMENT_3D ( 'NONE', #2756, #18640, #19307 ) ;
#10256=ORIENTED_EDGE ( 'NONE', *, *, #19415, .F. ) ;
#10295=TOROIDAL_SURFACE ( 'NONE', #49608, 0.5000000000000000000, 0.2500000000000000000 ) ;
#10299=DIRECTION ( 'NONE',  ( 1.000000000000000000, 0.000000000000000000, 0.000000000000000000 ) ) ;
#10311=CIRCLE ( 'NONE', #37299, 4.499999999999976019 ) ;
#10324=VECTOR ( 'NONE', #27215, 1000.000000000000000 ) ;
#10335=AXIS2_PLACEMENT_3D ( 'NONE', #58902, #64525, #5074 ) ;
#10364=VECTOR ( 'NONE', #6638, 1000.000000000000000 ) ;
#10374=CARTESIAN_POINT ( 'NONE',  ( 11.00000000000000000, 8.000000000000000000, -3.500000000000017764 ) ) ;
#10393=DIRECTION ( 'NONE',  ( -0.000000000000000000, -0.000000000000000000, 1.000000000000000000 ) ) ;
#10395=DIRECTION ( 'NONE',  ( -9.376883653928687363E-17, 1.000000000000000000, 0.000000000000000000 ) ) ;
#10413=CARTESIAN_POINT ( 'NONE',  ( 0.000000000000000000, 24.74999999999998579, 3.750000000000000000 ) ) ;
#10502=CARTESIAN_POINT ( 'NONE',  ( -15.00000000000000000, 8.000000000000000000, -4.000000000000000000 ) ) ;
#10522=DIRECTION ( 'NONE',  ( -1.000000000000000000, 0.000000000000000000, 0.000000000000000000 ) ) ;
#10527=AXIS2_PLACEMENT_3D ( 'NONE', #7645, #6966, #2306 ) ;
#10530=DIRECTION ( 'NONE',  ( 0.000000000000000000, 0.000000000000000000, -1.000000000000000000 ) ) ;
#10557=ORIENTED_EDGE ( 'NONE', *, *, #31768, .F. ) ;
#10564=CIRCLE ( 'NONE', #49878, 0.2500000000000002220 ) ;
#10585=EDGE_CURVE ( 'NONE', #64274, #46287, #33623, .T. ) ;
#10586=VECTOR ( 'NONE', #66127, 1000.000000000000000 ) ;
#10618=LINE ( 'NONE', #41977, #51202 ) ;
#10619=EDGE_LOOP ( 'NONE', ( #26445, #7362, #50589, #66174 ) ) ;
#10625=EDGE_LOOP ( 'NONE', ( #51374, #60549, #30181, #14162 ) ) ;
#10650=EDGE_CURVE ( 'NONE', #19696, #35085, #32507, .T. ) ;
#10672=CARTESIAN_POINT ( 'NONE',  ( 24.00000000000000355, 37.00000000000000000, -3.000000000000000000 ) ) ;
#10693=DIRECTION ( 'NONE',  ( 0.000000000000000000, 0.000000000000000000, -1.000000000000000000 ) ) ;
#10702=EDGE_CURVE ( 'NONE', #51757, #47479, #16033, .T. ) ;
#10708=CIRCLE ( 'NONE', #2779, 1.000000000000000888 ) ;
#10710=LINE ( 'NONE', #32164, #6304 ) ;
#10718=CARTESIAN_POINT ( 'NONE',  ( 4.750000000000002665, 24.74999999999998579, -3.750000000000000000 ) ) ;
#10748=CARTESIAN_POINT ( 'NONE',  ( -18.25000000000000711, 31.24999999999999289, -4.000000000000000000 ) ) ;
#10768=EDGE_CURVE ( 'NONE', #51977, #19151, #20223, .T. ) ;
#10781=CARTESIAN_POINT ( 'NONE',  ( -24.00000000000000000, 1.000000000000000000, 3.000000000000000000 ) ) ;
#10785=DIRECTION ( 'NONE',  ( 0.000000000000000000, -1.000000000000000000, 0.000000000000000000 ) ) ;
#10789=LINE ( 'NONE', #20994, #12959 ) ;
#10800=ADVANCED_FACE ( 'NONE', ( #69463 ), #11178, .T. ) ;
#10822=DIRECTION ( 'NONE',  ( -1.000000000000000000, 0.000000000000000000, 0.000000000000000000 ) ) ;
#10855=CARTESIAN_POINT ( 'NONE',  ( 18.25000000000000711, 33.74999999999999289, 4.000000000000000000 ) ) ;
#10861=ORIENTED_EDGE ( 'NONE', *, *, #4694, .T. ) ;
#10869=EDGE_LOOP ( 'NONE', ( #60774, #46709, #57154, #29097 ) ) ;
#10908=LINE ( 'NONE', #33729, #10364 ) ;
#10920=ORIENTED_EDGE ( 'NONE', *, *, #9785, .T. ) ;
#10960=ADVANCED_FACE ( 'NONE', ( #27441 ), #21855, .T. ) ;
#10966=VERTEX_POINT ( 'NONE', #16936 ) ;
#10971=DIRECTION ( 'NONE',  ( 5.782411586589351722E-16, -1.000000000000000000, 0.000000000000000000 ) ) ;
#11005=CARTESIAN_POINT ( 'NONE',  ( -25.00000000000000000, 1.000000000000000888, 4.000000000000000000 ) ) ;
#11043=ORIENTED_EDGE ( 'NONE', *, *, #59959, .T. ) ;
#11046=ORIENTED_EDGE ( 'NONE', *, *, #18068, .F. ) ;
#11079=ORIENTED_EDGE ( 'NONE', *, *, #5978, .F. ) ;
#11081=EDGE_CURVE ( 'NONE', #23924, #58314, #65800, .T. ) ;
#11083=DIRECTION ( 'NONE',  ( -1.000000000000000000, 0.000000000000000000, 0.000000000000000000 ) ) ;
#11107=ADVANCED_FACE ( 'NONE', ( #36660 ), #26716, .T. ) ;
#11114=AXIS2_PLACEMENT_3D ( 'NONE', #66711, #18527, #13572 ) ;
#11124=DIRECTION ( 'NONE',  ( 0.000000000000000000, 0.000000000000000000, -1.000000000000000000 ) ) ;
#11130=EDGE_LOOP ( 'NONE', ( #63148, #40572, #44306, #21979 ) ) ;
#11178=TOROIDAL_SURFACE ( 'NONE', #16839, 0.5000000000000000000, 0.2500000000000000000 ) ;
#11179=FACE_OUTER_BOUND ( 'NONE', #10619, .T. ) ;
#11190=ADVANCED_FACE ( 'NONE', ( #62982 ), #67417, .T. ) ;
#11239=AXIS2_PLACEMENT_3D ( 'NONE', #38762, #2405, #28837 ) ;
#11253=DIRECTION ( 'NONE',  ( 1.000000000000000000, 0.000000000000000000, -0.000000000000000000 ) ) ;
#11279=DIRECTION ( 'NONE',  ( -1.000000000000000000, 0.000000000000000000, 0.000000000000000000 ) ) ;
#11336=LINE ( 'NONE', #50039, #18497 ) ;
#11359=DIRECTION ( 'NONE',  ( 0.000000000000000000, -1.000000000000000000, 0.000000000000000000 ) ) ;
#11393=VERTEX_POINT ( 'NONE', #52711 ) ;
#11412=CARTESIAN_POINT ( 'NONE',  ( 13.50000000000000533, 30.99999999999999289, 4.000000000000000000 ) ) ;
#11429=AXIS2_PLACEMENT_3D ( 'NONE', #63635, #53096, #25987 ) ;
#11451=CARTESIAN_POINT ( 'NONE',  ( 24.00000000000000000, 1.000000000000000000, -3.000000000000000000 ) ) ;
#11496=LINE ( 'NONE', #11841, #6544 ) ;
#11525=AXIS2_PLACEMENT_3D ( 'NONE', #18672, #40842, #25321 ) ;
#11538=DIRECTION ( 'NONE',  ( -0.000000000000000000, -0.000000000000000000, 1.000000000000000000 ) ) ;
#11561=ADVANCED_FACE ( 'NONE', ( #20154 ), #8003, .T. ) ;
#11569=DIRECTION ( 'NONE',  ( 0.000000000000000000, 1.000000000000000000, 0.000000000000000000 ) ) ;
#11573=CIRCLE ( 'NONE', #22788, 0.2500000000000002220 ) ;
#11585=EDGE_CURVE ( 'NONE', #2325, #53882, #63080, .T. ) ;
#11586=DIRECTION ( 'NONE',  ( 0.000000000000000000, 1.000000000000000000, 0.000000000000000000 ) ) ;
#11592=SPHERICAL_SURFACE ( 'NONE', #64259, 0.2500000000000000000 ) ;
#11612=EDGE_CURVE ( 'NONE', #31530, #11393, #58580, .T. ) ;
#11628=LINE ( 'NONE', #64048, #41505 ) ;
#11631=ORIENTED_EDGE ( 'NONE', *, *, #59095, .T. ) ;
#11668=VECTOR ( 'NONE', #34478, 1000.000000000000000 ) ;
#11694=CARTESIAN_POINT ( 'NONE',  ( -18.00000000000000711, 30.74999999999999289, -3.750000000000000000 ) ) ;
#11696=EDGE_CURVE ( 'NONE', #65002, #66039, #41310, .T. ) ;
#11740=CARTESIAN_POINT ( 'NONE',  ( 25.00000000000000000, 1.000000000000000888, -3.000000000000000000 ) ) ;
#11754=CIRCLE ( 'NONE', #23019, 0.2500000000000002220 ) ;
#11765=VECTOR ( 'NONE', #28672, 1000.000000000000000 ) ;
#11767=CIRCLE ( 'NONE', #51099, 0.2500000000000002220 ) ;
#11773=ORIENTED_EDGE ( 'NONE', *, *, #40286, .T. ) ;
#11785=ORIENTED_EDGE ( 'NONE', *, *, #17518, .T. ) ;
#11797=DIRECTION ( 'NONE',  ( -1.000000000000000000, 0.000000000000000000, 0.000000000000000000 ) ) ;
#11807=DIRECTION ( 'NONE',  ( 1.000000000000000000, 0.000000000000000000, 0.000000000000000000 ) ) ;
#11820=ADVANCED_FACE ( 'NONE', ( #68726 ), #10295, .T. ) ;
#11838=ADVANCED_FACE ( 'NONE', ( #43425 ), #13524, .T. ) ;
#11840=DIRECTION ( 'NONE',  ( 1.000000000000000000, -0.000000000000000000, -0.000000000000000000 ) ) ;
#11841=CARTESIAN_POINT ( 'NONE',  ( -18.00000000000000711, 33.74999999999999289, -3.750000000000000000 ) ) ;
#11853=LINE ( 'NONE', #38984, #48970 ) ;
#11860=CARTESIAN_POINT ( 'NONE',  ( -24.00000000000000355, 36.75000000000000000, -3.000000000000000000 ) ) ;
#11888=DIRECTION ( 'NONE',  ( -1.000000000000000000, 0.000000000000000000, 0.000000000000000000 ) ) ;
#11910=DIRECTION ( 'NONE',  ( 9.376883653928687363E-17, 1.000000000000000000, 0.000000000000000000 ) ) ;
#11913=ADVANCED_FACE ( 'NONE', ( #59876 ), #44454, .T. ) ;
#11915=FACE_OUTER_BOUND ( 'NONE', #47265, .T. ) ;
#11934=LINE ( 'NONE', #60446, #35467 ) ;
#11939=FACE_OUTER_BOUND ( 'NONE', #36065, .T. ) ;
#11954=CARTESIAN_POINT ( 'NONE',  ( 22.75000000000000711, 34.24999999999999289, 4.000000000000000000 ) ) ;
#11989=EDGE_LOOP ( 'NONE', ( #52499, #5215, #59498, #34876 ) ) ;
#12003=VERTEX_POINT ( 'NONE', #24649 ) ;
#12006=DIRECTION ( 'NONE',  ( 1.000000000000000000, 0.000000000000000000, 0.000000000000000000 ) ) ;
#12008=VECTOR ( 'NONE', #50187, 1000.000000000000000 ) ;
#12029=ORIENTED_EDGE ( 'NONE', *, *, #6056, .F. ) ;
#12047=CYLINDRICAL_SURFACE ( 'NONE', #2037, 0.2500000000000002220 ) ;
#12054=FACE_OUTER_BOUND ( 'NONE', #18906, .T. ) ;
#12098=DIRECTION ( 'NONE',  ( 1.000000000000000000, 0.000000000000000000, 0.000000000000000000 ) ) ;
#12113=AXIS2_PLACEMENT_3D ( 'NONE', #18477, #65615, #11797 ) ;
#12148=CARTESIAN_POINT ( 'NONE',  ( -13.75000000000000355, 28.24999999999998934, -4.000000000000000000 ) ) ;
#12149=ORIENTED_EDGE ( 'NONE', *, *, #33765, .F. ) ;
#12151=EDGE_CURVE ( 'NONE', #6652, #30380, #4221, .T. ) ;
#12155=DIRECTION ( 'NONE',  ( 0.000000000000000000, 0.000000000000000000, 1.000000000000000000 ) ) ;
#12180=VECTOR ( 'NONE', #32518, 1000.000000000000000 ) ;
#12191=DIRECTION ( 'NONE',  ( -0.000000000000000000, -0.000000000000000000, -1.000000000000000000 ) ) ;
#12193=CARTESIAN_POINT ( 'NONE',  ( -24.00000000000000355, 36.75000000000000000, 3.000000000000000000 ) ) ;
#12223=AXIS2_PLACEMENT_3D ( 'NONE', #8163, #56326, #40536 ) ;
#12228=CARTESIAN_POINT ( 'NONE',  ( 25.00000000000000355, 36.75000000000000000, 3.000000000000000000 ) ) ;
#12238=ORIENTED_EDGE ( 'NONE', *, *, #61518, .T. ) ;
#12248=DIRECTION ( 'NONE',  ( -0.000000000000000000, -0.000000000000000000, 1.000000000000000000 ) ) ;
#12252=DIRECTION ( 'NONE',  ( 0.000000000000000000, 1.000000000000000000, 0.000000000000000000 ) ) ;
#12256=VECTOR ( 'NONE', #64820, 1000.000000000000000 ) ;
#12259=CYLINDRICAL_SURFACE ( 'NONE', #50551, 0.2500000000000002220 ) ;
#12272=AXIS2_PLACEMENT_3D ( 'NONE', #28248, #60623, #65573 ) ;
#12281=DIRECTION ( 'NONE',  ( 0.000000000000000000, 1.000000000000000000, 0.000000000000000000 ) ) ;
#12301=VERTEX_POINT ( 'NONE', #11954 ) ;
#12306=EDGE_CURVE ( 'NONE', #66039, #49491, #49959, .T. ) ;
#12312=EDGE_LOOP ( 'NONE', ( #62149, #21004 ) ) ;
#12317=CIRCLE ( 'NONE', #51665, 1.000000000000000000 ) ;
#12341=CARTESIAN_POINT ( 'NONE',  ( -24.00000000000000000, -2.250452076942884869E-15, 3.000000000000000000 ) ) ;
#12360=DIRECTION ( 'NONE',  ( -1.000000000000000000, 0.000000000000000000, 0.000000000000000000 ) ) ;
#12363=DIRECTION ( 'NONE',  ( -1.000000000000000000, 0.000000000000000000, 0.000000000000000000 ) ) ;
#12368=EDGE_CURVE ( 'NONE', #68401, #59464, #56598, .T. ) ;
#12377=EDGE_CURVE ( 'NONE', #10966, #68484, #29146, .T. ) ;
#12479=DIRECTION ( 'NONE',  ( 0.000000000000000000, 1.000000000000000000, 0.000000000000000000 ) ) ;
#12485=EDGE_CURVE ( 'NONE', #35021, #31124, #1163, .T. ) ;
#12486=ORIENTED_EDGE ( 'NONE', *, *, #61868, .F. ) ;
#12496=EDGE_LOOP ( 'NONE', ( #54075, #6447, #62280, #18347 ) ) ;
#12530=AXIS2_PLACEMENT_3D ( 'NONE', #56798, #36040, #24413 ) ;
#12540=CARTESIAN_POINT ( 'NONE',  ( 13.75000000000000355, 28.24999999999998934, 4.000000000000000000 ) ) ;
#12568=EDGE_CURVE ( 'NONE', #35085, #6425, #33853, .T. ) ;
#12570=AXIS2_PLACEMENT_3D ( 'NONE', #17571, #49564, #54802 ) ;
#12591=CYLINDRICAL_SURFACE ( 'NONE', #54159, 0.2500000000000002220 ) ;
#12603=FACE_OUTER_BOUND ( 'NONE', #66335, .T. ) ;
#12608=DIRECTION ( 'NONE',  ( 0.7071067811865425767, 8.659560562354873694E-17, -0.7071067811865525687 ) ) ;
#12615=DIRECTION ( 'NONE',  ( 0.000000000000000000, 0.000000000000000000, -1.000000000000000000 ) ) ;
#12668=EDGE_LOOP ( 'NONE', ( #24640, #43479, #12029, #4093 ) ) ;
#12675=ORIENTED_EDGE ( 'NONE', *, *, #20697, .T. ) ;
#12679=CIRCLE ( 'NONE', #23934, 1.000000000000000000 ) ;
#12691=PLANE ( 'NONE',  #39942 ) ;
#12709=DIRECTION ( 'NONE',  ( 1.000000000000000000, -0.000000000000000000, 0.000000000000000000 ) ) ;
#12712=ORIENTED_EDGE ( 'NONE', *, *, #40214, .F. ) ;
#12723=VERTEX_POINT ( 'NONE', #30810 ) ;
#12743=ORIENTED_EDGE ( 'NONE', *, *, #55426, .T. ) ;
#12763=CARTESIAN_POINT ( 'NONE',  ( -4.750000000000002665, 0.000000000000000000, 3.750000000000000000 ) ) ;
#12768=DIRECTION ( 'NONE',  ( 0.000000000000000000, 0.000000000000000000, -1.000000000000000000 ) ) ;
#12771=TOROIDAL_SURFACE ( 'NONE', #13940, 0.5000000000000000000, 0.2500000000000000000 ) ;
#12786=EDGE_LOOP ( 'NONE', ( #13050, #49358, #4471 ) ) ;
#12798=CARTESIAN_POINT ( 'NONE',  ( 18.00000000000000711, 30.74999999999999289, -3.750000000000000000 ) ) ;
#12826=FACE_OUTER_BOUND ( 'NONE', #29053, .T. ) ;
#12857=EDGE_CURVE ( 'NONE', #37037, #33122, #22679, .T. ) ;
#12867=EDGE_CURVE ( 'NONE', #2945, #23924, #47424, .T. ) ;
#12869=VERTEX_POINT ( 'NONE', #64574 ) ;
#12892=FACE_OUTER_BOUND ( 'NONE', #53778, .T. ) ;
#12893=CYLINDRICAL_SURFACE ( 'NONE', #51181, 0.2500000000000002220 ) ;
#12901=AXIS2_PLACEMENT_3D ( 'NONE', #10502, #31939, #4661 ) ;
#12919=LINE ( 'NONE', #50229, #44285 ) ;
#12939=ORIENTED_EDGE ( 'NONE', *, *, #5972, .F. ) ;
#12950=CARTESIAN_POINT ( 'NONE',  ( -13.75000000000000533, 30.74999999999999289, -4.000000000000000000 ) ) ;
#12951=DIRECTION ( 'NONE',  ( 1.000000000000000000, -0.000000000000000000, 0.000000000000000000 ) ) ;
#12956=ORIENTED_EDGE ( 'NONE', *, *, #43634, .T. ) ;
#12958=ORIENTED_EDGE ( 'NONE', *, *, #22979, .T. ) ;
#12959=VECTOR ( 'NONE', #47430, 1000.000000000000000 ) ;
#12960=PLANE ( 'NONE',  #13197 ) ;
#12987=CARTESIAN_POINT ( 'NONE',  ( 24.00000000000000000, -2.250452076942884869E-15, 3.000000000000000000 ) ) ;
#13017=CARTESIAN_POINT ( 'NONE',  ( -24.00000000000000355, 37.00000000000000000, -4.000000000000000000 ) ) ;
#13025=ORIENTED_EDGE ( 'NONE', *, *, #21926, .T. ) ;
#13031=ORIENTED_EDGE ( 'NONE', *, *, #49556, .T. ) ;
#13032=VECTOR ( 'NONE', #31382, 1000.000000000000000 ) ;
#13050=ORIENTED_EDGE ( 'NONE', *, *, #63509, .T. ) ;
#13065=DIRECTION ( 'NONE',  ( 0.000000000000000000, 0.000000000000000000, 1.000000000000000000 ) ) ;
#13114=EDGE_CURVE ( 'NONE', #67128, #5051, #21839, .T. ) ;
#13122=ORIENTED_EDGE ( 'NONE', *, *, #11585, .T. ) ;
#13155=DIRECTION ( 'NONE',  ( -1.000000000000000000, 0.000000000000000000, 0.000000000000000000 ) ) ;
#13166=CARTESIAN_POINT ( 'NONE',  ( -18.25000000000000711, 33.74999999999999289, -3.750000000000000000 ) ) ;
#13171=PRODUCT_CONTEXT ( 'NONE', #17723, 'mechanical' ) ;
#13197=AXIS2_PLACEMENT_3D ( 'NONE', #60785, #28783, #13651 ) ;
#13257=ADVANCED_FACE ( 'NONE', ( #65783 ), #61192, .T. ) ;
#13263=ADVANCED_FACE ( 'NONE', ( #28461 ), #1706, .T. ) ;
#13268=CARTESIAN_POINT ( 'NONE',  ( 0.000000000000000000, 36.75000000000000000, 4.000000000000000000 ) ) ;
#13283=ORIENTED_EDGE ( 'NONE', *, *, #48807, .F. ) ;
#13292=ORIENTED_EDGE ( 'NONE', *, *, #62077, .F. ) ;
#13296=AXIS2_PLACEMENT_3D ( 'NONE', #19131, #39954, #61359 ) ;
#13303=DIRECTION ( 'NONE',  ( -0.000000000000000000, -0.000000000000000000, 1.000000000000000000 ) ) ;
#13319=ORIENTED_EDGE ( 'NONE', *, *, #19846, .T. ) ;
#13337=AXIS2_PLACEMENT_3D ( 'NONE', #4747, #92, #26202 ) ;
#13358=DIRECTION ( 'NONE',  ( 1.000000000000000000, -0.000000000000000000, 0.000000000000000000 ) ) ;
#13375=AXIS2_PLACEMENT_3D ( 'NONE', #55739, #59702, #13155 ) ;
#13376=DIRECTION ( 'NONE',  ( -1.000000000000000000, 0.000000000000000000, 0.000000000000000000 ) ) ;
#13443=VERTEX_POINT ( 'NONE', #18293 ) ;
#13469=LINE ( 'NONE', #40592, #45240 ) ;
#13479=ORIENTED_EDGE ( 'NONE', *, *, #2130, .F. ) ;
#13481=EDGE_CURVE ( 'NONE', #42335, #44124, #56408, .T. ) ;
#13482=FACE_OUTER_BOUND ( 'NONE', #37576, .T. ) ;
#13500=EDGE_CURVE ( 'NONE', #15255, #14152, #20362, .T. ) ;
#13517=AXIS2_PLACEMENT_3D ( 'NONE', #61833, #18923, #3050 ) ;
#13524=TOROIDAL_SURFACE ( 'NONE', #49657, 0.5000000000000000000, 0.2500000000000000000 ) ;
#13542=ORIENTED_EDGE ( 'NONE', *, *, #33203, .F. ) ;
#13556=COLOUR_RGB ( '', 0.72549020, 0.75294118, 0.79215686) ;
#13571=VECTOR ( 'NONE', #40441, 1000.000000000000000 ) ;
#13572=DIRECTION ( 'NONE',  ( 1.000000000000000000, 0.000000000000000000, 0.000000000000000000 ) ) ;
#13576=DIRECTION ( 'NONE',  ( 0.000000000000000000, 0.000000000000000000, -1.000000000000000000 ) ) ;
#13597=AXIS2_PLACEMENT_3D ( 'NONE', #55873, #45710, #28781 ) ;
#13606=CARTESIAN_POINT ( 'NONE',  ( 24.00000000000000355, 37.00000000000000000, 3.000000000000000000 ) ) ;
#13644=ADVANCED_FACE ( 'NONE', ( #11179 ), #15124, .F. ) ;
#13651=DIRECTION ( 'NONE',  ( 5.782411586589351722E-16, -1.000000000000000000, 0.000000000000000000 ) ) ;
#13664=CIRCLE ( 'NONE', #32808, 0.5000000000000004441 ) ;
#13698=CARTESIAN_POINT ( 'NONE',  ( 0.000000000000000000, 33.74999999999999289, 4.000000000000000000 ) ) ;
#13717=ORIENTED_EDGE ( 'NONE', *, *, #27819, .F. ) ;
#13720=DIRECTION ( 'NONE',  ( 0.000000000000000000, 0.000000000000000000, -1.000000000000000000 ) ) ;
#13739=CIRCLE ( 'NONE', #59782, 0.2500000000000002220 ) ;
#13764=CARTESIAN_POINT ( 'NONE',  ( 8.750000000000001776, 24.99999999999998579, -3.750000000000000000 ) ) ;
#13770=CARTESIAN_POINT ( 'NONE',  ( 17.75000000000000711, 31.24999999999999289, -3.750000000000000000 ) ) ;
#13811=DIRECTION ( 'NONE',  ( 0.000000000000000000, 0.000000000000000000, 1.000000000000000000 ) ) ;
#13840=CARTESIAN_POINT ( 'NONE',  ( -22.50000000000000711, 36.75000000000000000, -3.750000000000000000 ) ) ;
#13855=CARTESIAN_POINT ( 'NONE',  ( -4.500000000000002665, 24.74999999999998579, -3.750000000000000000 ) ) ;
#13904=ORIENTED_EDGE ( 'NONE', *, *, #16397, .T. ) ;
#13908=FACE_OUTER_BOUND ( 'NONE', #65563, .T. ) ;
#13921=CARTESIAN_POINT ( 'NONE',  ( -4.750000000000002665, 22.24999999999998579, 4.000000000000000000 ) ) ;
#13940=AXIS2_PLACEMENT_3D ( 'NONE', #5641, #15903, #9924 ) ;
#13983=DIRECTION ( 'NONE',  ( 0.000000000000000000, 0.000000000000000000, -1.000000000000000000 ) ) ;
#13991=AXIS2_PLACEMENT_3D ( 'NONE', #11412, #27217, #16041 ) ;
#14007=ORIENTED_EDGE ( 'NONE', *, *, #37400, .T. ) ;
#14034=VECTOR ( 'NONE', #13983, 1000.000000000000000 ) ;
#14069=VECTOR ( 'NONE', #27822, 1000.000000000000000 ) ;
#14090=ORIENTED_EDGE ( 'NONE', *, *, #67171, .F. ) ;
#14094=EDGE_CURVE ( 'NONE', #53491, #33122, #7223, .T. ) ;
#14103=CARTESIAN_POINT ( 'NONE',  ( -19.49999999999997513, 8.000000000000000000, -4.000000000000000000 ) ) ;
#14127=ORIENTED_EDGE ( 'NONE', *, *, #61868, .T. ) ;
#14140=CARTESIAN_POINT ( 'NONE',  ( 22.75000000000000711, 36.75000000000000000, -4.000000000000000000 ) ) ;
#14152=VERTEX_POINT ( 'NONE', #59265 ) ;
#14162=ORIENTED_EDGE ( 'NONE', *, *, #26056, .T. ) ;
#14205=EDGE_CURVE ( 'NONE', #16875, #9166, #36955, .T. ) ;
#14206=CARTESIAN_POINT ( 'NONE',  ( -4.750000000000002665, 24.74999999999998579, -3.750000000000000000 ) ) ;
#14230=CARTESIAN_POINT ( 'NONE',  ( 0.000000000000000000, 30.74999999999999289, 4.000000000000000000 ) ) ;
#14239=ADVANCED_FACE ( 'NONE', ( #67339 ), #28987, .F. ) ;
#14246=DIRECTION ( 'NONE',  ( 1.000000000000000000, 0.000000000000000000, 0.000000000000000000 ) ) ;
#14257=ADVANCED_FACE ( 'NONE', ( #30044 ), #51504, .F. ) ;
#14282=SPHERICAL_SURFACE ( 'NONE', #66024, 0.2500000000000000000 ) ;
#14310=CIRCLE ( 'NONE', #64868, 0.5000000000000004441 ) ;
#14311=EDGE_CURVE ( 'NONE', #34405, #54990, #44793, .T. ) ;
#14321=ORIENTED_EDGE ( 'NONE', *, *, #53226, .F. ) ;
#14322=ORIENTED_EDGE ( 'NONE', *, *, #37380, .T. ) ;
#14353=VECTOR ( 'NONE', #16378, 1000.000000000000000 ) ;
#14357=DIRECTION ( 'NONE',  ( -1.000000000000000000, 0.000000000000000000, 0.000000000000000000 ) ) ;
#14358=ORIENTED_EDGE ( 'NONE', *, *, #21882, .T. ) ;
#14369=PLANE ( 'NONE',  #65036 ) ;
#14373=AXIS2_PLACEMENT_3D ( 'NONE', #7562, #28992, #61018 ) ;
#14374=EDGE_CURVE ( 'NONE', #65002, #61213, #31266, .T. ) ;
#14399=AXIS2_PLACEMENT_3D ( 'NONE', #42117, #16050, #48416 ) ;
#14405=ORIENTED_EDGE ( 'NONE', *, *, #12377, .F. ) ;
#14409=DIRECTION ( 'NONE',  ( 0.000000000000000000, 1.000000000000000000, -0.000000000000000000 ) ) ;
#14411=CARTESIAN_POINT ( 'NONE',  ( -22.75000000000000711, 0.000000000000000000, 4.000000000000000000 ) ) ;
#14416=CARTESIAN_POINT ( 'NONE',  ( -22.25000000000000711, 34.24999999999999289, -3.750000000000000000 ) ) ;
#14439=ORIENTED_EDGE ( 'NONE', *, *, #21126, .F. ) ;
#14443=CIRCLE ( 'NONE', #42556, 0.2500000000000002220 ) ;
#14479=DIRECTION ( 'NONE',  ( -9.376883653928687363E-17, -1.000000000000000000, -0.000000000000000000 ) ) ;
#14481=DIRECTION ( 'NONE',  ( 0.000000000000000000, 0.000000000000000000, -1.000000000000000000 ) ) ;
#14482=CIRCLE ( 'NONE', #53796, 0.2500000000000002220 ) ;
#14492=CARTESIAN_POINT ( 'NONE',  ( -22.25000000000000711, 33.99999999999999289, -3.750000000000000000 ) ) ;
#14506=EDGE_LOOP ( 'NONE', ( #7431, #49272, #55222, #18216 ) ) ;
#14529=ORIENTED_EDGE ( 'NONE', *, *, #27893, .F. ) ;
#14547=CIRCLE ( 'NONE', #23521, 0.2500000000000002220 ) ;
#14552=AXIS2_PLACEMENT_3D ( 'NONE', #46711, #4063, #62809 ) ;
#14565=SURFACE_STYLE_USAGE ( .BOTH. , #14937 ) ;
#14567=AXIS2_PLACEMENT_3D ( 'NONE', #58342, #48525, #42912 ) ;
#14588=EDGE_LOOP ( 'NONE', ( #9900, #31925, #55629, #13319 ) ) ;
#14602=CARTESIAN_POINT ( 'NONE',  ( 4.750000000000002665, 24.74999999999998579, -3.750000000000000000 ) ) ;
#14612=ADVANCED_FACE ( 'NONE', ( #49359 ), #33513, .T. ) ;
#14618=LINE ( 'NONE', #64176, #42710 ) ;
#14619=VECTOR ( 'NONE', #37562, 1000.000000000000000 ) ;
#14620=ADVANCED_FACE ( 'NONE', ( #38838 ), #12047, .T. ) ;
#14642=EDGE_CURVE ( 'NONE', #35085, #68501, #57186, .T. ) ;
#14679=FACE_OUTER_BOUND ( 'NONE', #37291, .T. ) ;
#14693=VECTOR ( 'NONE', #69090, 1000.000000000000000 ) ;
#14694=CARTESIAN_POINT ( 'NONE',  ( -13.50000000000000533, 30.99999999999999289, 3.750000000000000000 ) ) ;
#14699=AXIS2_PLACEMENT_3D ( 'NONE', #15061, #7426, #23930 ) ;
#14778=CARTESIAN_POINT ( 'NONE',  ( 22.50000000000000711, 36.75000000000000000, 4.000000000000000000 ) ) ;
#14783=EDGE_LOOP ( 'NONE', ( #18496, #33715, #53768, #19478 ) ) ;
#14813=AXIS2_PLACEMENT_3D ( 'NONE', #26891, #53998, #54346 ) ;
#14814=DIRECTION ( 'NONE',  ( 0.000000000000000000, 0.000000000000000000, -1.000000000000000000 ) ) ;
#14825=DIRECTION ( 'NONE',  ( 0.000000000000000000, 0.000000000000000000, -1.000000000000000000 ) ) ;
#14844=DIRECTION ( 'NONE',  ( 0.000000000000000000, 1.000000000000000000, -0.000000000000000000 ) ) ;
#14853=EDGE_LOOP ( 'NONE', ( #65654, #19010, #50249, #20122 ) ) ;
#14887=LINE ( 'NONE', #36370, #30531 ) ;
#14904=ORIENTED_EDGE ( 'NONE', *, *, #43370, .F. ) ;
#14908=SPHERICAL_SURFACE ( 'NONE', #48293, 0.2500000000000000000 ) ;
#14937=SURFACE_SIDE_STYLE ('',( #68380 ) ) ;
#14940=AXIS2_PLACEMENT_3D ( 'NONE', #13770, #44447, #12360 ) ;
#14953=EDGE_CURVE ( 'NONE', #37155, #19696, #66180, .T. ) ;
#14959=VECTOR ( 'NONE', #67838, 1000.000000000000000 ) ;
#14966=ORIENTED_EDGE ( 'NONE', *, *, #69037, .T. ) ;
#15001=SHAPE_REPRESENTATION ( '7. Upper Jaw', ( #42840 ), #18040 ) ;
#15061=CARTESIAN_POINT ( 'NONE',  ( 17.75000000000000711, 31.24999999999999289, 3.750000000000000000 ) ) ;
#15077=LINE ( 'NONE', #4821, #879 ) ;
#15082=ORIENTED_EDGE ( 'NONE', *, *, #36084, .F. ) ;
#15095=ORIENTED_EDGE ( 'NONE', *, *, #1927, .T. ) ;
#15124=PLANE ( 'NONE',  #29291 ) ;
#15137=ORIENTED_EDGE ( 'NONE', *, *, #62014, .T. ) ;
#15213=AXIS2_PLACEMENT_3D ( 'NONE', #58149, #52540, #9962 ) ;
#15226=ORIENTED_EDGE ( 'NONE', *, *, #5978, .T. ) ;
#15233=VERTEX_POINT ( 'NONE', #51769 ) ;
#15236=ORIENTED_EDGE ( 'NONE', *, *, #31614, .T. ) ;
#15237=DIRECTION ( 'NONE',  ( 1.000000000000000000, -0.000000000000000000, -0.000000000000000000 ) ) ;
#15253=SPHERICAL_SURFACE ( 'NONE', #144, 0.2500000000000000000 ) ;
#15255=VERTEX_POINT ( 'NONE', #41238 ) ;
#15265=FACE_OUTER_BOUND ( 'NONE', #33067, .T. ) ;
#15274=AXIS2_PLACEMENT_3D ( 'NONE', #61035, #29010, #67031 ) ;
#15276=AXIS2_PLACEMENT_3D ( 'NONE', #19969, #41469, #60041 ) ;
#15282=DIRECTION ( 'NONE',  ( -1.000000000000000000, 0.000000000000000000, 0.000000000000000000 ) ) ;
#15352=CARTESIAN_POINT ( 'NONE',  ( 13.25000000000000355, 28.24999999999998934, 3.750000000000000000 ) ) ;
#15364=DIRECTION ( 'NONE',  ( 0.000000000000000000, -1.000000000000000000, 0.000000000000000000 ) ) ;
#15377=ADVANCED_FACE ( 'NONE', ( #5981 ), #645, .F. ) ;
#15379=CARTESIAN_POINT ( 'NONE',  ( -13.25000000000000355, 28.24999999999998934, 3.750000000000000000 ) ) ;
#15392=CARTESIAN_POINT ( 'NONE',  ( -17.75000000000000711, 31.24999999999999289, 3.750000000000000000 ) ) ;
#15425=DIRECTION ( 'NONE',  ( 0.000000000000000000, 0.000000000000000000, -1.000000000000000000 ) ) ;
#15448=EDGE_CURVE ( 'NONE', #65737, #7265, #25857, .T. ) ;
#15503=DIRECTION ( 'NONE',  ( 0.000000000000000000, 0.000000000000000000, -1.000000000000000000 ) ) ;
#15513=CARTESIAN_POINT ( 'NONE',  ( 17.75000000000000711, 31.24999999999999289, -3.750000000000000000 ) ) ;
#15542=DIRECTION ( 'NONE',  ( -0.000000000000000000, -0.000000000000000000, -1.000000000000000000 ) ) ;
#15613=VECTOR ( 'NONE', #55439, 1000.000000000000000 ) ;
#15647=DIRECTION ( 'NONE',  ( 0.000000000000000000, -0.000000000000000000, -1.000000000000000000 ) ) ;
#15652=DIRECTION ( 'NONE',  ( 1.000000000000000000, 0.000000000000000000, 0.000000000000000000 ) ) ;
#15729=DIRECTION ( 'NONE',  ( 0.000000000000000000, 0.000000000000000000, -1.000000000000000000 ) ) ;
#15731=ORIENTED_EDGE ( 'NONE', *, *, #57437, .F. ) ;
#15739=EDGE_CURVE ( 'NONE', #1324, #8679, #43587, .T. ) ;
#15764=DIRECTION ( 'NONE',  ( -1.000000000000000000, 0.000000000000000000, 0.000000000000000000 ) ) ;
#15765=AXIS2_PLACEMENT_3D ( 'NONE', #55174, #12615, #61481 ) ;
#15768=EDGE_CURVE ( 'NONE', #38442, #58700, #41065, .T. ) ;
#15786=CIRCLE ( 'NONE', #47243, 0.7499999999999997780 ) ;
#15796=AXIS2_PLACEMENT_3D ( 'NONE', #54169, #12281, #66101 ) ;
#15806=FACE_OUTER_BOUND ( 'NONE', #28311, .T. ) ;
#15811=VECTOR ( 'NONE', #36232, 1000.000000000000000 ) ;
#15814=TOROIDAL_SURFACE ( 'NONE', #14699, 0.5000000000000000000, 0.2500000000000000000 ) ;
#15816=FACE_OUTER_BOUND ( 'NONE', #35551, .T. ) ;
#15831=CIRCLE ( 'NONE', #59574, 0.2500000000000002220 ) ;
#15837=VERTEX_POINT ( 'NONE', #19208 ) ;
#15855=DIRECTION ( 'NONE',  ( -1.000000000000000000, 0.000000000000000000, 0.000000000000000000 ) ) ;
#15856=DIRECTION ( 'NONE',  ( 0.000000000000000000, 0.000000000000000000, -1.000000000000000000 ) ) ;
#15860=ADVANCED_FACE ( 'NONE', ( #67411 ), #30110, .T. ) ;
#15865=DIRECTION ( 'NONE',  ( 0.000000000000000000, 0.000000000000000000, 1.000000000000000000 ) ) ;
#15883=VECTOR ( 'NONE', #40828, 1000.000000000000000 ) ;
#15890=DIRECTION ( 'NONE',  ( 0.000000000000000000, -1.000000000000000000, 0.000000000000000000 ) ) ;
#15900=ORIENTED_EDGE ( 'NONE', *, *, #62983, .T. ) ;
#15903=DIRECTION ( 'NONE',  ( 0.000000000000000000, 0.000000000000000000, -1.000000000000000000 ) ) ;
#15908=DIRECTION ( 'NONE',  ( 1.000000000000000000, -0.000000000000000000, 0.000000000000000000 ) ) ;
#15917=ORIENTED_EDGE ( 'NONE', *, *, #21203, .F. ) ;
#15937=ADVANCED_FACE ( 'NONE', ( #34 ), #32818, .F. ) ;
#15957=CIRCLE ( 'NONE', #16002, 0.2500000000000002220 ) ;
#15970=CARTESIAN_POINT ( 'NONE',  ( -13.25000000000000355, 28.24999999999998934, -3.750000000000000000 ) ) ;
#16002=AXIS2_PLACEMENT_3D ( 'NONE', #35480, #25259, #46057 ) ;
#16006=CARTESIAN_POINT ( 'NONE',  ( 13.50000000000000355, 27.99999999999998934, 4.000000000000000000 ) ) ;
#16016=DIRECTION ( 'NONE',  ( 0.000000000000000000, 0.000000000000000000, -1.000000000000000000 ) ) ;
#16029=CIRCLE ( 'NONE', #37449, 0.7499999999999997780 ) ;
#16033=LINE ( 'NONE', #46678, #8936 ) ;
#16041=DIRECTION ( 'NONE',  ( 5.782411586589351722E-16, 1.000000000000000000, 0.000000000000000000 ) ) ;
#16042=DIRECTION ( 'NONE',  ( -1.000000000000000000, 0.000000000000000000, 0.000000000000000000 ) ) ;
#16050=DIRECTION ( 'NONE',  ( 1.000000000000000000, -0.000000000000000000, 0.000000000000000000 ) ) ;
#16054=CARTESIAN_POINT ( 'NONE',  ( -8.750000000000001776, 25.24999999999998934, -3.750000000000000000 ) ) ;
#16068=DIRECTION ( 'NONE',  ( 8.673617379884026597E-16, -1.000000000000000000, 0.000000000000000000 ) ) ;
#16077=DIRECTION ( 'NONE',  ( -5.782411586589351722E-16, 1.000000000000000000, 0.000000000000000000 ) ) ;
#16115=CYLINDRICAL_SURFACE ( 'NONE', #63069, 0.2500000000000002220 ) ;
#16116=FACE_OUTER_BOUND ( 'NONE', #48240, .T. ) ;
#16122=CARTESIAN_POINT ( 'NONE',  ( -25.00000000000000355, 36.75000000000000000, 4.000000000000000000 ) ) ;
#16132=ORIENTED_EDGE ( 'NONE', *, *, #14205, .F. ) ;
#16153=EDGE_CURVE ( 'NONE', #44124, #12301, #47155, .T. ) ;
#16192=DIRECTION ( 'NONE',  ( 0.000000000000000000, 0.000000000000000000, -1.000000000000000000 ) ) ;
#16208=FACE_OUTER_BOUND ( 'NONE', #48598, .T. ) ;
#16213=ADVANCED_FACE ( 'NONE', ( #31690 ), #27430, .T. ) ;
#16221=DIRECTION ( 'NONE',  ( 1.000000000000000000, 0.000000000000000000, 0.000000000000000000 ) ) ;
#16245=VECTOR ( 'NONE', #53311, 1000.000000000000000 ) ;
#16248=CARTESIAN_POINT ( 'NONE',  ( 18.25000000000000711, 0.000000000000000000, 3.750000000000000000 ) ) ;
#16267=DIRECTION ( 'NONE',  ( -1.000000000000000000, 0.000000000000000000, 0.000000000000000000 ) ) ;
#16275=EDGE_LOOP ( 'NONE', ( #21952, #46117, #27117, #48230 ) ) ;
#16338=CIRCLE ( 'NONE', #20833, 0.2500000000000002220 ) ;
#16355=DIRECTION ( 'NONE',  ( 0.000000000000000000, 0.000000000000000000, -1.000000000000000000 ) ) ;
#16368=DIRECTION ( 'NONE',  ( 0.000000000000000000, 0.000000000000000000, -1.000000000000000000 ) ) ;
#16371=CIRCLE ( 'NONE', #15274, 0.2500000000000002220 ) ;
#16378=DIRECTION ( 'NONE',  ( 0.000000000000000000, 1.000000000000000000, 0.000000000000000000 ) ) ;
#16397=EDGE_CURVE ( 'NONE', #56763, #38684, #65128, .T. ) ;
#16473=VECTOR ( 'NONE', #1752, 1000.000000000000000 ) ;
#16486=CARTESIAN_POINT ( 'NONE',  ( -17.75000000000000711, 31.24999999999999289, -4.000000000000000000 ) ) ;
#16497=FACE_OUTER_BOUND ( 'NONE', #14853, .T. ) ;
#16509=DIRECTION ( 'NONE',  ( 0.000000000000000000, 1.000000000000000000, 0.000000000000000000 ) ) ;
#16511=CARTESIAN_POINT ( 'NONE',  ( -19.49999999999997513, 8.000000000000000000, -4.000000000000000000 ) ) ;
#16549=EDGE_CURVE ( 'NONE', #58067, #34410, #55069, .T. ) ;
#16550=DIRECTION ( 'NONE',  ( 0.000000000000000000, 0.000000000000000000, -1.000000000000000000 ) ) ;
#16611=CARTESIAN_POINT ( 'NONE',  ( 9.250000000000003553, 27.74999999999998934, 4.000000000000000000 ) ) ;
#16629=DIRECTION ( 'NONE',  ( 0.000000000000000000, 0.000000000000000000, 1.000000000000000000 ) ) ;
#16658=CARTESIAN_POINT ( 'NONE',  ( -8.750000000000001776, 25.24999999999998934, 3.750000000000000000 ) ) ;
#16659=AXIS2_PLACEMENT_3D ( 'NONE', #17739, #59932, #33217 ) ;
#16667=DIRECTION ( 'NONE',  ( 0.000000000000000000, 0.000000000000000000, -1.000000000000000000 ) ) ;
#16676=DIRECTION ( 'NONE',  ( 0.000000000000000000, 0.000000000000000000, -1.000000000000000000 ) ) ;
#16703=PRESENTATION_STYLE_ASSIGNMENT (( #60596 ) ) ;
#16721=AXIS2_PLACEMENT_3D ( 'NONE', #59419, #11253, #32701 ) ;
#16733=AXIS2_PLACEMENT_3D ( 'NONE', #63348, #41941, #5615 ) ;
#16753=DIRECTION ( 'NONE',  ( 1.000000000000000000, 8.673617379884027583E-16, 0.000000000000000000 ) ) ;
#16759=VECTOR ( 'NONE', #46434, 1000.000000000000000 ) ;
#16771=ADVANCED_FACE ( 'NONE', ( #2666 ), #19918, .T. ) ;
#16809=AXIS2_PLACEMENT_3D ( 'NONE', #63003, #14844, #36321 ) ;
#16838=AXIS2_PLACEMENT_3D ( 'NONE', #3130, #35207, #50695 ) ;
#16839=AXIS2_PLACEMENT_3D ( 'NONE', #64175, #30776, #51913 ) ;
#16845=VERTEX_POINT ( 'NONE', #67082 ) ;
#16853=ORIENTED_EDGE ( 'NONE', *, *, #39621, .T. ) ;
#16875=VERTEX_POINT ( 'NONE', #52991 ) ;
#16885=VERTEX_POINT ( 'NONE', #4786 ) ;
#16889=AXIS2_PLACEMENT_3D ( 'NONE', #41932, #14825, #5267 ) ;
#16890=DIRECTION ( 'NONE',  ( 0.000000000000000000, 1.000000000000000000, 0.000000000000000000 ) ) ;
#16911=ORIENTED_EDGE ( 'NONE', *, *, #14953, .F. ) ;
#16923=CARTESIAN_POINT ( 'NONE',  ( 0.000000000000000000, 30.74999999999999289, 3.750000000000000000 ) ) ;
#16936=CARTESIAN_POINT ( 'NONE',  ( 13.75000000000000533, 30.74999999999999289, 4.000000000000000000 ) ) ;
#16948=EDGE_LOOP ( 'NONE', ( #47508, #64377, #5758, #21344 ) ) ;
#17020=ADVANCED_FACE ( 'NONE', ( #54359 ), #27943, .T. ) ;
#17034=ORIENTED_EDGE ( 'NONE', *, *, #34232, .F. ) ;
#17086=CARTESIAN_POINT ( 'NONE',  ( -4.750000000000002665, 22.24999999999998579, -4.000000000000000000 ) ) ;
#17091=CARTESIAN_POINT ( 'NONE',  ( -22.75000000000000711, 36.75000000000000000, -3.750000000000000000 ) ) ;
#17100=DIRECTION ( 'NONE',  ( 0.000000000000000000, 0.000000000000000000, 1.000000000000000000 ) ) ;
#17103=VECTOR ( 'NONE', #14479, 1000.000000000000000 ) ;
#17109=DIRECTION ( 'NONE',  ( 0.000000000000000000, 0.000000000000000000, -1.000000000000000000 ) ) ;
#17144=DIRECTION ( 'NONE',  ( 0.000000000000000000, 0.000000000000000000, -1.000000000000000000 ) ) ;
#17155=DIRECTION ( 'NONE',  ( 0.000000000000000000, -0.000000000000000000, -1.000000000000000000 ) ) ;
#17171=DIRECTION ( 'NONE',  ( 0.000000000000000000, 0.000000000000000000, -1.000000000000000000 ) ) ;
#17188=CLOSED_SHELL ( 'NONE', ( #44217, #27677, #54164, #37972, #14239, #60821, #21697, #28663, #40713, #58934, #17525, #15377, #59104, #3022, #2136, #15937, #43512, #37152, #38893, #67997, #61565, #13644, #66117, #57677, #27696, #419, #4319, #4036, #22392, #53624, #58080, #53764, #14257, #20014, #54550, #18552, #21049, #932, #20492, #7475, #65664, #20405, #20158, #57989, #42460, #59234, #41928, #32959, #54781, #35533, #49345, #18685, #41332, #51610, #35929, #66030, #44309, #62107, #47472, #18525, #19885, #44137, #59968, #22778, #17020, #59300, #26809, #59222, #55436, #53527, #16771, #39221, #55261, #61476, #6504, #15860, #4698, #27071, #3870, #67889, #14620, #2234, #5878, #10960, #11913, #30137, #68741, #51235, #50060, #36423, #11820, #54077, #22092, #38106, #23491, #25303, #8516, #34088, #7946, #59701, #38976, #11838, #52447, #29381, #56313, #18762, #21973, #35350, #13263, #51556, #27680, #40333, #52833, #38017, #41092, #11107, #19457, #65694, #4824, #68642, #53074, #68384, #6838, #34783, #30880, #46052, #10800, #58049, #43727, #55937, #66082, #58693, #37310, #41748, #28882, #13257, #47421, #45405, #20815, #16213, #18022, #43979, #11190, #23367, #14612, #5711, #55496, #36430, #34686, #37550, #32239, #30391, #585, #11561, #68084, #19123, #7696, #45008 ) ) ;
#17206=PLANE ( 'NONE',  #23688 ) ;
#17238=SPHERICAL_SURFACE ( 'NONE', #4212, 0.2500000000000000000 ) ;
#17241=CARTESIAN_POINT ( 'NONE',  ( -22.50000000000000711, 34.24999999999999289, 3.750000000000000000 ) ) ;
#17284=DIRECTION ( 'NONE',  ( -0.000000000000000000, -0.000000000000000000, 1.000000000000000000 ) ) ;
#17293=CARTESIAN_POINT ( 'NONE',  ( 0.000000000000000000, 24.74999999999998579, 3.750000000000000000 ) ) ;
#17294=VERTEX_POINT ( 'NONE', #48358 ) ;
#17295=ORIENTED_EDGE ( 'NONE', *, *, #3485, .F. ) ;
#17301=DIRECTION ( 'NONE',  ( 0.000000000000000000, 0.000000000000000000, -1.000000000000000000 ) ) ;
#17311=VERTEX_POINT ( 'NONE', #37820 ) ;
#17362=CIRCLE ( 'NONE', #69068, 0.2500000000000002220 ) ;
#17376=ORIENTED_EDGE ( 'NONE', *, *, #46021, .T. ) ;
#17378=DIRECTION ( 'NONE',  ( -1.000000000000000000, 0.000000000000000000, 0.000000000000000000 ) ) ;
#17437=AXIS2_PLACEMENT_3D ( 'NONE', #16006, #749, #15647 ) ;
#17444=AXIS2_PLACEMENT_3D ( 'NONE', #27195, #16368, #64856 ) ;
#17450=AXIS2_PLACEMENT_3D ( 'NONE', #31154, #63189, #30818 ) ;
#17466=ORIENTED_EDGE ( 'NONE', *, *, #345, .T. ) ;
#17474=ORIENTED_EDGE ( 'NONE', *, *, #14953, .T. ) ;
#17508=ORIENTED_EDGE ( 'NONE', *, *, #3976, .F. ) ;
#17518=EDGE_CURVE ( 'NONE', #66411, #58978, #65276, .T. ) ;
#17525=ADVANCED_FACE ( 'NONE', ( #68570 ), #29886, .F. ) ;
#17571=CARTESIAN_POINT ( 'NONE',  ( 22.75000000000000711, 36.75000000000000000, 4.000000000000000000 ) ) ;
#17573=VERTEX_POINT ( 'NONE', #30207 ) ;
#17582=ORIENTED_EDGE ( 'NONE', *, *, #41906, .F. ) ;
#17603=EDGE_CURVE ( 'NONE', #32928, #37155, #69265, .T. ) ;
#17650=CARTESIAN_POINT ( 'NONE',  ( -4.500000000000002665, 21.99999999999998579, 3.750000000000000000 ) ) ;
#17671=ORIENTED_EDGE ( 'NONE', *, *, #9476, .T. ) ;
#17676=DIRECTION ( 'NONE',  ( 0.000000000000000000, 0.000000000000000000, -1.000000000000000000 ) ) ;
#17677=CARTESIAN_POINT ( 'NONE',  ( -22.25000000000000711, 33.74999999999999289, -4.000000000000000000 ) ) ;
#17683=FACE_OUTER_BOUND ( 'NONE', #58386, .T. ) ;
#17702=CIRCLE ( 'NONE', #28900, 0.2500000000000002220 ) ;
#17704=CARTESIAN_POINT ( 'NONE',  ( 4.250000000000001776, 21.99999999999998579, -4.000000000000000000 ) ) ;
#17712=DIRECTION ( 'NONE',  ( 0.000000000000000000, 0.000000000000000000, -1.000000000000000000 ) ) ;
#17723=APPLICATION_CONTEXT ( 'automotive_design' ) ;
#17739=CARTESIAN_POINT ( 'NONE',  ( -4.750000000000002665, 24.74999999999998579, -3.750000000000000000 ) ) ;
#17777=DIRECTION ( 'NONE',  ( 0.000000000000000000, 1.000000000000000000, -0.000000000000000000 ) ) ;
#17788=LINE ( 'NONE', #49128, #53914 ) ;
#17804=ORIENTED_EDGE ( 'NONE', *, *, #6267, .T. ) ;
#17837=FACE_OUTER_BOUND ( 'NONE', #62153, .T. ) ;
#17850=VECTOR ( 'NONE', #59692, 1000.000000000000114 ) ;
#17862=EDGE_CURVE ( 'NONE', #40174, #30006, #6874, .T. ) ;
#17866=VERTEX_POINT ( 'NONE', #18909 ) ;
#17886=CARTESIAN_POINT ( 'NONE',  ( 8.750000000000001776, 25.24999999999998934, 3.750000000000000000 ) ) ;
#17889=ORIENTED_EDGE ( 'NONE', *, *, #18741, .T. ) ;
#17973=DIRECTION ( 'NONE',  ( 1.000000000000000000, -0.000000000000000000, -0.000000000000000000 ) ) ;
#18022=ADVANCED_FACE ( 'NONE', ( #33309 ), #16115, .T. ) ;
#18027=AXIS2_PLACEMENT_3D ( 'NONE', #20366, #35164, #56622 ) ;
#18034=CARTESIAN_POINT ( 'NONE',  ( 22.50000000000000711, 36.75000000000000000, -3.750000000000000000 ) ) ;
#18040=( GEOMETRIC_REPRESENTATION_CONTEXT ( 3 ) GLOBAL_UNCERTAINTY_ASSIGNED_CONTEXT ( ( #42470 ) ) GLOBAL_UNIT_ASSIGNED_CONTEXT ( ( #67001, #67335, #62731 ) ) REPRESENTATION_CONTEXT ( 'NONE', 'WORKASPACE' ) );
#18068=EDGE_CURVE ( 'NONE', #47699, #36693, #58996, .T. ) ;
#18079=AXIS2_PLACEMENT_3D ( 'NONE', #42652, #15908, #63018 ) ;
#18107=DIRECTION ( 'NONE',  ( 0.000000000000000000, 0.000000000000000000, -1.000000000000000000 ) ) ;
#18121=DIRECTION ( 'NONE',  ( -1.000000000000000000, 0.000000000000000000, 0.000000000000000000 ) ) ;
#18162=AXIS2_PLACEMENT_3D ( 'NONE', #12763, #51451, #23668 ) ;
#18163=LINE ( 'NONE', #56486, #56724 ) ;
#18189=EDGE_CURVE ( 'NONE', #43113, #1595, #37309, .T. ) ;
#18207=ORIENTED_EDGE ( 'NONE', *, *, #16549, .T. ) ;
#18216=ORIENTED_EDGE ( 'NONE', *, *, #51324, .F. ) ;
#18237=DIRECTION ( 'NONE',  ( -1.000000000000000000, 0.000000000000000000, 0.000000000000000000 ) ) ;
#18242=CARTESIAN_POINT ( 'NONE',  ( 22.75000000000000711, 36.75000000000000000, -3.750000000000000000 ) ) ;
#18284=TOROIDAL_SURFACE ( 'NONE', #14940, 0.5000000000000000000, 0.2500000000000000000 ) ;
#18293=CARTESIAN_POINT ( 'NONE',  ( 9.250000000000003553, 27.74999999999998934, -4.000000000000000000 ) ) ;
#18316=DIRECTION ( 'NONE',  ( -1.000000000000000000, 0.000000000000000000, 0.000000000000000000 ) ) ;
#18330=EDGE_CURVE ( 'NONE', #47699, #15837, #23799, .T. ) ;
#18347=ORIENTED_EDGE ( 'NONE', *, *, #43370, .T. ) ;
#18361=DIRECTION ( 'NONE',  ( 1.000000000000000000, -0.000000000000000000, -0.000000000000000000 ) ) ;
#18364=EDGE_CURVE ( 'NONE', #17866, #6972, #28532, .T. ) ;
#18379=EDGE_CURVE ( 'NONE', #42065, #60451, #5688, .T. ) ;
#18391=ORIENTED_EDGE ( 'NONE', *, *, #52659, .F. ) ;
#18401=DIRECTION ( 'NONE',  ( 1.000000000000000000, -0.000000000000000000, 0.000000000000000000 ) ) ;
#18410=CARTESIAN_POINT ( 'NONE',  ( 4.250000000000001776, 21.74999999999998579, 4.000000000000000000 ) ) ;
#18427=DIRECTION ( 'NONE',  ( -0.000000000000000000, -0.000000000000000000, 1.000000000000000000 ) ) ;
#18435=EDGE_CURVE ( 'NONE', #5753, #17573, #22650, .T. ) ;
#18436=TOROIDAL_SURFACE ( 'NONE', #30762, 0.5000000000000000000, 0.2500000000000000000 ) ;
#18442=CYLINDRICAL_SURFACE ( 'NONE', #46635, 0.2500000000000002220 ) ;
#18459=EDGE_CURVE ( 'NONE', #36655, #54902, #56330, .T. ) ;
#18462=LINE ( 'NONE', #34611, #42604 ) ;
#18477=CARTESIAN_POINT ( 'NONE',  ( -18.25000000000000711, 33.74999999999999289, 4.000000000000000000 ) ) ;
#18480=CARTESIAN_POINT ( 'NONE',  ( -9.250000000000003553, 25.24999999999998934, -4.000000000000000000 ) ) ;
#18496=ORIENTED_EDGE ( 'NONE', *, *, #52902, .T. ) ;
#18497=VECTOR ( 'NONE', #66182, 1000.000000000000000 ) ;
#18513=EDGE_CURVE ( 'NONE', #38684, #27999, #2091, .T. ) ;
#18525=ADVANCED_FACE ( 'NONE', ( #45121 ), #19013, .T. ) ;
#18526=VECTOR ( 'NONE', #45664, 1000.000000000000000 ) ;
#18527=DIRECTION ( 'NONE',  ( 0.000000000000000000, 0.000000000000000000, 1.000000000000000000 ) ) ;
#18537=CARTESIAN_POINT ( 'NONE',  ( 22.75000000000000711, 36.75000000000000000, -4.000000000000000000 ) ) ;
#18548=DIRECTION ( 'NONE',  ( 5.782411586589351722E-16, 1.000000000000000000, -0.000000000000000000 ) ) ;
#18552=ADVANCED_FACE ( 'NONE', ( #9553 ), #31664, .F. ) ;
#18564=AXIS2_PLACEMENT_3D ( 'NONE', #39472, #38789, #45460 ) ;
#18595=DIRECTION ( 'NONE',  ( 0.000000000000000000, 0.000000000000000000, 1.000000000000000000 ) ) ;
#18601=ORIENTED_EDGE ( 'NONE', *, *, #11585, .F. ) ;
#18614=DIRECTION ( 'NONE',  ( -1.000000000000000000, 0.000000000000000000, 0.000000000000000000 ) ) ;
#18640=DIRECTION ( 'NONE',  ( 0.000000000000000000, 1.000000000000000000, 0.000000000000000000 ) ) ;
#18653=ORIENTED_EDGE ( 'NONE', *, *, #12368, .T. ) ;
#18663=CIRCLE ( 'NONE', #43430, 0.2500000000000002220 ) ;
#18664=ORIENTED_EDGE ( 'NONE', *, *, #14094, .T. ) ;
#18672=CARTESIAN_POINT ( 'NONE',  ( 24.00000000000000000, 1.000000000000000000, 3.000000000000000000 ) ) ;
#18685=ADVANCED_FACE ( 'NONE', ( #21111 ), #42609, .F. ) ;
#18700=CARTESIAN_POINT ( 'NONE',  ( -18.25000000000000711, 33.74999999999999289, 3.750000000000000000 ) ) ;
#18712=AXIS2_PLACEMENT_3D ( 'NONE', #50504, #66321, #61383 ) ;
#18723=CARTESIAN_POINT ( 'NONE',  ( -9.250000000000003553, 27.74999999999998934, 3.750000000000000000 ) ) ;
#18741=EDGE_CURVE ( 'NONE', #31383, #48589, #10908, .T. ) ;
#18742=ORIENTED_EDGE ( 'NONE', *, *, #32914, .T. ) ;
#18762=ADVANCED_FACE ( 'NONE', ( #54498 ), #11592, .T. ) ;
#18789=EDGE_LOOP ( 'NONE', ( #10920, #27179, #11043, #33829 ) ) ;
#18799=CARTESIAN_POINT ( 'NONE',  ( -4.750000000000002665, 22.24999999999998579, -4.000000000000000000 ) ) ;
#18832=EDGE_LOOP ( 'NONE', ( #3477, #13904, #10557, #66868 ) ) ;
#18846=DIRECTION ( 'NONE',  ( -1.000000000000000000, 0.000000000000000000, 0.000000000000000000 ) ) ;
#18857=DIRECTION ( 'NONE',  ( 0.000000000000000000, 0.000000000000000000, -1.000000000000000000 ) ) ;
#18861=VECTOR ( 'NONE', #50883, 1000.000000000000000 ) ;
#18906=EDGE_LOOP ( 'NONE', ( #28676, #21423, #25300 ) ) ;
#18909=CARTESIAN_POINT ( 'NONE',  ( -18.00000000000000711, 31.24999999999999289, 3.750000000000000000 ) ) ;
#18912=DIRECTION ( 'NONE',  ( 0.000000000000000000, 0.000000000000000000, -1.000000000000000000 ) ) ;
#18923=DIRECTION ( 'NONE',  ( 0.000000000000000000, -1.000000000000000000, 0.000000000000000000 ) ) ;
#18948=AXIS2_PLACEMENT_3D ( 'NONE', #37620, #12191, #60052 ) ;
#18970=EDGE_CURVE ( 'NONE', #28845, #59451, #29462, .T. ) ;
#18995=ORIENTED_EDGE ( 'NONE', *, *, #53531, .F. ) ;
#19010=ORIENTED_EDGE ( 'NONE', *, *, #27572, .T. ) ;
#19013=CYLINDRICAL_SURFACE ( 'NONE', #8030, 1.000000000000000000 ) ;
#19017=ORIENTED_EDGE ( 'NONE', *, *, #9517, .T. ) ;
#19040=EDGE_CURVE ( 'NONE', #2945, #62845, #7029, .T. ) ;
#19045=CARTESIAN_POINT ( 'NONE',  ( -17.75000000000000711, 30.99999999999999289, 4.000000000000000000 ) ) ;
#19062=ORIENTED_EDGE ( 'NONE', *, *, #1085, .T. ) ;
#19123=ADVANCED_FACE ( 'NONE', ( #21357 ), #66585, .F. ) ;
#19131=CARTESIAN_POINT ( 'NONE',  ( -18.25000000000000711, 33.74999999999999289, -3.750000000000000000 ) ) ;
#19151=VERTEX_POINT ( 'NONE', #54741 ) ;
#19158=DIRECTION ( 'NONE',  ( 0.000000000000000000, -1.000000000000000000, 0.000000000000000000 ) ) ;
#19163=DIRECTION ( 'NONE',  ( 1.000000000000000000, -0.000000000000000000, -0.000000000000000000 ) ) ;
#19187=ORIENTED_EDGE ( 'NONE', *, *, #63167, .T. ) ;
#19189=CARTESIAN_POINT ( 'NONE',  ( -9.000000000000003553, 25.24999999999998934, -3.750000000000000000 ) ) ;
#19208=CARTESIAN_POINT ( 'NONE',  ( 13.75000000000000533, 30.99999999999999289, -3.750000000000000000 ) ) ;
#19253=FACE_OUTER_BOUND ( 'NONE', #44944, .T. ) ;
#19256=ORIENTED_EDGE ( 'NONE', *, *, #39187, .T. ) ;
#19266=CIRCLE ( 'NONE', #39559, 0.2500000000000002220 ) ;
#19286=DIRECTION ( 'NONE',  ( 0.000000000000000000, -1.000000000000000000, 0.000000000000000000 ) ) ;
#19307=DIRECTION ( 'NONE',  ( 0.000000000000000000, 0.000000000000000000, 1.000000000000000000 ) ) ;
#19309=DIRECTION ( 'NONE',  ( 0.000000000000000000, -1.000000000000000000, 0.000000000000000000 ) ) ;
#19342=SPHERICAL_SURFACE ( 'NONE', #11525, 1.000000000000000000 ) ;
#19367=EDGE_CURVE ( 'NONE', #37693, #52614, #63222, .T. ) ;
#19376=CARTESIAN_POINT ( 'NONE',  ( 0.000000000000000000, 1.000000000000000000, 3.000000000000000000 ) ) ;
#19381=ORIENTED_EDGE ( 'NONE', *, *, #13500, .T. ) ;
#19410=CIRCLE ( 'NONE', #27164, 0.2500000000000002220 ) ;
#19412=CARTESIAN_POINT ( 'NONE',  ( 24.00000000000000355, 36.75000000000000000, 3.750000000000000000 ) ) ;
#19415=EDGE_CURVE ( 'NONE', #11393, #1454, #42449, .T. ) ;
#19416=CARTESIAN_POINT ( 'NONE',  ( 22.25000000000000711, 33.74999999999999289, 3.750000000000000000 ) ) ;
#19447=ORIENTED_EDGE ( 'NONE', *, *, #29555, .F. ) ;
#19453=ORIENTED_EDGE ( 'NONE', *, *, #55112, .T. ) ;
#19457=ADVANCED_FACE ( 'NONE', ( #36103 ), #47031, .T. ) ;
#19461=CARTESIAN_POINT ( 'NONE',  ( 8.750000000000001776, 25.24999999999998934, -3.750000000000000000 ) ) ;
#19478=ORIENTED_EDGE ( 'NONE', *, *, #60667, .F. ) ;
#19501=AXIS2_PLACEMENT_3D ( 'NONE', #19416, #40558, #62332 ) ;
#19532=VECTOR ( 'NONE', #37600, 1000.000000000000000 ) ;
#19543=CIRCLE ( 'NONE', #30786, 0.2500000000000002220 ) ;
#19554=DIRECTION ( 'NONE',  ( -9.376883653928687363E-17, 1.000000000000000000, 0.000000000000000000 ) ) ;
#19569=CIRCLE ( 'NONE', #58849, 4.000000000000000000 ) ;
#19600=ORIENTED_EDGE ( 'NONE', *, *, #9655, .T. ) ;
#19636=ORIENTED_EDGE ( 'NONE', *, *, #8831, .T. ) ;
#19650=AXIS2_PLACEMENT_3D ( 'NONE', #61632, #23329, #50415 ) ;
#19696=VERTEX_POINT ( 'NONE', #68037 ) ;
#19717=EDGE_CURVE ( 'NONE', #4438, #2325, #25104, .T. ) ;
#19721=DIRECTION ( 'NONE',  ( 0.000000000000000000, 0.000000000000000000, -1.000000000000000000 ) ) ;
#19733=ORIENTED_EDGE ( 'NONE', *, *, #9414, .T. ) ;
#19748=CYLINDRICAL_SURFACE ( 'NONE', #50554, 1.000000000000000888 ) ;
#19768=SPHERICAL_SURFACE ( 'NONE', #61772, 0.2500000000000000000 ) ;
#19796=DIRECTION ( 'NONE',  ( 1.000000000000000000, 0.000000000000000000, 0.000000000000000000 ) ) ;
#19836=SHAPE_REPRESENTATION_RELATIONSHIP ( 'NONE' , 'NONE' ,  #15001, #55567 ) ;
#19840=DIRECTION ( 'NONE',  ( -1.000000000000000000, 0.000000000000000000, 0.000000000000000000 ) ) ;
#19846=EDGE_CURVE ( 'NONE', #67406, #50331, #41150, .T. ) ;
#19871=ORIENTED_EDGE ( 'NONE', *, *, #14642, .F. ) ;
#19878=PLANE ( 'NONE',  #4409 ) ;
#19885=ADVANCED_FACE ( 'NONE', ( #39760 ), #29514, .T. ) ;
#19886=DIRECTION ( 'NONE',  ( -1.000000000000000000, 0.000000000000000000, 0.000000000000000000 ) ) ;
#19895=CARTESIAN_POINT ( 'NONE',  ( -24.00000000000000000, -2.250452076942884869E-15, 4.000000000000000000 ) ) ;
#19896=DIRECTION ( 'NONE',  ( -1.000000000000000000, 0.000000000000000000, 0.000000000000000000 ) ) ;
#19903=ORIENTED_EDGE ( 'NONE', *, *, #43278, .T. ) ;
#19918=SPHERICAL_SURFACE ( 'NONE', #48451, 0.2500000000000000000 ) ;
#19969=CARTESIAN_POINT ( 'NONE',  ( -17.75000000000000711, 31.24999999999999289, -3.750000000000000000 ) ) ;
#19980=DIRECTION ( 'NONE',  ( 0.000000000000000000, 0.000000000000000000, 1.000000000000000000 ) ) ;
#19996=EDGE_CURVE ( 'NONE', #6652, #25552, #21214, .T. ) ;
#20014=ADVANCED_FACE ( 'NONE', ( #16497 ), #6933, .F. ) ;
#20015=DIRECTION ( 'NONE',  ( 0.000000000000000000, 0.000000000000000000, 1.000000000000000000 ) ) ;
#20069=CARTESIAN_POINT ( 'NONE',  ( 9.250000000000003553, 27.74999999999998934, -3.750000000000000000 ) ) ;
#20122=ORIENTED_EDGE ( 'NONE', *, *, #9938, .T. ) ;
#20139=DIRECTION ( 'NONE',  ( 0.000000000000000000, 1.000000000000000000, 0.000000000000000000 ) ) ;
#20154=FACE_OUTER_BOUND ( 'NONE', #55251, .T. ) ;
#20158=ADVANCED_FACE ( 'NONE', ( #55471 ), #45305, .T. ) ;
#20201=DIRECTION ( 'NONE',  ( 0.000000000000000000, 0.000000000000000000, -1.000000000000000000 ) ) ;
#20203=DIRECTION ( 'NONE',  ( -0.000000000000000000, 1.000000000000000000, -0.000000000000000000 ) ) ;
#20207=ORIENTED_EDGE ( 'NONE', *, *, #10585, .F. ) ;
#20223=LINE ( 'NONE', #9706, #67370 ) ;
#20239=EDGE_CURVE ( 'NONE', #35855, #68529, #47042, .T. ) ;
#20259=CARTESIAN_POINT ( 'NONE',  ( 13.75000000000000355, 28.24999999999998934, -4.000000000000000000 ) ) ;
#20265=AXIS2_PLACEMENT_3D ( 'NONE', #10855, #1881, #38930 ) ;
#20298=ORIENTED_EDGE ( 'NONE', *, *, #65904, .T. ) ;
#20300=CARTESIAN_POINT ( 'NONE',  ( 15.00000000000000000, 8.000000000000000000, -3.500000000000017764 ) ) ;
#20311=CIRCLE ( 'NONE', #59626, 0.2500000000000002220 ) ;
#20354=CARTESIAN_POINT ( 'NONE',  ( 4.500000000000002665, 24.99999999999998579, 4.000000000000000000 ) ) ;
#20359=PRODUCT ( '7. Upper Jaw', '7. Upper Jaw', '', ( #13171 ) ) ;
#20362=CIRCLE ( 'NONE', #10245, 0.2500000000000002220 ) ;
#20366=CARTESIAN_POINT ( 'NONE',  ( -25.00000000000000000, 0.000000000000000000, 4.000000000000000000 ) ) ;
#20405=ADVANCED_FACE ( 'NONE', ( #52643 ), #4400, .F. ) ;
#20429=ORIENTED_EDGE ( 'NONE', *, *, #26518, .F. ) ;
#20456=LINE ( 'NONE', #16511, #61775 ) ;
#20471=DIRECTION ( 'NONE',  ( 0.000000000000000000, 0.000000000000000000, -1.000000000000000000 ) ) ;
#20472=DIRECTION ( 'NONE',  ( 1.000000000000000000, -0.000000000000000000, -0.000000000000000000 ) ) ;
#20489=DIRECTION ( 'NONE',  ( -0.000000000000000000, -1.000000000000000000, -0.000000000000000000 ) ) ;
#20492=ADVANCED_FACE ( 'NONE', ( #39598 ), #34286, .T. ) ;
#20498=ORIENTED_EDGE ( 'NONE', *, *, #21616, .T. ) ;
#20507=VECTOR ( 'NONE', #59931, 1000.000000000000000 ) ;
#20521=VERTEX_POINT ( 'NONE', #56078 ) ;
#20574=DIRECTION ( 'NONE',  ( 1.000000000000000000, 0.000000000000000000, 0.000000000000000000 ) ) ;
#20640=VERTEX_POINT ( 'NONE', #24405 ) ;
#20650=ORIENTED_EDGE ( 'NONE', *, *, #12306, .F. ) ;
#20658=CARTESIAN_POINT ( 'NONE',  ( 4.750000000000002665, 24.99999999999998579, -3.750000000000000000 ) ) ;
#20666=DIRECTION ( 'NONE',  ( -1.000000000000000000, 0.000000000000000000, 0.000000000000000000 ) ) ;
#20693=ORIENTED_EDGE ( 'NONE', *, *, #5972, .T. ) ;
#20697=EDGE_CURVE ( 'NONE', #37155, #6425, #31406, .T. ) ;
#20698=CARTESIAN_POINT ( 'NONE',  ( -19.00000000000000000, 8.000000000000000000, 3.500000000000003997 ) ) ;
#20702=EDGE_CURVE ( 'NONE', #12003, #26708, #51045, .T. ) ;
#20723=LINE ( 'NONE', #63626, #26966 ) ;
#20735=EDGE_CURVE ( 'NONE', #68501, #46540, #12317, .T. ) ;
#20746=VERTEX_POINT ( 'NONE', #61560 ) ;
#20748=DIRECTION ( 'NONE',  ( 1.000000000000000000, -0.000000000000000000, 0.000000000000000000 ) ) ;
#20768=DIRECTION ( 'NONE',  ( 0.000000000000000000, 1.000000000000000000, 0.000000000000000000 ) ) ;
#20815=ADVANCED_FACE ( 'NONE', ( #34848 ), #24294, .T. ) ;
#20832=ORIENTED_EDGE ( 'NONE', *, *, #40446, .T. ) ;
#20833=AXIS2_PLACEMENT_3D ( 'NONE', #53212, #58473, #16629 ) ;
#20835=CARTESIAN_POINT ( 'NONE',  ( -13.50000000000000533, 30.74999999999999289, -3.750000000000000000 ) ) ;
#20844=CIRCLE ( 'NONE', #47862, 0.2500000000000002220 ) ;
#20846=ORIENTED_EDGE ( 'NONE', *, *, #65904, .F. ) ;
#20875=ORIENTED_EDGE ( 'NONE', *, *, #27572, .F. ) ;
#20901=DIRECTION ( 'NONE',  ( 1.000000000000000000, -0.000000000000000000, 0.000000000000000000 ) ) ;
#20910=CARTESIAN_POINT ( 'NONE',  ( 13.50000000000000355, 28.24999999999998934, -3.750000000000000000 ) ) ;
#20935=CARTESIAN_POINT ( 'NONE',  ( 8.750000000000001776, 25.24999999999998934, 4.000000000000000000 ) ) ;
#20946=CARTESIAN_POINT ( 'NONE',  ( 4.500000000000002665, 22.24999999999998579, 3.750000000000000000 ) ) ;
#20966=CARTESIAN_POINT ( 'NONE',  ( -9.250000000000003553, 27.74999999999998934, -4.000000000000000000 ) ) ;
#20971=AXIS2_PLACEMENT_3D ( 'NONE', #8299, #35375, #24112 ) ;
#20987=CARTESIAN_POINT ( 'NONE',  ( 9.250000000000003553, 0.000000000000000000, 3.750000000000000000 ) ) ;
#20994=CARTESIAN_POINT ( 'NONE',  ( 13.75000000000000533, 30.99999999999999289, -3.750000000000000000 ) ) ;
#21002=CARTESIAN_POINT ( 'NONE',  ( 17.75000000000000711, 30.74999999999999289, 3.750000000000000000 ) ) ;
#21004=ORIENTED_EDGE ( 'NONE', *, *, #26606, .T. ) ;
#21025=ORIENTED_EDGE ( 'NONE', *, *, #23410, .F. ) ;
#21038=EDGE_CURVE ( 'NONE', #7265, #38885, #20723, .T. ) ;
#21046=AXIS2_PLACEMENT_3D ( 'NONE', #37867, #94, #59237 ) ;
#21049=ADVANCED_FACE ( 'NONE', ( #15806 ), #56094, .T. ) ;
#21070=FACE_OUTER_BOUND ( 'NONE', #14588, .T. ) ;
#21083=DIRECTION ( 'NONE',  ( -0.000000000000000000, 0.000000000000000000, -1.000000000000000000 ) ) ;
#21091=CIRCLE ( 'NONE', #16659, 0.2500000000000002220 ) ;
#21095=VERTEX_POINT ( 'NONE', #28995 ) ;
#21097=ORIENTED_EDGE ( 'NONE', *, *, #53475, .T. ) ;
#21100=DIRECTION ( 'NONE',  ( -0.000000000000000000, -0.000000000000000000, 1.000000000000000000 ) ) ;
#21111=FACE_OUTER_BOUND ( 'NONE', #38322, .T. ) ;
#21126=EDGE_CURVE ( 'NONE', #28845, #38442, #5548, .T. ) ;
#21133=ORIENTED_EDGE ( 'NONE', *, *, #48401, .T. ) ;
#21147=LINE ( 'NONE', #69688, #33676 ) ;
#21157=EDGE_CURVE ( 'NONE', #55864, #52256, #45599, .T. ) ;
#21160=ORIENTED_EDGE ( 'NONE', *, *, #21157, .F. ) ;
#21164=CIRCLE ( 'NONE', #16733, 0.2500000000000002220 ) ;
#21203=EDGE_CURVE ( 'NONE', #30380, #39136, #15831, .T. ) ;
#21214=CIRCLE ( 'NONE', #41440, 0.2500000000000002220 ) ;
#21273=EDGE_CURVE ( 'NONE', #13443, #31383, #20311, .T. ) ;
#21301=VECTOR ( 'NONE', #45473, 1000.000000000000000 ) ;
#21332=ORIENTED_EDGE ( 'NONE', *, *, #10702, .F. ) ;
#21344=ORIENTED_EDGE ( 'NONE', *, *, #44127, .T. ) ;
#21347=CARTESIAN_POINT ( 'NONE',  ( 17.75000000000000711, 30.74999999999999289, -4.000000000000000000 ) ) ;
#21357=FACE_OUTER_BOUND ( 'NONE', #57804, .T. ) ;
#21392=VERTEX_POINT ( 'NONE', #743 ) ;
#21402=AXIS2_PLACEMENT_3D ( 'NONE', #31208, #57265, #40421 ) ;
#21408=DIRECTION ( 'NONE',  ( 1.000000000000000000, 0.000000000000000000, 0.000000000000000000 ) ) ;
#21409=CARTESIAN_POINT ( 'NONE',  ( 9.250000000000003553, 27.74999999999998934, 3.750000000000000000 ) ) ;
#21423=ORIENTED_EDGE ( 'NONE', *, *, #50704, .F. ) ;
#21442=CARTESIAN_POINT ( 'NONE',  ( 22.75000000000000711, 36.75000000000000000, 3.750000000000000000 ) ) ;
#21499=DIRECTION ( 'NONE',  ( -0.000000000000000000, -0.000000000000000000, 1.000000000000000000 ) ) ;
#21566=DIRECTION ( 'NONE',  ( 1.000000000000000000, 0.000000000000000000, 0.000000000000000000 ) ) ;
#21593=DIRECTION ( 'NONE',  ( 0.000000000000000000, 0.000000000000000000, -1.000000000000000000 ) ) ;
#21614=ORIENTED_EDGE ( 'NONE', *, *, #5459, .T. ) ;
#21616=EDGE_CURVE ( 'NONE', #2945, #56729, #6009, .T. ) ;
#21642=DIRECTION ( 'NONE',  ( 0.000000000000000000, 0.000000000000000000, -1.000000000000000000 ) ) ;
#21645=ORIENTED_EDGE ( 'NONE', *, *, #18970, .T. ) ;
#21654=FACE_OUTER_BOUND ( 'NONE', #47335, .T. ) ;
#21655=CIRCLE ( 'NONE', #47591, 0.2500000000000002220 ) ;
#21665=CARTESIAN_POINT ( 'NONE',  ( -13.74999999999998757, -7.950815931560351124E-15, 3.750000000000000000 ) ) ;
#21679=ORIENTED_EDGE ( 'NONE', *, *, #33462, .F. ) ;
#21681=CARTESIAN_POINT ( 'NONE',  ( -17.75000000000000711, 31.24999999999999289, 4.000000000000000000 ) ) ;
#21685=ORIENTED_EDGE ( 'NONE', *, *, #5159, .F. ) ;
#21688=DIRECTION ( 'NONE',  ( -1.000000000000000000, 0.000000000000000000, 0.000000000000000000 ) ) ;
#21694=ORIENTED_EDGE ( 'NONE', *, *, #35258, .T. ) ;
#21697=ADVANCED_FACE ( 'NONE', ( #6353, #1370, #48974 ), #65453, .F. ) ;
#21726=CARTESIAN_POINT ( 'NONE',  ( 8.750000000000001776, 25.24999999999998934, 3.750000000000000000 ) ) ;
#21733=DIRECTION ( 'NONE',  ( -0.000000000000000000, 1.000000000000000000, -0.000000000000000000 ) ) ;
#21735=AXIS2_PLACEMENT_3D ( 'NONE', #43952, #21408, #43284 ) ;
#21752=CYLINDRICAL_SURFACE ( 'NONE', #8948, 0.2500000000000002220 ) ;
#21764=CARTESIAN_POINT ( 'NONE',  ( -13.75000000000000533, 30.99999999999999289, -3.750000000000000000 ) ) ;
#21801=DIRECTION ( 'NONE',  ( 0.000000000000000000, -1.000000000000000000, 0.000000000000000000 ) ) ;
#21812=ORIENTED_EDGE ( 'NONE', *, *, #62970, .T. ) ;
#21814=DIRECTION ( 'NONE',  ( 0.000000000000000000, 1.000000000000000000, 0.000000000000000000 ) ) ;
#21818=ORIENTED_EDGE ( 'NONE', *, *, #59335, .F. ) ;
#21831=CARTESIAN_POINT ( 'NONE',  ( -15.00000000000000000, 8.000000000000000000, 3.500000000000003997 ) ) ;
#21839=LINE ( 'NONE', #654, #6951 ) ;
#21855=CYLINDRICAL_SURFACE ( 'NONE', #48339, 0.2500000000000002220 ) ;
#21859=CARTESIAN_POINT ( 'NONE',  ( 25.00000000000000000, 1.000000000000000888, 4.000000000000000000 ) ) ;
#21864=EDGE_LOOP ( 'NONE', ( #64995, #56970, #18391, #52104 ) ) ;
#21882=EDGE_CURVE ( 'NONE', #44845, #51757, #3455, .T. ) ;
#21926=EDGE_CURVE ( 'NONE', #26708, #6652, #30564, .T. ) ;
#21952=ORIENTED_EDGE ( 'NONE', *, *, #69037, .F. ) ;
#21957=FACE_OUTER_BOUND ( 'NONE', #58544, .T. ) ;
#21973=ADVANCED_FACE ( 'NONE', ( #15816 ), #3508, .T. ) ;
#21975=ORIENTED_EDGE ( 'NONE', *, *, #30713, .T. ) ;
#21979=ORIENTED_EDGE ( 'NONE', *, *, #9655, .F. ) ;
#21996=CARTESIAN_POINT ( 'NONE',  ( -22.25000000000000711, 34.24999999999999289, 4.000000000000000000 ) ) ;
#21997=ORIENTED_EDGE ( 'NONE', *, *, #66217, .F. ) ;
#22009=EDGE_CURVE ( 'NONE', #22236, #38885, #32777, .T. ) ;
#22025=CYLINDRICAL_SURFACE ( 'NONE', #59679, 0.2500000000000002220 ) ;
#22026=ORIENTED_EDGE ( 'NONE', *, *, #40286, .F. ) ;
#22038=DIRECTION ( 'NONE',  ( 0.000000000000000000, 1.000000000000000000, 0.000000000000000000 ) ) ;
#22063=DIRECTION ( 'NONE',  ( -1.000000000000000000, 0.000000000000000000, 0.000000000000000000 ) ) ;
#22072=ORIENTED_EDGE ( 'NONE', *, *, #68305, .F. ) ;
#22082=CYLINDRICAL_SURFACE ( 'NONE', #13375, 0.2500000000000002220 ) ;
#22092=ADVANCED_FACE ( 'NONE', ( #22453 ), #28035, .T. ) ;
#22148=FACE_OUTER_BOUND ( 'NONE', #56676, .T. ) ;
#22163=DIRECTION ( 'NONE',  ( 0.000000000000000000, 0.000000000000000000, 1.000000000000000000 ) ) ;
#22179=CARTESIAN_POINT ( 'NONE',  ( -13.75000000000000355, 28.24999999999998934, -4.000000000000000000 ) ) ;
#22236=VERTEX_POINT ( 'NONE', #61444 ) ;
#22279=CARTESIAN_POINT ( 'NONE',  ( -24.00000000000000355, 37.00000000000000000, -3.750000000000000000 ) ) ;
#22291=DIRECTION ( 'NONE',  ( 1.000000000000000000, 0.000000000000000000, 0.000000000000000000 ) ) ;
#22318=CARTESIAN_POINT ( 'NONE',  ( 25.00000000000000355, 37.00000000000000000, 3.000000000000000000 ) ) ;
#22324=EDGE_CURVE ( 'NONE', #38885, #51977, #37352, .T. ) ;
#22332=EDGE_CURVE ( 'NONE', #44124, #64274, #60340, .T. ) ;
#22338=DIRECTION ( 'NONE',  ( -1.000000000000000000, 0.000000000000000000, 0.000000000000000000 ) ) ;
#22341=CIRCLE ( 'NONE', #56015, 0.2500000000000002220 ) ;
#22343=EDGE_LOOP ( 'NONE', ( #38952, #62932, #50963, #61416 ) ) ;
#22367=ORIENTED_EDGE ( 'NONE', *, *, #52052, .T. ) ;
#22376=ORIENTED_EDGE ( 'NONE', *, *, #4516, .T. ) ;
#22386=DIRECTION ( 'NONE',  ( 0.000000000000000000, -1.000000000000000000, 0.000000000000000000 ) ) ;
#22392=ADVANCED_FACE ( 'NONE', ( #50166 ), #67362, .F. ) ;
#22394=EDGE_LOOP ( 'NONE', ( #50159, #63103, #17889, #64226 ) ) ;
#22414=CARTESIAN_POINT ( 'NONE',  ( -9.250000000000003553, 27.74999999999998934, -4.000000000000000000 ) ) ;
#22447=ORIENTED_EDGE ( 'NONE', *, *, #43278, .F. ) ;
#22453=FACE_OUTER_BOUND ( 'NONE', #61797, .T. ) ;
#22456=CYLINDRICAL_SURFACE ( 'NONE', #21735, 0.2500000000000002220 ) ;
#22478=DIRECTION ( 'NONE',  ( 0.000000000000000000, 0.000000000000000000, 1.000000000000000000 ) ) ;
#22496=CARTESIAN_POINT ( 'NONE',  ( 18.25000000000000711, 33.99999999999999289, -3.750000000000000000 ) ) ;
#22526=CARTESIAN_POINT ( 'NONE',  ( 13.75000000000000533, 30.99999999999999289, 4.000000000000000000 ) ) ;
#22535=DIRECTION ( 'NONE',  ( 0.000000000000000000, 0.000000000000000000, 1.000000000000000000 ) ) ;
#22541=AXIS2_PLACEMENT_3D ( 'NONE', #18723, #34546, #7478 ) ;
#22548=ORIENTED_EDGE ( 'NONE', *, *, #4253, .F. ) ;
#22551=DIRECTION ( 'NONE',  ( 0.000000000000000000, 0.000000000000000000, 1.000000000000000000 ) ) ;
#22552=EDGE_LOOP ( 'NONE', ( #41016, #8815, #36994, #66327 ) ) ;
#22566=ORIENTED_EDGE ( 'NONE', *, *, #22717, .T. ) ;
#22578=EDGE_CURVE ( 'NONE', #51757, #37913, #32882, .T. ) ;
#22590=CARTESIAN_POINT ( 'NONE',  ( 13.75000000000000533, 30.74999999999999289, -3.750000000000000000 ) ) ;
#22618=DIRECTION ( 'NONE',  ( 0.000000000000000000, 0.000000000000000000, 1.000000000000000000 ) ) ;
#22639=CIRCLE ( 'NONE', #52975, 0.5000000000000004441 ) ;
#22650=CIRCLE ( 'NONE', #61955, 1.000000000000000000 ) ;
#22666=LINE ( 'NONE', #32876, #21301 ) ;
#22679=CIRCLE ( 'NONE', #61974, 0.2500000000000002220 ) ;
#22711=CIRCLE ( 'NONE', #44103, 0.5000000000000004441 ) ;
#22713=DIRECTION ( 'NONE',  ( -0.000000000000000000, -0.000000000000000000, 1.000000000000000000 ) ) ;
#22717=EDGE_CURVE ( 'NONE', #43113, #50288, #44749, .T. ) ;
#22738=DIRECTION ( 'NONE',  ( 0.000000000000000000, 0.000000000000000000, -1.000000000000000000 ) ) ;
#22778=ADVANCED_FACE ( 'NONE', ( #67543 ), #19342, .T. ) ;
#22788=AXIS2_PLACEMENT_3D ( 'NONE', #28402, #49560, #1290 ) ;
#22798=EDGE_CURVE ( 'NONE', #58151, #62845, #34831, .T. ) ;
#22799=FACE_OUTER_BOUND ( 'NONE', #18789, .T. ) ;
#22818=DIRECTION ( 'NONE',  ( -1.000000000000000000, 0.000000000000000000, 0.000000000000000000 ) ) ;
#22822=ORIENTED_EDGE ( 'NONE', *, *, #8077, .T. ) ;
#22840=DIRECTION ( 'NONE',  ( 0.000000000000000000, 1.000000000000000000, 0.000000000000000000 ) ) ;
#22851=CYLINDRICAL_SURFACE ( 'NONE', #50888, 0.2500000000000002220 ) ;
#22858=CIRCLE ( 'NONE', #27270, 0.2500000000000002220 ) ;
#22886=ORIENTED_EDGE ( 'NONE', *, *, #11612, .T. ) ;
#22906=AXIS2_PLACEMENT_3D ( 'NONE', #14416, #68253, #36634 ) ;
#22932=ORIENTED_EDGE ( 'NONE', *, *, #12151, .F. ) ;
#22979=EDGE_CURVE ( 'NONE', #59464, #44845, #11573, .T. ) ;
#23019=AXIS2_PLACEMENT_3D ( 'NONE', #64028, #43337, #53813 ) ;
#23046=ORIENTED_EDGE ( 'NONE', *, *, #41098, .T. ) ;
#23051=AXIS2_PLACEMENT_3D ( 'NONE', #29793, #56158, #55480 ) ;
#23054=EDGE_CURVE ( 'NONE', #50331, #6652, #19410, .T. ) ;
#23082=VECTOR ( 'NONE', #25397, 1000.000000000000000 ) ;
#23086=DIRECTION ( 'NONE',  ( 0.000000000000000000, 0.000000000000000000, -1.000000000000000000 ) ) ;
#23101=ORIENTED_EDGE ( 'NONE', *, *, #38244, .F. ) ;
#23117=DIRECTION ( 'NONE',  ( -1.000000000000000000, 0.000000000000000000, 0.000000000000000000 ) ) ;
#23122=EDGE_LOOP ( 'NONE', ( #63547, #31960, #62009, #26553 ) ) ;
#23152=VERTEX_POINT ( 'NONE', #30140 ) ;
#23159=ORIENTED_EDGE ( 'NONE', *, *, #18068, .T. ) ;
#23165=ORIENTED_EDGE ( 'NONE', *, *, #59959, .F. ) ;
#23180=LINE ( 'NONE', #6291, #1905 ) ;
#23191=LINE ( 'NONE', #34423, #7240 ) ;
#23202=EDGE_CURVE ( 'NONE', #36655, #8380, #36540, .T. ) ;
#23212=EDGE_CURVE ( 'NONE', #41176, #67128, #4095, .T. ) ;
#23228=EDGE_LOOP ( 'NONE', ( #6456, #44079, #17295, #49637 ) ) ;
#23238=CARTESIAN_POINT ( 'NONE',  ( -18.25000000000000711, 33.74999999999999289, -4.000000000000000000 ) ) ;
#23247=DIRECTION ( 'NONE',  ( -1.000000000000000000, 0.000000000000000000, 0.000000000000000000 ) ) ;
#23263=CARTESIAN_POINT ( 'NONE',  ( -4.500000000000002665, 24.74999999999998579, 3.750000000000000000 ) ) ;
#23270=DIRECTION ( 'NONE',  ( 1.000000000000000000, 9.376883653928660246E-17, 0.000000000000000000 ) ) ;
#23280=CARTESIAN_POINT ( 'NONE',  ( -11.00000000000000000, 8.000000000000000000, 3.500000000000003997 ) ) ;
#23288=CARTESIAN_POINT ( 'NONE',  ( 8.750000000000001776, 25.24999999999998934, -4.000000000000000000 ) ) ;
#23296=CARTESIAN_POINT ( 'NONE',  ( -15.00000000000000000, 8.000000000000000000, 3.500000000000003997 ) ) ;
#23297=FACE_OUTER_BOUND ( 'NONE', #65079, .T. ) ;
#23308=ORIENTED_EDGE ( 'NONE', *, *, #13481, .T. ) ;
#23329=DIRECTION ( 'NONE',  ( 0.000000000000000000, -1.000000000000000000, 0.000000000000000000 ) ) ;
#23333=EDGE_CURVE ( 'NONE', #46369, #16845, #29387, .T. ) ;
#23361=EDGE_LOOP ( 'NONE', ( #14904, #4025, #35360 ) ) ;
#23367=ADVANCED_FACE ( 'NONE', ( #60688 ), #37922, .T. ) ;
#23394=ORIENTED_EDGE ( 'NONE', *, *, #61417, .T. ) ;
#23399=DIRECTION ( 'NONE',  ( 0.000000000000000000, 0.000000000000000000, -1.000000000000000000 ) ) ;
#23407=CARTESIAN_POINT ( 'NONE',  ( 13.75000000000000533, 30.74999999999999289, 3.750000000000000000 ) ) ;
#23410=EDGE_CURVE ( 'NONE', #48589, #39136, #67617, .T. ) ;
#23433=DIRECTION ( 'NONE',  ( 0.000000000000000000, 0.000000000000000000, 1.000000000000000000 ) ) ;
#23463=VECTOR ( 'NONE', #21733, 1000.000000000000000 ) ;
#23468=AXIS2_PLACEMENT_3D ( 'NONE', #12987, #34444, #24560 ) ;
#23491=ADVANCED_FACE ( 'NONE', ( #51208 ), #34652, .T. ) ;
#23496=EDGE_LOOP ( 'NONE', ( #573, #56570, #68987, #66615 ) ) ;
#23515=EDGE_CURVE ( 'NONE', #58700, #10966, #13739, .T. ) ;
#23517=FACE_OUTER_BOUND ( 'NONE', #50578, .T. ) ;
#23521=AXIS2_PLACEMENT_3D ( 'NONE', #14206, #40971, #3597 ) ;
#23527=CARTESIAN_POINT ( 'NONE',  ( -17.75000000000000711, 30.74999999999999289, 3.750000000000000000 ) ) ;
#23550=AXIS2_PLACEMENT_3D ( 'NONE', #5041, #65159, #38494 ) ;
#23570=LINE ( 'NONE', #45084, #11668 ) ;
#23580=FACE_OUTER_BOUND ( 'NONE', #1929, .T. ) ;
#23594=DIRECTION ( 'NONE',  ( 0.000000000000000000, -0.000000000000000000, -1.000000000000000000 ) ) ;
#23605=DIRECTION ( 'NONE',  ( 1.000000000000000000, -0.000000000000000000, -0.000000000000000000 ) ) ;
#23626=DIRECTION ( 'NONE',  ( 1.000000000000000000, 0.000000000000000000, 0.000000000000000000 ) ) ;
#23644=CARTESIAN_POINT ( 'NONE',  ( 24.00000000000000000, 0.000000000000000000, -4.000000000000000000 ) ) ;
#23649=EDGE_CURVE ( 'NONE', #67128, #23842, #30591, .T. ) ;
#23659=EDGE_CURVE ( 'NONE', #5753, #69477, #40728, .T. ) ;
#23663=DIRECTION ( 'NONE',  ( 0.000000000000000000, 1.000000000000000000, 0.000000000000000000 ) ) ;
#23665=ORIENTED_EDGE ( 'NONE', *, *, #68140, .F. ) ;
#23668=DIRECTION ( 'NONE',  ( 0.000000000000000000, 0.000000000000000000, 1.000000000000000000 ) ) ;
#23688=AXIS2_PLACEMENT_3D ( 'NONE', #60746, #11888, #44300 ) ;
#23755=CARTESIAN_POINT ( 'NONE',  ( -8.750000000000001776, 24.74999999999998579, -4.000000000000000000 ) ) ;
#23775=AXIS2_PLACEMENT_3D ( 'NONE', #65708, #27005, #66041 ) ;
#23788=FACE_OUTER_BOUND ( 'NONE', #26016, .T. ) ;
#23799=CIRCLE ( 'NONE', #36184, 0.2500000000000002220 ) ;
#23808=CARTESIAN_POINT ( 'NONE',  ( 24.75000000000000355, 37.00000000000000000, 3.000000000000000000 ) ) ;
#23842=VERTEX_POINT ( 'NONE', #9266 ) ;
#23850=FACE_OUTER_BOUND ( 'NONE', #12786, .T. ) ;
#23854=CARTESIAN_POINT ( 'NONE',  ( 17.75000000000000711, 31.24999999999999289, 4.000000000000000000 ) ) ;
#23921=CARTESIAN_POINT ( 'NONE',  ( -17.75000000000000711, 30.74999999999999289, -4.000000000000000000 ) ) ;
#23924=VERTEX_POINT ( 'NONE', #9621 ) ;
#23930=DIRECTION ( 'NONE',  ( -1.000000000000000000, 0.000000000000000000, 0.000000000000000000 ) ) ;
#23931=AXIS2_PLACEMENT_3D ( 'NONE', #9541, #69629, #68267 ) ;
#23934=AXIS2_PLACEMENT_3D ( 'NONE', #36641, #42952, #42595 ) ;
#23950=EDGE_LOOP ( 'NONE', ( #67355, #21685, #58341, #20846 ) ) ;
#23963=EDGE_LOOP ( 'NONE', ( #33678, #19453, #6509, #42426 ) ) ;
#23985=FACE_OUTER_BOUND ( 'NONE', #11130, .T. ) ;
#24031=VERTEX_POINT ( 'NONE', #22179 ) ;
#24039=CARTESIAN_POINT ( 'NONE',  ( 15.00000000000000000, 8.000000000000000000, -4.000000000000000000 ) ) ;
#24047=ORIENTED_EDGE ( 'NONE', *, *, #2940, .F. ) ;
#24064=EDGE_CURVE ( 'NONE', #15837, #64993, #50302, .T. ) ;
#24104=AXIS2_PLACEMENT_3D ( 'NONE', #53707, #59676, #15764 ) ;
#24107=CARTESIAN_POINT ( 'NONE',  ( -24.00000000000000000, 1.000000000000000000, 3.000000000000000000 ) ) ;
#24112=DIRECTION ( 'NONE',  ( 0.000000000000000000, 0.000000000000000000, 1.000000000000000000 ) ) ;
#24142=EDGE_CURVE ( 'NONE', #25552, #30753, #13664, .T. ) ;
#24153=DIRECTION ( 'NONE',  ( 0.000000000000000000, 0.000000000000000000, 1.000000000000000000 ) ) ;
#24164=CARTESIAN_POINT ( 'NONE',  ( 0.000000000000000000, 30.74999999999999289, 4.000000000000000000 ) ) ;
#24175=LINE ( 'NONE', #21859, #23 ) ;
#24183=ORIENTED_EDGE ( 'NONE', *, *, #29777, .F. ) ;
#24215=EDGE_LOOP ( 'NONE', ( #31893, #27200, #68750 ) ) ;
#24233=EDGE_CURVE ( 'NONE', #5366, #54390, #25845, .T. ) ;
#24260=AXIS2_PLACEMENT_3D ( 'NONE', #44611, #13576, #35045 ) ;
#24265=CARTESIAN_POINT ( 'NONE',  ( -22.75000000000000711, 36.75000000000000000, 3.750000000000000000 ) ) ;
#24272=ORIENTED_EDGE ( 'NONE', *, *, #23649, .F. ) ;
#24294=SPHERICAL_SURFACE ( 'NONE', #38190, 0.2500000000000000000 ) ;
#24307=EDGE_CURVE ( 'NONE', #40140, #7265, #39568, .T. ) ;
#24363=EDGE_CURVE ( 'NONE', #39136, #25552, #32867, .T. ) ;
#24386=FACE_BOUND ( 'NONE', #39316, .T. ) ;
#24392=CARTESIAN_POINT ( 'NONE',  ( 24.00000000000000355, 36.75000000000000000, 3.000000000000000000 ) ) ;
#24405=CARTESIAN_POINT ( 'NONE',  ( -19.00000000000000000, 8.000000000000000000, 3.500000000000003997 ) ) ;
#24413=DIRECTION ( 'NONE',  ( 0.000000000000000000, 0.000000000000000000, 1.000000000000000000 ) ) ;
#24416=DIRECTION ( 'NONE',  ( 0.000000000000000000, 1.000000000000000000, 0.000000000000000000 ) ) ;
#24424=CARTESIAN_POINT ( 'NONE',  ( -18.00000000000000711, 33.74999999999999289, -3.750000000000000000 ) ) ;
#24435=EDGE_CURVE ( 'NONE', #58978, #9509, #13469, .T. ) ;
#24437=EDGE_CURVE ( 'NONE', #21392, #30006, #66609, .T. ) ;
#24447=DIRECTION ( 'NONE',  ( 0.000000000000000000, 0.000000000000000000, -1.000000000000000000 ) ) ;
#24455=ORIENTED_EDGE ( 'NONE', *, *, #3191, .F. ) ;
#24464=CYLINDRICAL_SURFACE ( 'NONE', #11114, 0.2500000000000002220 ) ;
#24498=DIRECTION ( 'NONE',  ( 1.000000000000000000, -0.000000000000000000, 0.000000000000000000 ) ) ;
#24533=FACE_OUTER_BOUND ( 'NONE', #51903, .T. ) ;
#24560=DIRECTION ( 'NONE',  ( -1.000000000000000000, 9.376883653928660246E-17, 0.000000000000000000 ) ) ;
#24620=CARTESIAN_POINT ( 'NONE',  ( -22.75000000000000711, 37.00000000000000000, -3.750000000000000000 ) ) ;
#24637=DIRECTION ( 'NONE',  ( 1.000000000000000000, -0.000000000000000000, 0.000000000000000000 ) ) ;
#24640=ORIENTED_EDGE ( 'NONE', *, *, #10096, .T. ) ;
#24649=CARTESIAN_POINT ( 'NONE',  ( 9.000000000000003553, 27.74999999999998934, -3.750000000000000000 ) ) ;
#24697=ORIENTED_EDGE ( 'NONE', *, *, #34232, .T. ) ;
#24718=FACE_OUTER_BOUND ( 'NONE', #66360, .T. ) ;
#24740=AXIS2_PLACEMENT_3D ( 'NONE', #9495, #30916, #40820 ) ;
#24752=DIRECTION ( 'NONE',  ( -0.000000000000000000, -0.000000000000000000, -1.000000000000000000 ) ) ;
#24794=DIRECTION ( 'NONE',  ( 1.000000000000000000, -0.000000000000000000, 0.000000000000000000 ) ) ;
#24815=ORIENTED_EDGE ( 'NONE', *, *, #61376, .T. ) ;
#24836=DIRECTION ( 'NONE',  ( 0.000000000000000000, 1.000000000000000000, 0.000000000000000000 ) ) ;
#24878=APPLICATION_CONTEXT ( 'automotive_design' ) ;
#24885=CIRCLE ( 'NONE', #56325, 0.2500000000000002220 ) ;
#24897=EDGE_CURVE ( 'NONE', #1324, #1454, #36312, .T. ) ;
#24904=ORIENTED_EDGE ( 'NONE', *, *, #56333, .T. ) ;
#24917=CARTESIAN_POINT ( 'NONE',  ( 9.000000000000003553, 24.99999999999998579, 3.750000000000000000 ) ) ;
#24957=PLANE ( 'NONE',  #50989 ) ;
#24970=DIRECTION ( 'NONE',  ( 0.000000000000000000, 0.000000000000000000, 1.000000000000000000 ) ) ;
#24974=DIRECTION ( 'NONE',  ( 0.000000000000000000, 1.000000000000000000, -0.000000000000000000 ) ) ;
#25038=EDGE_CURVE ( 'NONE', #54990, #39699, #19266, .T. ) ;
#25043=FACE_OUTER_BOUND ( 'NONE', #31987, .T. ) ;
#25072=FACE_OUTER_BOUND ( 'NONE', #12668, .T. ) ;
#25078=VECTOR ( 'NONE', #48036, 1000.000000000000000 ) ;
#25104=LINE ( 'NONE', #62714, #66183 ) ;
#25128=CARTESIAN_POINT ( 'NONE',  ( 22.75000000000000711, 36.75000000000000000, 3.750000000000000000 ) ) ;
#25192=ORIENTED_EDGE ( 'NONE', *, *, #64981, .T. ) ;
#25193=TOROIDAL_SURFACE ( 'NONE', #61088, 0.5000000000000000000, 0.2500000000000000000 ) ;
#25208=DIRECTION ( 'NONE',  ( 0.000000000000000000, 1.000000000000000000, 0.000000000000000000 ) ) ;
#25226=LINE ( 'NONE', #41097, #14034 ) ;
#25240=ORIENTED_EDGE ( 'NONE', *, *, #21203, .T. ) ;
#25251=CARTESIAN_POINT ( 'NONE',  ( 4.500000000000002665, 24.74999999999998579, 4.000000000000000000 ) ) ;
#25256=TOROIDAL_SURFACE ( 'NONE', #15213, 0.5000000000000000000, 0.2500000000000000000 ) ;
#25259=DIRECTION ( 'NONE',  ( 1.000000000000000000, -0.000000000000000000, 0.000000000000000000 ) ) ;
#25277=CARTESIAN_POINT ( 'NONE',  ( 9.250000000000003553, 25.24999999999998934, 3.750000000000000000 ) ) ;
#25300=ORIENTED_EDGE ( 'NONE', *, *, #54561, .F. ) ;
#25303=ADVANCED_FACE ( 'NONE', ( #3763 ), #57621, .T. ) ;
#25321=DIRECTION ( 'NONE',  ( 1.000000000000000000, 0.000000000000000000, 0.000000000000000000 ) ) ;
#25326=FACE_OUTER_BOUND ( 'NONE', #67988, .T. ) ;
#25328=ORIENTED_EDGE ( 'NONE', *, *, #65117, .T. ) ;
#25345=CIRCLE ( 'NONE', #6207, 0.2500000000000002220 ) ;
#25397=DIRECTION ( 'NONE',  ( -1.000000000000000000, 0.000000000000000000, 0.000000000000000000 ) ) ;
#25404=EDGE_CURVE ( 'NONE', #5753, #35195, #43812, .T. ) ;
#25453=EDGE_CURVE ( 'NONE', #8679, #1837, #22711, .T. ) ;
#25492=DIRECTION ( 'NONE',  ( 0.000000000000000000, -1.000000000000000000, 0.000000000000000000 ) ) ;
#25498=ORIENTED_EDGE ( 'NONE', *, *, #23659, .F. ) ;
#25516=ORIENTED_EDGE ( 'NONE', *, *, #49556, .F. ) ;
#25548=EDGE_CURVE ( 'NONE', #52546, #61196, #40963, .T. ) ;
#25552=VERTEX_POINT ( 'NONE', #40249 ) ;
#25618=DIRECTION ( 'NONE',  ( 1.000000000000000000, 0.000000000000000000, -0.000000000000000000 ) ) ;
#25638=CIRCLE ( 'NONE', #63810, 4.499999999999976019 ) ;
#25675=CARTESIAN_POINT ( 'NONE',  ( -22.75000000000000711, 36.75000000000000000, -3.750000000000000000 ) ) ;
#25683=VECTOR ( 'NONE', #18361, 1000.000000000000000 ) ;
#25727=FACE_OUTER_BOUND ( 'NONE', #14506, .T. ) ;
#25766=ORIENTED_EDGE ( 'NONE', *, *, #52543, .T. ) ;
#25840=CARTESIAN_POINT ( 'NONE',  ( 24.75000000000000355, 36.75000000000000000, 3.000000000000000000 ) ) ;
#25843=AXIS2_PLACEMENT_3D ( 'NONE', #47247, #64058, #16267 ) ;
#25845=LINE ( 'NONE', #30405, #31643 ) ;
#25857=CIRCLE ( 'NONE', #15796, 0.2500000000000002220 ) ;
#25893=CARTESIAN_POINT ( 'NONE',  ( -4.500000000000002665, 24.74999999999998579, -3.750000000000000000 ) ) ;
#25902=CYLINDRICAL_SURFACE ( 'NONE', #63000, 0.2500000000000002220 ) ;
#25906=CYLINDRICAL_SURFACE ( 'NONE', #3966, 0.2500000000000002220 ) ;
#25912=DIRECTION ( 'NONE',  ( 5.782411586589351722E-16, -1.000000000000000000, -0.000000000000000000 ) ) ;
#25933=AXIS2_PLACEMENT_3D ( 'NONE', #36446, #14246, #20201 ) ;
#25987=DIRECTION ( 'NONE',  ( -1.000000000000000000, 0.000000000000000000, 0.000000000000000000 ) ) ;
#25990=DIRECTION ( 'NONE',  ( 0.000000000000000000, -1.000000000000000000, 0.000000000000000000 ) ) ;
#26016=EDGE_LOOP ( 'NONE', ( #69553, #14322, #60175, #19903 ) ) ;
#26035=ORIENTED_EDGE ( 'NONE', *, *, #54561, .T. ) ;
#26036=DIRECTION ( 'NONE',  ( 0.000000000000000000, 0.000000000000000000, -1.000000000000000000 ) ) ;
#26038=AXIS2_PLACEMENT_3D ( 'NONE', #52663, #15729, #43536 ) ;
#26044=CIRCLE ( 'NONE', #65363, 0.2500000000000002220 ) ;
#26048=CIRCLE ( 'NONE', #22541, 0.2500000000000002220 ) ;
#26056=EDGE_CURVE ( 'NONE', #52256, #27282, #58764, .T. ) ;
#26073=AXIS2_PLACEMENT_3D ( 'NONE', #65068, #17284, #38750 ) ;
#26091=ORIENTED_EDGE ( 'NONE', *, *, #17862, .T. ) ;
#26149=LINE ( 'NONE', #47685, #14693 ) ;
#26157=VECTOR ( 'NONE', #5269, 1000.000000000000000 ) ;
#26185=DIRECTION ( 'NONE',  ( -1.000000000000000000, 0.000000000000000000, 0.000000000000000000 ) ) ;
#26199=EDGE_CURVE ( 'NONE', #61564, #46540, #54505, .T. ) ;
#26202=DIRECTION ( 'NONE',  ( -1.000000000000000000, 0.000000000000000000, 0.000000000000000000 ) ) ;
#26209=AXIS2_PLACEMENT_3D ( 'NONE', #47777, #36848, #42832 ) ;
#26218=FACE_OUTER_BOUND ( 'NONE', #69193, .T. ) ;
#26246=AXIS2_PLACEMENT_3D ( 'NONE', #67815, #51993, #41447 ) ;
#26260=CIRCLE ( 'NONE', #7203, 0.5000000000000000000 ) ;
#26272=ORIENTED_EDGE ( 'NONE', *, *, #57166, .T. ) ;
#26291=CARTESIAN_POINT ( 'NONE',  ( -22.75000000000000711, 36.75000000000000000, 3.750000000000000000 ) ) ;
#26301=ORIENTED_EDGE ( 'NONE', *, *, #31340, .T. ) ;
#26352=CIRCLE ( 'NONE', #67908, 0.2500000000000002220 ) ;
#26353=PLANE ( 'NONE',  #42351 ) ;
#26362=AXIS2_PLACEMENT_3D ( 'NONE', #20069, #5274, #22163 ) ;
#26370=CARTESIAN_POINT ( 'NONE',  ( 13.75000000000000355, 28.24999999999998934, 3.750000000000000000 ) ) ;
#26406=AXIS2_PLACEMENT_3D ( 'NONE', #5198, #26978, #5889 ) ;
#26419=CIRCLE ( 'NONE', #15276, 0.2500000000000002220 ) ;
#26445=ORIENTED_EDGE ( 'NONE', *, *, #64751, .T. ) ;
#26471=ORIENTED_EDGE ( 'NONE', *, *, #52052, .F. ) ;
#26518=EDGE_CURVE ( 'NONE', #31530, #2782, #5513, .T. ) ;
#26533=CARTESIAN_POINT ( 'NONE',  ( -13.75000000000000355, 28.24999999999998934, 3.750000000000000000 ) ) ;
#26553=ORIENTED_EDGE ( 'NONE', *, *, #53078, .F. ) ;
#26575=CARTESIAN_POINT ( 'NONE',  ( -13.25000000000000355, 27.99999999999998934, -3.750000000000000000 ) ) ;
#26587=DIRECTION ( 'NONE',  ( 0.000000000000000000, 0.000000000000000000, -1.000000000000000000 ) ) ;
#26606=EDGE_CURVE ( 'NONE', #17311, #60451, #44239, .T. ) ;
#26607=ORIENTED_EDGE ( 'NONE', *, *, #68287, .F. ) ;
#26638=DIRECTION ( 'NONE',  ( 1.000000000000000000, -0.000000000000000000, 0.000000000000000000 ) ) ;
#26668=EDGE_CURVE ( 'NONE', #23152, #1324, #39318, .T. ) ;
#26699=LINE ( 'NONE', #30600, #38599 ) ;
#26708=VERTEX_POINT ( 'NONE', #61081 ) ;
#26711=DIRECTION ( 'NONE',  ( 0.000000000000000000, 0.000000000000000000, 1.000000000000000000 ) ) ;
#26716=CYLINDRICAL_SURFACE ( 'NONE', #5635, 0.2500000000000002220 ) ;
#26733=EDGE_CURVE ( 'NONE', #529, #20746, #6927, .T. ) ;
#26765=CIRCLE ( 'NONE', #41429, 0.5000000000000004441 ) ;
#26798=TOROIDAL_SURFACE ( 'NONE', #27947, 0.5000000000000000000, 0.2500000000000000000 ) ;
#26809=ADVANCED_FACE ( 'NONE', ( #60381 ), #53254, .T. ) ;
#26834=ORIENTED_EDGE ( 'NONE', *, *, #12485, .T. ) ;
#26857=CARTESIAN_POINT ( 'NONE',  ( -4.250000000000001776, 21.74999999999998579, -4.000000000000000000 ) ) ;
#26864=CARTESIAN_POINT ( 'NONE',  ( -24.75000000000000355, 37.00000000000000000, 3.000000000000000000 ) ) ;
#26868=CIRCLE ( 'NONE', #63952, 0.2500000000000002220 ) ;
#26876=DIRECTION ( 'NONE',  ( 0.000000000000000000, 0.000000000000000000, -1.000000000000000000 ) ) ;
#26891=CARTESIAN_POINT ( 'NONE',  ( -22.75000000000000711, 36.75000000000000000, 3.750000000000000000 ) ) ;
#26899=AXIS2_PLACEMENT_3D ( 'NONE', #63673, #42288, #46870 ) ;
#26904=EDGE_CURVE ( 'NONE', #31124, #5413, #10564, .T. ) ;
#26966=VECTOR ( 'NONE', #9137, 1000.000000000000000 ) ;
#26978=DIRECTION ( 'NONE',  ( 0.000000000000000000, 0.000000000000000000, 1.000000000000000000 ) ) ;
#26999=DIRECTION ( 'NONE',  ( 0.000000000000000000, 1.000000000000000000, -0.000000000000000000 ) ) ;
#27005=DIRECTION ( 'NONE',  ( 1.000000000000000000, 0.000000000000000000, 0.000000000000000000 ) ) ;
#27043=AXIS2_PLACEMENT_3D ( 'NONE', #11451, #12479, #44209 ) ;
#27051=EDGE_CURVE ( 'NONE', #1324, #56729, #17362, .T. ) ;
#27065=EDGE_CURVE ( 'NONE', #68529, #57180, #7239, .T. ) ;
#27071=ADVANCED_FACE ( 'NONE', ( #66639 ), #9521, .T. ) ;
#27094=DIRECTION ( 'NONE',  ( 0.000000000000000000, 1.000000000000000000, 0.000000000000000000 ) ) ;
#27101=ORIENTED_EDGE ( 'NONE', *, *, #52902, .F. ) ;
#27104=ORIENTED_EDGE ( 'NONE', *, *, #31768, .T. ) ;
#27117=ORIENTED_EDGE ( 'NONE', *, *, #58444, .F. ) ;
#27126=ORIENTED_EDGE ( 'NONE', *, *, #5792, .F. ) ;
#27164=AXIS2_PLACEMENT_3D ( 'NONE', #17886, #56187, #3739 ) ;
#27176=SPHERICAL_SURFACE ( 'NONE', #32619, 0.2500000000000000000 ) ;
#27179=ORIENTED_EDGE ( 'NONE', *, *, #19415, .T. ) ;
#27187=EDGE_LOOP ( 'NONE', ( #24815, #45015, #3754 ) ) ;
#27193=ORIENTED_EDGE ( 'NONE', *, *, #17603, .T. ) ;
#27195=CARTESIAN_POINT ( 'NONE',  ( 8.750000000000001776, 25.24999999999998934, -3.750000000000000000 ) ) ;
#27200=ORIENTED_EDGE ( 'NONE', *, *, #53544, .F. ) ;
#27214=ORIENTED_EDGE ( 'NONE', *, *, #791, .F. ) ;
#27215=DIRECTION ( 'NONE',  ( -9.376883653928687363E-17, -1.000000000000000000, -0.000000000000000000 ) ) ;
#27217=DIRECTION ( 'NONE',  ( 1.000000000000000000, -5.782411586589351722E-16, 0.000000000000000000 ) ) ;
#27270=AXIS2_PLACEMENT_3D ( 'NONE', #686, #6033, #64440 ) ;
#27282=VERTEX_POINT ( 'NONE', #50807 ) ;
#27314=ORIENTED_EDGE ( 'NONE', *, *, #54905, .F. ) ;
#27334=AXIS2_PLACEMENT_3D ( 'NONE', #48560, #42267, #64703 ) ;
#27387=CARTESIAN_POINT ( 'NONE',  ( -25.00000000000000355, 36.75000000000000000, -3.750000000000000000 ) ) ;
#27396=DIRECTION ( 'NONE',  ( 0.000000000000000000, 0.000000000000000000, -1.000000000000000000 ) ) ;
#27400=SPHERICAL_SURFACE ( 'NONE', #67713, 1.000000000000000000 ) ;
#27430=CYLINDRICAL_SURFACE ( 'NONE', #57299, 0.2500000000000002220 ) ;
#27441=FACE_OUTER_BOUND ( 'NONE', #37835, .T. ) ;
#27499=CARTESIAN_POINT ( 'NONE',  ( 13.50000000000000355, 28.24999999999998934, -3.750000000000000000 ) ) ;
#27553=PLANE ( 'NONE',  #29965 ) ;
#27572=EDGE_CURVE ( 'NONE', #42065, #20640, #46657, .T. ) ;
#27613=CARTESIAN_POINT ( 'NONE',  ( 15.00000000000000000, 8.000000000000000000, 3.500000000000003997 ) ) ;
#27630=CARTESIAN_POINT ( 'NONE',  ( 10.50000000000002309, 8.000000000000000000, -4.000000000000000000 ) ) ;
#27640=CARTESIAN_POINT ( 'NONE',  ( 22.75000000000000711, 36.75000000000000000, 3.750000000000000000 ) ) ;
#27643=FACE_OUTER_BOUND ( 'NONE', #48303, .T. ) ;
#27657=DIRECTION ( 'NONE',  ( 0.000000000000000000, 0.000000000000000000, 1.000000000000000000 ) ) ;
#27677=ADVANCED_FACE ( 'NONE', ( #58671 ), #43298, .F. ) ;
#27680=ADVANCED_FACE ( 'NONE', ( #15265 ), #25256, .T. ) ;
#27696=ADVANCED_FACE ( 'NONE', ( #8575 ), #36385, .F. ) ;
#27709=CARTESIAN_POINT ( 'NONE',  ( 17.75000000000000711, 30.99999999999999289, -3.750000000000000000 ) ) ;
#27724=DIRECTION ( 'NONE',  ( -0.000000000000000000, -0.000000000000000000, 1.000000000000000000 ) ) ;
#27726=EDGE_LOOP ( 'NONE', ( #8925, #898, #25766, #62453 ) ) ;
#27812=ORIENTED_EDGE ( 'NONE', *, *, #66388, .T. ) ;
#27819=EDGE_CURVE ( 'NONE', #20640, #60418, #69392, .T. ) ;
#27822=DIRECTION ( 'NONE',  ( -0.000000000000000000, -0.000000000000000000, -1.000000000000000000 ) ) ;
#27825=DIRECTION ( 'NONE',  ( 0.000000000000000000, 0.000000000000000000, -1.000000000000000000 ) ) ;
#27826=CARTESIAN_POINT ( 'NONE',  ( 22.25000000000000711, 33.74999999999999289, -4.000000000000000000 ) ) ;
#27854=CARTESIAN_POINT ( 'NONE',  ( 22.75000000000000711, 37.00000000000000000, -3.750000000000000000 ) ) ;
#27858=DIRECTION ( 'NONE',  ( -0.000000000000000000, -0.000000000000000000, -1.000000000000000000 ) ) ;
#27882=SURFACE_SIDE_STYLE ('',( #48378 ) ) ;
#27893=EDGE_CURVE ( 'NONE', #43138, #50411, #51056, .T. ) ;
#27927=CIRCLE ( 'NONE', #13337, 0.5000000000000004441 ) ;
#27930=EDGE_CURVE ( 'NONE', #63457, #15233, #61918, .T. ) ;
#27943=SPHERICAL_SURFACE ( 'NONE', #27043, 1.000000000000000000 ) ;
#27944=DIRECTION ( 'NONE',  ( -0.000000000000000000, 1.000000000000000000, -0.000000000000000000 ) ) ;
#27947=AXIS2_PLACEMENT_3D ( 'NONE', #21726, #64644, #549 ) ;
#27968=AXIS2_PLACEMENT_3D ( 'NONE', #27640, #6532, #1215 ) ;
#27999=VERTEX_POINT ( 'NONE', #57716 ) ;
#28035=CYLINDRICAL_SURFACE ( 'NONE', #23775, 0.2500000000000002220 ) ;
#28065=ORIENTED_EDGE ( 'NONE', *, *, #28247, .F. ) ;
#28068=FACE_OUTER_BOUND ( 'NONE', #61484, .T. ) ;
#28074=AXIS2_PLACEMENT_3D ( 'NONE', #35950, #56711, #57755 ) ;
#28077=ORIENTED_EDGE ( 'NONE', *, *, #50693, .F. ) ;
#28155=ORIENTED_EDGE ( 'NONE', *, *, #42939, .F. ) ;
#28169=ORIENTED_EDGE ( 'NONE', *, *, #5159, .T. ) ;
#28176=AXIS2_PLACEMENT_3D ( 'NONE', #35955, #57402, #30647 ) ;
#28191=( GEOMETRIC_REPRESENTATION_CONTEXT ( 3 ) GLOBAL_UNCERTAINTY_ASSIGNED_CONTEXT ( ( #50905 ) ) GLOBAL_UNIT_ASSIGNED_CONTEXT ( ( #36036, #57476, #46268 ) ) REPRESENTATION_CONTEXT ( 'NONE', 'WORKASPACE' ) );
#28203=EDGE_CURVE ( 'NONE', #31124, #5580, #6634, .T. ) ;
#28247=EDGE_CURVE ( 'NONE', #58978, #19151, #15957, .T. ) ;
#28248=CARTESIAN_POINT ( 'NONE',  ( -22.50000000000000711, 33.74999999999999289, -3.750000000000000000 ) ) ;
#28251=VECTOR ( 'NONE', #48263, 1000.000000000000000 ) ;
#28261=LINE ( 'NONE', #49770, #12180 ) ;
#28283=DIRECTION ( 'NONE',  ( 0.000000000000000000, -1.000000000000000000, 0.000000000000000000 ) ) ;
#28311=EDGE_LOOP ( 'NONE', ( #40566, #55934, #27126, #15236 ) ) ;
#28333=AXIS2_PLACEMENT_3D ( 'NONE', #26291, #53399, #4473 ) ;
#28342=CARTESIAN_POINT ( 'NONE',  ( -22.75000000000000711, 36.75000000000000000, 4.000000000000000000 ) ) ;
#28379=DIRECTION ( 'NONE',  ( 1.000000000000000000, -0.000000000000000000, -0.000000000000000000 ) ) ;
#28390=EDGE_LOOP ( 'NONE', ( #23165, #35007, #5560, #45073 ) ) ;
#28399=CIRCLE ( 'NONE', #4881, 1.000000000000000000 ) ;
#28402=CARTESIAN_POINT ( 'NONE',  ( 24.00000000000000355, 36.75000000000000000, -3.750000000000000000 ) ) ;
#28403=ORIENTED_EDGE ( 'NONE', *, *, #2130, .T. ) ;
#28408=DIRECTION ( 'NONE',  ( 0.000000000000000000, -1.000000000000000000, 0.000000000000000000 ) ) ;
#28423=DIRECTION ( 'NONE',  ( -1.000000000000000000, 0.000000000000000000, 0.000000000000000000 ) ) ;
#28461=FACE_OUTER_BOUND ( 'NONE', #40764, .T. ) ;
#28516=CARTESIAN_POINT ( 'NONE',  ( 18.25000000000000711, 33.74999999999999289, -4.000000000000000000 ) ) ;
#28528=CARTESIAN_POINT ( 'NONE',  ( 0.000000000000000000, 27.74999999999998934, 4.000000000000000000 ) ) ;
#28532=LINE ( 'NONE', #49012, #34997 ) ;
#28533=DIRECTION ( 'NONE',  ( 1.000000000000000000, 0.000000000000000000, 0.000000000000000000 ) ) ;
#28579=CIRCLE ( 'NONE', #5002, 0.5000000000000000000 ) ;
#28601=DIRECTION ( 'NONE',  ( 9.376883653928687363E-17, -1.000000000000000000, 0.000000000000000000 ) ) ;
#28610=ORIENTED_EDGE ( 'NONE', *, *, #35017, .F. ) ;
#28663=ADVANCED_FACE ( 'NONE', ( #51151, #24386, #40253 ), #2898, .T. ) ;
#28668=AXIS2_PLACEMENT_3D ( 'NONE', #48148, #32975, #43571 ) ;
#28672=DIRECTION ( 'NONE',  ( -0.000000000000000000, -0.000000000000000000, 1.000000000000000000 ) ) ;
#28676=ORIENTED_EDGE ( 'NONE', *, *, #42939, .T. ) ;
#28691=CARTESIAN_POINT ( 'NONE',  ( 13.74999999999998757, -7.950815931560351124E-15, 3.750000000000000000 ) ) ;
#28718=AXIS2_PLACEMENT_3D ( 'NONE', #44655, #61122, #22818 ) ;
#28737=EDGE_CURVE ( 'NONE', #40140, #67406, #34267, .T. ) ;
#28755=ORIENTED_EDGE ( 'NONE', *, *, #61840, .T. ) ;
#28756=VECTOR ( 'NONE', #18912, 1000.000000000000000 ) ;
#28758=FACE_OUTER_BOUND ( 'NONE', #22552, .T. ) ;
#28761=ORIENTED_EDGE ( 'NONE', *, *, #27930, .T. ) ;
#28769=DIRECTION ( 'NONE',  ( -1.000000000000000000, 0.000000000000000000, 0.000000000000000000 ) ) ;
#28771=ORIENTED_EDGE ( 'NONE', *, *, #3809, .F. ) ;
#28781=DIRECTION ( 'NONE',  ( -1.000000000000000000, 0.000000000000000000, 0.000000000000000000 ) ) ;
#28783=DIRECTION ( 'NONE',  ( -1.000000000000000000, -5.782411586589351722E-16, 0.000000000000000000 ) ) ;
#28837=DIRECTION ( 'NONE',  ( 0.000000000000000000, 0.000000000000000000, -1.000000000000000000 ) ) ;
#28845=VERTEX_POINT ( 'NONE', #27499 ) ;
#28852=ORIENTED_EDGE ( 'NONE', *, *, #43574, .F. ) ;
#28862=FACE_OUTER_BOUND ( 'NONE', #9354, .T. ) ;
#28865=AXIS2_PLACEMENT_3D ( 'NONE', #38265, #22386, #17144 ) ;
#28876=DIRECTION ( 'NONE',  ( 0.000000000000000000, -1.000000000000000000, 0.000000000000000000 ) ) ;
#28882=ADVANCED_FACE ( 'NONE', ( #56319 ), #18284, .T. ) ;
#28888=ORIENTED_EDGE ( 'NONE', *, *, #22578, .T. ) ;
#28900=AXIS2_PLACEMENT_3D ( 'NONE', #51658, #2726, #30519 ) ;
#28903=DIRECTION ( 'NONE',  ( 0.000000000000000000, 0.000000000000000000, -1.000000000000000000 ) ) ;
#28924=ORIENTED_EDGE ( 'NONE', *, *, #48042, .F. ) ;
#28975=FACE_OUTER_BOUND ( 'NONE', #62665, .T. ) ;
#28977=ORIENTED_EDGE ( 'NONE', *, *, #27065, .T. ) ;
#28987=CYLINDRICAL_SURFACE ( 'NONE', #50380, 4.000000000000000000 ) ;
#28991=CIRCLE ( 'NONE', #36939, 0.5000000000000004441 ) ;
#28992=DIRECTION ( 'NONE',  ( -0.000000000000000000, -0.000000000000000000, -1.000000000000000000 ) ) ;
#28995=CARTESIAN_POINT ( 'NONE',  ( -13.25000000000000355, 27.99999999999998934, -3.750000000000000000 ) ) ;
#29007=DIRECTION ( 'NONE',  ( 0.000000000000000000, -0.000000000000000000, -1.000000000000000000 ) ) ;
#29010=DIRECTION ( 'NONE',  ( -0.000000000000000000, -0.000000000000000000, 1.000000000000000000 ) ) ;
#29043=DIRECTION ( 'NONE',  ( -0.000000000000000000, -0.000000000000000000, 1.000000000000000000 ) ) ;
#29053=EDGE_LOOP ( 'NONE', ( #57984, #13542, #63664, #13479 ) ) ;
#29097=ORIENTED_EDGE ( 'NONE', *, *, #6646, .F. ) ;
#29134=VECTOR ( 'NONE', #2441, 1000.000000000000000 ) ;
#29146=LINE ( 'NONE', #45737, #48433 ) ;
#29160=ORIENTED_EDGE ( 'NONE', *, *, #1980, .F. ) ;
#29203=EDGE_CURVE ( 'NONE', #61204, #32928, #43040, .T. ) ;
#29229=DIRECTION ( 'NONE',  ( 1.000000000000000000, 0.000000000000000000, 0.000000000000000000 ) ) ;
#29237=CARTESIAN_POINT ( 'NONE',  ( 8.750000000000001776, 24.74999999999998579, -4.000000000000000000 ) ) ;
#29291=AXIS2_PLACEMENT_3D ( 'NONE', #20354, #25618, #59035 ) ;
#29351=DIRECTION ( 'NONE',  ( 0.000000000000000000, -1.000000000000000000, -0.000000000000000000 ) ) ;
#29366=AXIS2_PLACEMENT_3D ( 'NONE', #34859, #17676, #39145 ) ;
#29367=FACE_OUTER_BOUND ( 'NONE', #58383, .T. ) ;
#29381=ADVANCED_FACE ( 'NONE', ( #64408 ), #64756, .T. ) ;
#29384=ORIENTED_EDGE ( 'NONE', *, *, #18364, .F. ) ;
#29387=CIRCLE ( 'NONE', #68744, 0.2500000000000002220 ) ;
#29396=CARTESIAN_POINT ( 'NONE',  ( -9.250000000000003553, 27.74999999999998934, 3.750000000000000000 ) ) ;
#29410=LINE ( 'NONE', #51232, #18861 ) ;
#29429=CARTESIAN_POINT ( 'NONE',  ( 17.75000000000000711, 30.99999999999999289, -4.000000000000000000 ) ) ;
#29453=ORIENTED_EDGE ( 'NONE', *, *, #24064, .T. ) ;
#29459=ORIENTED_EDGE ( 'NONE', *, *, #32623, .T. ) ;
#29460=CARTESIAN_POINT ( 'NONE',  ( 24.75000000000000355, 36.75000000000000000, -3.000000000000000000 ) ) ;
#29462=CIRCLE ( 'NONE', #40747, 0.2500000000000002220 ) ;
#29476=VECTOR ( 'NONE', #28601, 1000.000000000000000 ) ;
#29479=ORIENTED_EDGE ( 'NONE', *, *, #37400, .F. ) ;
#29481=VERTEX_POINT ( 'NONE', #44391 ) ;
#29498=ORIENTED_EDGE ( 'NONE', *, *, #67674, .T. ) ;
#29500=CARTESIAN_POINT ( 'NONE',  ( -13.50000000000000355, 28.24999999999998934, -3.750000000000000000 ) ) ;
#29514=CYLINDRICAL_SURFACE ( 'NONE', #23468, 1.000000000000000888 ) ;
#29542=CARTESIAN_POINT ( 'NONE',  ( 22.75000000000000711, 37.00000000000000000, -3.750000000000000000 ) ) ;
#29555=EDGE_CURVE ( 'NONE', #42883, #33741, #9494, .T. ) ;
#29560=DIRECTION ( 'NONE',  ( 0.000000000000000000, -1.000000000000000000, 0.000000000000000000 ) ) ;
#29572=DIRECTION ( 'NONE',  ( 1.000000000000000000, 0.000000000000000000, 0.000000000000000000 ) ) ;
#29578=CARTESIAN_POINT ( 'NONE',  ( -4.750000000000002665, 24.74999999999998579, 3.750000000000000000 ) ) ;
#29659=DIRECTION ( 'NONE',  ( -1.000000000000000000, 0.000000000000000000, 0.000000000000000000 ) ) ;
#29666=EDGE_LOOP ( 'NONE', ( #18995, #28169, #29384, #68486 ) ) ;
#29675=ORIENTED_EDGE ( 'NONE', *, *, #33462, .T. ) ;
#29688=DIRECTION ( 'NONE',  ( 0.000000000000000000, 0.000000000000000000, -1.000000000000000000 ) ) ;
#29707=VECTOR ( 'NONE', #58350, 1000.000000000000000 ) ;
#29762=CARTESIAN_POINT ( 'NONE',  ( 22.50000000000000711, 33.99999999999999289, 4.000000000000000000 ) ) ;
#29769=EDGE_LOOP ( 'NONE', ( #451, #3582, #24047, #58202 ) ) ;
#29777=EDGE_CURVE ( 'NONE', #61721, #38442, #8297, .T. ) ;
#29787=CARTESIAN_POINT ( 'NONE',  ( 13.50000000000000533, 30.74999999999999289, 4.000000000000000000 ) ) ;
#29793=CARTESIAN_POINT ( 'NONE',  ( 13.75000000000000533, 30.74999999999999289, -3.750000000000000000 ) ) ;
#29802=CARTESIAN_POINT ( 'NONE',  ( 15.00000000000000000, 8.000000000000000000, 4.000000000000000000 ) ) ;
#29803=EDGE_LOOP ( 'NONE', ( #59958, #48344, #33764, #36859 ) ) ;
#29828=ORIENTED_EDGE ( 'NONE', *, *, #55313, .T. ) ;
#29836=EDGE_LOOP ( 'NONE', ( #934, #54212, #37646, #66969 ) ) ;
#29839=CYLINDRICAL_SURFACE ( 'NONE', #9022, 1.000000000000000888 ) ;
#29844=DIRECTION ( 'NONE',  ( 0.000000000000000000, 0.000000000000000000, -1.000000000000000000 ) ) ;
#29879=EDGE_CURVE ( 'NONE', #13443, #9871, #12919, .T. ) ;
#29886=PLANE ( 'NONE',  #18027 ) ;
#29889=AXIS2_PLACEMENT_3D ( 'NONE', #612, #12951, #66421 ) ;
#29912=CARTESIAN_POINT ( 'NONE',  ( 18.00000000000000711, 31.24999999999999289, -3.750000000000000000 ) ) ;
#29937=CIRCLE ( 'NONE', #54677, 0.2500000000000002220 ) ;
#29965=AXIS2_PLACEMENT_3D ( 'NONE', #48736, #60279, #6122 ) ;
#30006=VERTEX_POINT ( 'NONE', #30468 ) ;
#30007=DIRECTION ( 'NONE',  ( 0.000000000000000000, -0.000000000000000000, -1.000000000000000000 ) ) ;
#30044=FACE_OUTER_BOUND ( 'NONE', #65819, .T. ) ;
#30065=AXIS2_PLACEMENT_3D ( 'NONE', #55783, #8644, #62773 ) ;
#30067=CARTESIAN_POINT ( 'NONE',  ( 19.49999999999997513, 8.000000000000000000, -4.000000000000000000 ) ) ;
#30098=DIRECTION ( 'NONE',  ( -1.000000000000000000, 0.000000000000000000, 0.000000000000000000 ) ) ;
#30110=CYLINDRICAL_SURFACE ( 'NONE', #31377, 0.2500000000000002220 ) ;
#30137=ADVANCED_FACE ( 'NONE', ( #49058 ), #18436, .T. ) ;
#30140=CARTESIAN_POINT ( 'NONE',  ( -24.00000000000000355, 36.75000000000000000, -4.000000000000000000 ) ) ;
#30181=ORIENTED_EDGE ( 'NONE', *, *, #61518, .F. ) ;
#30199=ORIENTED_EDGE ( 'NONE', *, *, #23202, .T. ) ;
#30207=CARTESIAN_POINT ( 'NONE',  ( 24.00000000000000355, 36.75000000000000000, 4.000000000000000000 ) ) ;
#30237=ORIENTED_EDGE ( 'NONE', *, *, #18330, .T. ) ;
#30243=CARTESIAN_POINT ( 'NONE',  ( -11.00000000000000000, 8.000000000000000000, -3.500000000000017764 ) ) ;
#30256=TOROIDAL_SURFACE ( 'NONE', #14567, 0.5000000000000000000, 0.2500000000000000000 ) ;
#30281=CARTESIAN_POINT ( 'NONE',  ( -24.75000000000000355, 37.00000000000000000, -3.000000000000000000 ) ) ;
#30286=CARTESIAN_POINT ( 'NONE',  ( 4.750000000000002665, 24.74999999999998579, 4.000000000000000000 ) ) ;
#30303=FACE_OUTER_BOUND ( 'NONE', #31520, .T. ) ;
#30338=EDGE_LOOP ( 'NONE', ( #951, #7280, #39278 ) ) ;
#30357=DIRECTION ( 'NONE',  ( 0.000000000000000000, 1.000000000000000000, 0.000000000000000000 ) ) ;
#30380=VERTEX_POINT ( 'NONE', #58117 ) ;
#30384=CARTESIAN_POINT ( 'NONE',  ( 11.00000000000000000, 8.000000000000000000, 3.500000000000003997 ) ) ;
#30391=ADVANCED_FACE ( 'NONE', ( #25727 ), #31707, .T. ) ;
#30405=CARTESIAN_POINT ( 'NONE',  ( 18.25000000000000711, 33.99999999999999289, 4.000000000000000000 ) ) ;
#30468=CARTESIAN_POINT ( 'NONE',  ( -25.00000000000000000, 1.000000000000000000, -3.000000000000000000 ) ) ;
#30479=DIRECTION ( 'NONE',  ( 0.000000000000000000, 0.000000000000000000, 1.000000000000000000 ) ) ;
#30481=ORIENTED_EDGE ( 'NONE', *, *, #23659, .T. ) ;
#30519=DIRECTION ( 'NONE',  ( 0.000000000000000000, 0.000000000000000000, -1.000000000000000000 ) ) ;
#30531=VECTOR ( 'NONE', #20489, 1000.000000000000000 ) ;
#30564=LINE ( 'NONE', #46106, #67518 ) ;
#30591=CIRCLE ( 'NONE', #209, 0.2500000000000002220 ) ;
#30600=CARTESIAN_POINT ( 'NONE',  ( -4.250000000000001776, 21.99999999999998579, 4.000000000000000000 ) ) ;
#30643=VECTOR ( 'NONE', #62597, 1000.000000000000000 ) ;
#30644=CARTESIAN_POINT ( 'NONE',  ( -8.750000000000001776, 24.99999999999998579, -3.750000000000000000 ) ) ;
#30647=DIRECTION ( 'NONE',  ( 0.000000000000000000, 0.000000000000000000, 1.000000000000000000 ) ) ;
#30650=FACE_OUTER_BOUND ( 'NONE', #55546, .T. ) ;
#30654=DIRECTION ( 'NONE',  ( 0.000000000000000000, 1.000000000000000000, 0.000000000000000000 ) ) ;
#30655=DIRECTION ( 'NONE',  ( -1.000000000000000000, 0.000000000000000000, 0.000000000000000000 ) ) ;
#30672=VERTEX_POINT ( 'NONE', #23921 ) ;
#30678=CYLINDRICAL_SURFACE ( 'NONE', #9249, 0.2500000000000002220 ) ;
#30704=CARTESIAN_POINT ( 'NONE',  ( 19.00000000000000000, 8.000000000000000000, 4.000000000000000000 ) ) ;
#30708=CIRCLE ( 'NONE', #9405, 4.000000000000000000 ) ;
#30713=EDGE_CURVE ( 'NONE', #63323, #5366, #8460, .T. ) ;
#30722=ORIENTED_EDGE ( 'NONE', *, *, #791, .T. ) ;
#30727=EDGE_CURVE ( 'NONE', #68401, #51757, #63424, .T. ) ;
#30732=FACE_OUTER_BOUND ( 'NONE', #47752, .T. ) ;
#30744=ORIENTED_EDGE ( 'NONE', *, *, #2293, .T. ) ;
#30753=VERTEX_POINT ( 'NONE', #63637 ) ;
#30762=AXIS2_PLACEMENT_3D ( 'NONE', #15392, #17712, #44134 ) ;
#30776=DIRECTION ( 'NONE',  ( 0.000000000000000000, 0.000000000000000000, -1.000000000000000000 ) ) ;
#30781=FACE_OUTER_BOUND ( 'NONE', #58039, .T. ) ;
#30786=AXIS2_PLACEMENT_3D ( 'NONE', #4084, #68847, #30479 ) ;
#30810=CARTESIAN_POINT ( 'NONE',  ( 22.25000000000000711, 33.74999999999999289, -4.000000000000000000 ) ) ;
#30818=DIRECTION ( 'NONE',  ( 0.000000000000000000, 0.000000000000000000, -1.000000000000000000 ) ) ;
#30822=CONICAL_SURFACE ( 'NONE', #445, 4.499999999999976019, 0.7853981633974412846 ) ;
#30834=CARTESIAN_POINT ( 'NONE',  ( 17.75000000000000711, 30.74999999999999289, -3.750000000000000000 ) ) ;
#30855=SPHERICAL_SURFACE ( 'NONE', #26246, 0.2500000000000000000 ) ;
#30879=DIRECTION ( 'NONE',  ( 0.000000000000000000, 0.000000000000000000, -1.000000000000000000 ) ) ;
#30880=ADVANCED_FACE ( 'NONE', ( #59367 ), #22456, .T. ) ;
#30916=DIRECTION ( 'NONE',  ( -0.000000000000000000, -0.000000000000000000, 1.000000000000000000 ) ) ;
#30941=ORIENTED_EDGE ( 'NONE', *, *, #18435, .F. ) ;
#30945=ORIENTED_EDGE ( 'NONE', *, *, #31340, .F. ) ;
#30963=DIRECTION ( 'NONE',  ( 1.000000000000000000, -0.000000000000000000, 0.000000000000000000 ) ) ;
#30967=ORIENTED_EDGE ( 'NONE', *, *, #22798, .T. ) ;
#30991=VECTOR ( 'NONE', #64523, 1000.000000000000000 ) ;
#31008=LINE ( 'NONE', #23238, #10586 ) ;
#31017=CARTESIAN_POINT ( 'NONE',  ( 13.75000000000000533, 30.74999999999999289, -4.000000000000000000 ) ) ;
#31032=FACE_OUTER_BOUND ( 'NONE', #51654, .T. ) ;
#31037=DIRECTION ( 'NONE',  ( 0.000000000000000000, 0.000000000000000000, -1.000000000000000000 ) ) ;
#31077=AXIS2_PLACEMENT_3D ( 'NONE', #9619, #52531, #31037 ) ;
#31124=VERTEX_POINT ( 'NONE', #30644 ) ;
#31154=CARTESIAN_POINT ( 'NONE',  ( -24.00000000000000000, 1.000000000000000000, -3.000000000000000000 ) ) ;
#31169=FACE_OUTER_BOUND ( 'NONE', #42731, .T. ) ;
#31174=ORIENTED_EDGE ( 'NONE', *, *, #23054, .F. ) ;
#31189=ORIENTED_EDGE ( 'NONE', *, *, #56471, .T. ) ;
#31208=CARTESIAN_POINT ( 'NONE',  ( -13.75000000000000533, 30.74999999999999289, 3.750000000000000000 ) ) ;
#31213=AXIS2_PLACEMENT_3D ( 'NONE', #34355, #55805, #57185 ) ;
#31246=AXIS2_PLACEMENT_3D ( 'NONE', #44053, #44408, #23247 ) ;
#31266=CIRCLE ( 'NONE', #876, 4.000000000000000000 ) ;
#31278=EDGE_LOOP ( 'NONE', ( #45768, #63141, #43609, #43059 ) ) ;
#31282=CONICAL_SURFACE ( 'NONE', #50387, 4.499999999999976019, 0.7853981633974412846 ) ;
#31340=EDGE_CURVE ( 'NONE', #36018, #60418, #19569, .T. ) ;
#31351=LINE ( 'NONE', #64064, #54850 ) ;
#31353=AXIS2_PLACEMENT_3D ( 'NONE', #8648, #2958, #24447 ) ;
#31377=AXIS2_PLACEMENT_3D ( 'NONE', #3344, #24836, #24153 ) ;
#31382=DIRECTION ( 'NONE',  ( 0.000000000000000000, 0.000000000000000000, -1.000000000000000000 ) ) ;
#31383=VERTEX_POINT ( 'NONE', #303 ) ;
#31406=CIRCLE ( 'NONE', #16838, 0.2500000000000002220 ) ;
#31442=DIRECTION ( 'NONE',  ( -1.000000000000000000, 0.000000000000000000, 0.000000000000000000 ) ) ;
#31485=DIRECTION ( 'NONE',  ( 0.000000000000000000, 1.000000000000000000, 0.000000000000000000 ) ) ;
#31520=EDGE_LOOP ( 'NONE', ( #22072, #20875, #32094, #45374 ) ) ;
#31530=VERTEX_POINT ( 'NONE', #50301 ) ;
#31531=ORIENTED_EDGE ( 'NONE', *, *, #19367, .T. ) ;
#31534=CARTESIAN_POINT ( 'NONE',  ( -17.75000000000000711, 31.24999999999999289, -3.750000000000000000 ) ) ;
#31549=DIRECTION ( 'NONE',  ( 1.000000000000000000, -0.000000000000000000, -0.000000000000000000 ) ) ;
#31557=CARTESIAN_POINT ( 'NONE',  ( 13.25000000000000355, 28.24999999999998934, 4.000000000000000000 ) ) ;
#31564=CARTESIAN_POINT ( 'NONE',  ( 13.25000000000000355, 27.99999999999998934, -3.750000000000000000 ) ) ;
#31603=DIRECTION ( 'NONE',  ( -1.000000000000000000, 0.000000000000000000, 0.000000000000000000 ) ) ;
#31614=EDGE_CURVE ( 'NONE', #65139, #54390, #43227, .T. ) ;
#31627=DIRECTION ( 'NONE',  ( 0.000000000000000000, 0.000000000000000000, -1.000000000000000000 ) ) ;
#31633=ORIENTED_EDGE ( 'NONE', *, *, #62711, .F. ) ;
#31643=VECTOR ( 'NONE', #4360, 1000.000000000000000 ) ;
#31664=CYLINDRICAL_SURFACE ( 'NONE', #45231, 0.2500000000000002220 ) ;
#31690=FACE_OUTER_BOUND ( 'NONE', #31278, .T. ) ;
#31707=CYLINDRICAL_SURFACE ( 'NONE', #65620, 0.2500000000000002220 ) ;
#31728=CARTESIAN_POINT ( 'NONE',  ( 18.00000000000000711, 31.24999999999999289, -3.750000000000000000 ) ) ;
#31739=EDGE_LOOP ( 'NONE', ( #61985, #38545, #8820, #50527 ) ) ;
#31768=EDGE_CURVE ( 'NONE', #66883, #38684, #9125, .T. ) ;
#31776=DIRECTION ( 'NONE',  ( 1.000000000000000000, 0.000000000000000000, 0.000000000000000000 ) ) ;
#31844=AXIS2_PLACEMENT_3D ( 'NONE', #21409, #10530, #54106 ) ;
#31876=AXIS2_PLACEMENT_3D ( 'NONE', #56036, #8573, #56760 ) ;
#31879=CARTESIAN_POINT ( 'NONE',  ( -24.00000000000000000, 1.000000000000000000, 3.000000000000000000 ) ) ;
#31881=ORIENTED_EDGE ( 'NONE', *, *, #10585, .T. ) ;
#31893=ORIENTED_EDGE ( 'NONE', *, *, #27051, .T. ) ;
#31919=ORIENTED_EDGE ( 'NONE', *, *, #41307, .T. ) ;
#31925=ORIENTED_EDGE ( 'NONE', *, *, #61600, .T. ) ;
#31927=EDGE_CURVE ( 'NONE', #46369, #39699, #40037, .T. ) ;
#31930=DIRECTION ( 'NONE',  ( -0.000000000000000000, -0.000000000000000000, 1.000000000000000000 ) ) ;
#31937=CARTESIAN_POINT ( 'NONE',  ( -8.750000000000001776, 24.74999999999998579, -3.750000000000000000 ) ) ;
#31939=DIRECTION ( 'NONE',  ( -0.000000000000000000, -0.000000000000000000, -1.000000000000000000 ) ) ;
#31960=ORIENTED_EDGE ( 'NONE', *, *, #9938, .F. ) ;
#31961=EDGE_LOOP ( 'NONE', ( #63811, #29828, #42935, #54884 ) ) ;
#31987=EDGE_LOOP ( 'NONE', ( #12675, #34945, #51748, #16911 ) ) ;
#32025=EDGE_CURVE ( 'NONE', #15837, #55021, #61198, .T. ) ;
#32055=CIRCLE ( 'NONE', #28668, 0.2500000000000002220 ) ;
#32094=ORIENTED_EDGE ( 'NONE', *, *, #18379, .T. ) ;
#32096=EDGE_CURVE ( 'NONE', #30006, #33741, #56742, .T. ) ;
#32154=CARTESIAN_POINT ( 'NONE',  ( 4.500000000000002665, 24.99999999999998579, 3.750000000000000000 ) ) ;
#32158=ORIENTED_EDGE ( 'NONE', *, *, #40446, .F. ) ;
#32164=CARTESIAN_POINT ( 'NONE',  ( 0.000000000000000000, 1.000000000000000000, 4.000000000000000000 ) ) ;
#32176=ORIENTED_EDGE ( 'NONE', *, *, #54460, .F. ) ;
#32190=DIRECTION ( 'NONE',  ( 0.000000000000000000, 0.000000000000000000, -1.000000000000000000 ) ) ;
#32211=VECTOR ( 'NONE', #19163, 1000.000000000000000 ) ;
#32221=LINE ( 'NONE', #26575, #66313 ) ;
#32239=ADVANCED_FACE ( 'NONE', ( #21654 ), #2762, .T. ) ;
#32248=ORIENTED_EDGE ( 'NONE', *, *, #39110, .F. ) ;
#32265=ORIENTED_EDGE ( 'NONE', *, *, #52741, .F. ) ;
#32273=LINE ( 'NONE', #20698, #17850 ) ;
#32304=DIRECTION ( 'NONE',  ( 0.000000000000000000, 0.000000000000000000, -1.000000000000000000 ) ) ;
#32311=EDGE_LOOP ( 'NONE', ( #41884, #57422, #49893, #7733 ) ) ;
#32339=DIRECTION ( 'NONE',  ( 0.000000000000000000, -1.000000000000000000, 0.000000000000000000 ) ) ;
#32345=ORIENTED_EDGE ( 'NONE', *, *, #24064, .F. ) ;
#32409=EDGE_CURVE ( 'NONE', #16875, #8380, #20844, .T. ) ;
#32414=ORIENTED_EDGE ( 'NONE', *, *, #5321, .F. ) ;
#32444=CARTESIAN_POINT ( 'NONE',  ( -17.75000000000000711, 30.74999999999999289, -3.750000000000000000 ) ) ;
#32474=AXIS2_PLACEMENT_3D ( 'NONE', #46960, #8591, #52558 ) ;
#32502=ORIENTED_EDGE ( 'NONE', *, *, #50704, .T. ) ;
#32507=CIRCLE ( 'NONE', #31353, 0.2500000000000002220 ) ;
#32518=DIRECTION ( 'NONE',  ( -1.000000000000000000, 0.000000000000000000, 0.000000000000000000 ) ) ;
#32570=DIRECTION ( 'NONE',  ( -1.000000000000000000, 0.000000000000000000, 0.000000000000000000 ) ) ;
#32619=AXIS2_PLACEMENT_3D ( 'NONE', #55316, #65533, #414 ) ;
#32620=DIRECTION ( 'NONE',  ( 0.000000000000000000, -1.000000000000000000, -0.000000000000000000 ) ) ;
#32623=EDGE_CURVE ( 'NONE', #50288, #2387, #8538, .T. ) ;
#32652=ORIENTED_EDGE ( 'NONE', *, *, #19040, .F. ) ;
#32701=DIRECTION ( 'NONE',  ( -0.000000000000000000, 0.000000000000000000, -1.000000000000000000 ) ) ;
#32703=DIRECTION ( 'NONE',  ( 0.000000000000000000, 0.000000000000000000, -1.000000000000000000 ) ) ;
#32705=EDGE_LOOP ( 'NONE', ( #15900, #21975, #61392, #19256 ) ) ;
#32713=DIRECTION ( 'NONE',  ( -1.000000000000000000, 0.000000000000000000, 0.000000000000000000 ) ) ;
#32777=CIRCLE ( 'NONE', #54098, 0.2500000000000002220 ) ;
#32792=TOROIDAL_SURFACE ( 'NONE', #61828, 0.7500000000000000000, 0.2500000000000000000 ) ;
#32808=AXIS2_PLACEMENT_3D ( 'NONE', #20935, #47354, #26185 ) ;
#32818=PLANE ( 'NONE',  #23550 ) ;
#32836=DIRECTION ( 'NONE',  ( 1.000000000000000000, -0.000000000000000000, 0.000000000000000000 ) ) ;
#32842=DIRECTION ( 'NONE',  ( 1.000000000000000000, 0.000000000000000000, 0.000000000000000000 ) ) ;
#32867=LINE ( 'NONE', #65209, #20507 ) ;
#32876=CARTESIAN_POINT ( 'NONE',  ( -18.00000000000000711, 33.99999999999999289, 3.750000000000000000 ) ) ;
#32882=CIRCLE ( 'NONE', #59836, 0.2500000000000002220 ) ;
#32884=EDGE_CURVE ( 'NONE', #50288, #51977, #44802, .T. ) ;
#32903=DIRECTION ( 'NONE',  ( -1.000000000000000000, 0.000000000000000000, 0.000000000000000000 ) ) ;
#32914=EDGE_CURVE ( 'NONE', #454, #39136, #56342, .T. ) ;
#32920=DIRECTION ( 'NONE',  ( 0.000000000000000000, -1.000000000000000000, 0.000000000000000000 ) ) ;
#32928=VERTEX_POINT ( 'NONE', #30281 ) ;
#32931=ORIENTED_EDGE ( 'NONE', *, *, #22009, .F. ) ;
#32932=DIRECTION ( 'NONE',  ( 0.000000000000000000, 0.000000000000000000, 1.000000000000000000 ) ) ;
#32953=CARTESIAN_POINT ( 'NONE',  ( 4.250000000000001776, 21.99999999999998579, 3.750000000000000000 ) ) ;
#32959=ADVANCED_FACE ( 'NONE', ( #8177 ), #4237, .T. ) ;
#32963=ORIENTED_EDGE ( 'NONE', *, *, #31927, .T. ) ;
#32968=AXIS2_PLACEMENT_3D ( 'NONE', #36276, #46491, #4188 ) ;
#32975=DIRECTION ( 'NONE',  ( -0.000000000000000000, -0.000000000000000000, 1.000000000000000000 ) ) ;
#32997=CIRCLE ( 'NONE', #45444, 0.2500000000000002220 ) ;
#33026=VERTEX_POINT ( 'NONE', #36328 ) ;
#33048=CYLINDRICAL_SURFACE ( 'NONE', #45321, 0.2500000000000002220 ) ;
#33067=EDGE_LOOP ( 'NONE', ( #36462, #50814, #32931, #29479 ) ) ;
#33077=EDGE_CURVE ( 'NONE', #60418, #58121, #20456, .T. ) ;
#33099=ORIENTED_EDGE ( 'NONE', *, *, #32914, .F. ) ;
#33111=AXIS2_PLACEMENT_3D ( 'NONE', #9113, #19286, #21642 ) ;
#33122=VERTEX_POINT ( 'NONE', #60070 ) ;
#33168=EDGE_CURVE ( 'NONE', #20521, #69477, #15786, .T. ) ;
#33203=EDGE_CURVE ( 'NONE', #50598, #63457, #39342, .T. ) ;
#33217=DIRECTION ( 'NONE',  ( -1.000000000000000000, 0.000000000000000000, 0.000000000000000000 ) ) ;
#33280=CARTESIAN_POINT ( 'NONE',  ( 24.75000000000000355, 37.00000000000000000, 4.000000000000000000 ) ) ;
#33302=LINE ( 'NONE', #65303, #15613 ) ;
#33305=CYLINDRICAL_SURFACE ( 'NONE', #59227, 0.2500000000000002220 ) ;
#33309=FACE_OUTER_BOUND ( 'NONE', #68313, .T. ) ;
#33353=ORIENTED_EDGE ( 'NONE', *, *, #23202, .F. ) ;
#33384=CARTESIAN_POINT ( 'NONE',  ( -13.25000000000000355, 27.99999999999998934, 4.000000000000000000 ) ) ;
#33387=SPHERICAL_SURFACE ( 'NONE', #33406, 0.2500000000000000000 ) ;
#33399=CARTESIAN_POINT ( 'NONE',  ( -4.750000000000002665, 24.74999999999998579, 3.750000000000000000 ) ) ;
#33406=AXIS2_PLACEMENT_3D ( 'NONE', #43317, #16890, #54815 ) ;
#33412=CARTESIAN_POINT ( 'NONE',  ( 19.49999999999997513, 8.000000000000000000, -4.000000000000000000 ) ) ;
#33449=CARTESIAN_POINT ( 'NONE',  ( 0.000000000000000000, 36.75000000000000000, 3.750000000000000000 ) ) ;
#33462=EDGE_CURVE ( 'NONE', #29481, #21095, #32221, .T. ) ;
#33471=CARTESIAN_POINT ( 'NONE',  ( 4.250000000000001776, 22.24999999999998579, 4.000000000000000000 ) ) ;
#33513=CYLINDRICAL_SURFACE ( 'NONE', #35814, 0.2500000000000002220 ) ;
#33623=CIRCLE ( 'NONE', #27968, 0.2500000000000002220 ) ;
#33651=AXIS2_PLACEMENT_3D ( 'NONE', #47759, #42455, #22338 ) ;
#33652=CARTESIAN_POINT ( 'NONE',  ( 15.00000000000000000, 8.000000000000000000, 3.500000000000003997 ) ) ;
#33676=VECTOR ( 'NONE', #21499, 1000.000000000000000 ) ;
#33678=ORIENTED_EDGE ( 'NONE', *, *, #6420, .F. ) ;
#33681=CARTESIAN_POINT ( 'NONE',  ( 24.00000000000000000, 1.000000000000000000, 3.000000000000000000 ) ) ;
#33714=CARTESIAN_POINT ( 'NONE',  ( -11.00000000000000000, 8.000000000000000000, 4.000000000000000000 ) ) ;
#33715=ORIENTED_EDGE ( 'NONE', *, *, #25038, .F. ) ;
#33723=ORIENTED_EDGE ( 'NONE', *, *, #66135, .F. ) ;
#33726=CARTESIAN_POINT ( 'NONE',  ( -24.75000000000000355, 36.75000000000000000, 4.000000000000000000 ) ) ;
#33729=CARTESIAN_POINT ( 'NONE',  ( 9.250000000000003553, 27.99999999999998934, 4.000000000000000000 ) ) ;
#33731=ORIENTED_EDGE ( 'NONE', *, *, #51324, .T. ) ;
#33741=VERTEX_POINT ( 'NONE', #5059 ) ;
#33763=AXIS2_PLACEMENT_3D ( 'NONE', #36533, #2787, #39806 ) ;
#33764=ORIENTED_EDGE ( 'NONE', *, *, #25404, .T. ) ;
#33765=EDGE_CURVE ( 'NONE', #41120, #38684, #26868, .T. ) ;
#33806=CARTESIAN_POINT ( 'NONE',  ( -22.50000000000000711, 33.99999999999999289, 4.000000000000000000 ) ) ;
#33829=ORIENTED_EDGE ( 'NONE', *, *, #11081, .T. ) ;
#33853=CIRCLE ( 'NONE', #49604, 1.000000000000000000 ) ;
#33986=DIRECTION ( 'NONE',  ( 0.000000000000000000, 0.000000000000000000, -1.000000000000000000 ) ) ;
#34003=DIRECTION ( 'NONE',  ( 9.376883653928687363E-17, 1.000000000000000000, 0.000000000000000000 ) ) ;
#34066=DIRECTION ( 'NONE',  ( 1.000000000000000000, -0.000000000000000000, -0.000000000000000000 ) ) ;
#34070=CARTESIAN_POINT ( 'NONE',  ( 22.50000000000000711, 34.24999999999999289, 4.000000000000000000 ) ) ;
#34083=EDGE_LOOP ( 'NONE', ( #2620, #46136, #24272, #57317 ) ) ;
#34088=ADVANCED_FACE ( 'NONE', ( #46560 ), #19768, .T. ) ;
#34134=ORIENTED_EDGE ( 'NONE', *, *, #19996, .T. ) ;
#34142=EDGE_CURVE ( 'NONE', #57180, #29481, #10093, .T. ) ;
#34164=DIRECTION ( 'NONE',  ( 0.000000000000000000, -1.000000000000000000, 0.000000000000000000 ) ) ;
#34219=AXIS2_PLACEMENT_3D ( 'NONE', #29762, #67057, #2633 ) ;
#34232=EDGE_CURVE ( 'NONE', #53882, #58067, #21147, .T. ) ;
#34240=CARTESIAN_POINT ( 'NONE',  ( -13.25000000000000355, 28.24999999999998934, -3.750000000000000000 ) ) ;
#34267=LINE ( 'NONE', #45206, #55322 ) ;
#34286=CYLINDRICAL_SURFACE ( 'NONE', #56070, 0.2500000000000002220 ) ;
#34294=CARTESIAN_POINT ( 'NONE',  ( 0.000000000000000000, 30.74999999999999289, 3.750000000000000000 ) ) ;
#34306=EDGE_CURVE ( 'NONE', #2782, #43549, #55000, .T. ) ;
#34330=EDGE_LOOP ( 'NONE', ( #49083, #48133, #14090 ) ) ;
#34355=CARTESIAN_POINT ( 'NONE',  ( -4.500000000000002665, 21.99999999999998579, 4.000000000000000000 ) ) ;
#34357=DIRECTION ( 'NONE',  ( 0.000000000000000000, -1.000000000000000000, 0.000000000000000000 ) ) ;
#34372=CIRCLE ( 'NONE', #65862, 0.2500000000000002220 ) ;
#34405=VERTEX_POINT ( 'NONE', #40137 ) ;
#34410=VERTEX_POINT ( 'NONE', #62927 ) ;
#34423=CARTESIAN_POINT ( 'NONE',  ( -25.00000000000000355, 37.00000000000000000, 3.750000000000000000 ) ) ;
#34444=DIRECTION ( 'NONE',  ( 9.376883653928687363E-17, 1.000000000000000000, 0.000000000000000000 ) ) ;
#34465=CIRCLE ( 'NONE', #65951, 0.2500000000000002220 ) ;
#34478=DIRECTION ( 'NONE',  ( 0.000000000000000000, 0.000000000000000000, -1.000000000000000000 ) ) ;
#34494=DIRECTION ( 'NONE',  ( 1.000000000000000000, 0.000000000000000000, 0.000000000000000000 ) ) ;
#34504=ORIENTED_EDGE ( 'NONE', *, *, #162, .T. ) ;
#34542=AXIS2_PLACEMENT_3D ( 'NONE', #60116, #66427, #66074 ) ;
#34546=DIRECTION ( 'NONE',  ( 1.000000000000000000, 0.000000000000000000, 0.000000000000000000 ) ) ;
#34561=LINE ( 'NONE', #7148, #55563 ) ;
#34594=DIRECTION ( 'NONE',  ( -1.000000000000000000, 0.000000000000000000, 0.000000000000000000 ) ) ;
#34611=CARTESIAN_POINT ( 'NONE',  ( 19.00000000000000000, 8.000000000000000000, 3.500000000000003997 ) ) ;
#34612=ORIENTED_EDGE ( 'NONE', *, *, #49261, .F. ) ;
#34623=DIRECTION ( 'NONE',  ( 1.000000000000000000, -0.000000000000000000, 0.000000000000000000 ) ) ;
#34638=EDGE_LOOP ( 'NONE', ( #7291, #7687, #31919, #48319 ) ) ;
#34652=SPHERICAL_SURFACE ( 'NONE', #51961, 0.2500000000000000000 ) ;
#34686=ADVANCED_FACE ( 'NONE', ( #57502 ), #36060, .T. ) ;
#34698=AXIS2_PLACEMENT_3D ( 'NONE', #63599, #31930, #42532 ) ;
#34722=DIRECTION ( 'NONE',  ( -1.000000000000000000, 0.000000000000000000, 0.000000000000000000 ) ) ;
#34753=DIRECTION ( 'NONE',  ( 1.000000000000000000, -0.000000000000000000, -0.000000000000000000 ) ) ;
#34767=DIRECTION ( 'NONE',  ( 0.000000000000000000, 1.000000000000000000, 0.000000000000000000 ) ) ;
#34783=ADVANCED_FACE ( 'NONE', ( #31169 ), #25902, .T. ) ;
#34831=LINE ( 'NONE', #14411, #30643 ) ;
#34844=ORIENTED_EDGE ( 'NONE', *, *, #42250, .T. ) ;
#34848=FACE_OUTER_BOUND ( 'NONE', #48823, .T. ) ;
#34857=EDGE_CURVE ( 'NONE', #69477, #39066, #43870, .T. ) ;
#34859=CARTESIAN_POINT ( 'NONE',  ( -17.75000000000000711, 31.24999999999999289, 4.000000000000000000 ) ) ;
#34866=CARTESIAN_POINT ( 'NONE',  ( -11.00000000000000000, 8.000000000000000000, 3.500000000000003997 ) ) ;
#34876=ORIENTED_EDGE ( 'NONE', *, *, #29203, .F. ) ;
#34899=DIRECTION ( 'NONE',  ( 0.000000000000000000, -1.000000000000000000, 0.000000000000000000 ) ) ;
#34945=ORIENTED_EDGE ( 'NONE', *, *, #12568, .F. ) ;
#34974=ORIENTED_EDGE ( 'NONE', *, *, #56948, .F. ) ;
#34981=DIRECTION ( 'NONE',  ( -0.000000000000000000, -0.000000000000000000, 1.000000000000000000 ) ) ;
#34982=VECTOR ( 'NONE', #59520, 1000.000000000000000 ) ;
#34988=VECTOR ( 'NONE', #40658, 1000.000000000000000 ) ;
#34990=CONICAL_SURFACE ( 'NONE', #62, 4.000000000000000000, 0.7853981633974482790 ) ;
#34994=VECTOR ( 'NONE', #45910, 1000.000000000000000 ) ;
#34997=VECTOR ( 'NONE', #65847, 1000.000000000000000 ) ;
#35000=CARTESIAN_POINT ( 'NONE',  ( -4.750000000000002665, 24.99999999999998579, -3.750000000000000000 ) ) ;
#35007=ORIENTED_EDGE ( 'NONE', *, *, #53544, .T. ) ;
#35017=EDGE_CURVE ( 'NONE', #30753, #53491, #2224, .T. ) ;
#35021=VERTEX_POINT ( 'NONE', #23755 ) ;
#35038=VECTOR ( 'NONE', #67706, 1000.000000000000000 ) ;
#35042=ORIENTED_EDGE ( 'NONE', *, *, #57166, .F. ) ;
#35045=DIRECTION ( 'NONE',  ( -1.000000000000000000, 0.000000000000000000, 0.000000000000000000 ) ) ;
#35070=DIRECTION ( 'NONE',  ( 0.000000000000000000, 0.000000000000000000, -1.000000000000000000 ) ) ;
#35075=ORIENTED_EDGE ( 'NONE', *, *, #55112, .F. ) ;
#35076=ORIENTED_EDGE ( 'NONE', *, *, #29879, .T. ) ;
#35082=EDGE_LOOP ( 'NONE', ( #32345, #53481, #55700, #67359 ) ) ;
#35085=VERTEX_POINT ( 'NONE', #48041 ) ;
#35101=CARTESIAN_POINT ( 'NONE',  ( -18.00000000000000711, 31.24999999999999289, -3.750000000000000000 ) ) ;
#35110=EDGE_CURVE ( 'NONE', #37037, #40236, #41705, .T. ) ;
#35124=DIRECTION ( 'NONE',  ( -1.000000000000000000, 0.000000000000000000, 0.000000000000000000 ) ) ;
#35130=EDGE_LOOP ( 'NONE', ( #50868, #65625, #32176, #25516 ) ) ;
#35142=DIRECTION ( 'NONE',  ( 0.000000000000000000, -0.000000000000000000, -1.000000000000000000 ) ) ;
#35148=AXIS2_PLACEMENT_3D ( 'NONE', #64382, #49251, #32703 ) ;
#35164=DIRECTION ( 'NONE',  ( 0.000000000000000000, 1.000000000000000000, 0.000000000000000000 ) ) ;
#35166=EDGE_LOOP ( 'NONE', ( #20832, #37372, #59093, #45758 ) ) ;
#35168=AXIS2_PLACEMENT_3D ( 'NONE', #10013, #52928, #4717 ) ;
#35189=VERTEX_POINT ( 'NONE', #10374 ) ;
#35190=CARTESIAN_POINT ( 'NONE',  ( -22.25000000000000711, 33.99999999999999289, 3.750000000000000000 ) ) ;
#35195=VERTEX_POINT ( 'NONE', #4345 ) ;
#35200=VECTOR ( 'NONE', #35861, 1000.000000000000000 ) ;
#35205=EDGE_CURVE ( 'NONE', #67406, #53491, #65314, .T. ) ;
#35207=DIRECTION ( 'NONE',  ( 0.000000000000000000, -0.000000000000000000, 1.000000000000000000 ) ) ;
#35253=DIRECTION ( 'NONE',  ( -0.000000000000000000, -0.000000000000000000, 1.000000000000000000 ) ) ;
#35258=EDGE_CURVE ( 'NONE', #1595, #58900, #22639, .T. ) ;
#35290=CARTESIAN_POINT ( 'NONE',  ( -18.25000000000000711, 33.74999999999999289, 4.000000000000000000 ) ) ;
#35291=ORIENTED_EDGE ( 'NONE', *, *, #38244, .T. ) ;
#35315=CARTESIAN_POINT ( 'NONE',  ( 0.000000000000000000, 0.000000000000000000, -4.000000000000000000 ) ) ;
#35350=ADVANCED_FACE ( 'NONE', ( #8554 ), #2866, .T. ) ;
#35360=ORIENTED_EDGE ( 'NONE', *, *, #35205, .F. ) ;
#35375=DIRECTION ( 'NONE',  ( -1.000000000000000000, 0.000000000000000000, 0.000000000000000000 ) ) ;
#35378=CARTESIAN_POINT ( 'NONE',  ( -9.250000000000003553, 27.74999999999998934, -3.750000000000000000 ) ) ;
#35381=CARTESIAN_POINT ( 'NONE',  ( -24.75000000000000355, 36.75000000000000000, -3.000000000000000000 ) ) ;
#35392=ORIENTED_EDGE ( 'NONE', *, *, #10768, .T. ) ;
#35465=ORIENTED_EDGE ( 'NONE', *, *, #31927, .F. ) ;
#35467=VECTOR ( 'NONE', #12608, 999.9999999999998863 ) ;
#35480=CARTESIAN_POINT ( 'NONE',  ( -4.250000000000001776, 21.74999999999998579, -3.750000000000000000 ) ) ;
#35481=ORIENTED_EDGE ( 'NONE', *, *, #52543, .F. ) ;
#35485=CARTESIAN_POINT ( 'NONE',  ( 4.750000000000002665, 24.74999999999998579, 3.750000000000000000 ) ) ;
#35509=CARTESIAN_POINT ( 'NONE',  ( 18.25000000000000711, 33.74999999999999289, 3.750000000000000000 ) ) ;
#35533=ADVANCED_FACE ( 'NONE', ( #45005 ), #12591, .T. ) ;
#35537=ORIENTED_EDGE ( 'NONE', *, *, #23333, .F. ) ;
#35551=EDGE_LOOP ( 'NONE', ( #52021, #55892, #28065, #56135 ) ) ;
#35598=DIRECTION ( 'NONE',  ( -0.000000000000000000, 0.000000000000000000, -1.000000000000000000 ) ) ;
#35646=EDGE_LOOP ( 'NONE', ( #922, #38779, #28852, #65269 ) ) ;
#35672=AXIS2_PLACEMENT_3D ( 'NONE', #56932, #29844, #41136 ) ;
#35748=FACE_OUTER_BOUND ( 'NONE', #66668, .T. ) ;
#35760=CARTESIAN_POINT ( 'NONE',  ( -13.50000000000000533, 30.74999999999999289, -3.750000000000000000 ) ) ;
#35781=AXIS2_PLACEMENT_3D ( 'NONE', #43340, #64387, #59425 ) ;
#35814=AXIS2_PLACEMENT_3D ( 'NONE', #27854, #1078, #22618 ) ;
#35855=VERTEX_POINT ( 'NONE', #41633 ) ;
#35861=DIRECTION ( 'NONE',  ( -1.000000000000000000, -0.000000000000000000, -0.000000000000000000 ) ) ;
#35929=ADVANCED_FACE ( 'NONE', ( #48663 ), #43402, .T. ) ;
#35950=CARTESIAN_POINT ( 'NONE',  ( -9.250000000000003553, 27.74999999999998934, 4.000000000000000000 ) ) ;
#35955=CARTESIAN_POINT ( 'NONE',  ( -18.00000000000000711, 33.99999999999999289, 4.000000000000000000 ) ) ;
#35977=ORIENTED_EDGE ( 'NONE', *, *, #22332, .T. ) ;
#35988=EDGE_LOOP ( 'NONE', ( #19381, #52748, #66962, #47970 ) ) ;
#36005=EDGE_LOOP ( 'NONE', ( #49663, #2115, #23665, #56149 ) ) ;
#36018=VERTEX_POINT ( 'NONE', #30243 ) ;
#36019=CARTESIAN_POINT ( 'NONE',  ( -22.25000000000000711, 34.24999999999999289, -3.750000000000000000 ) ) ;
#36027=VECTOR ( 'NONE', #32620, 1000.000000000000000 ) ;
#36036=( LENGTH_UNIT ( ) NAMED_UNIT ( * ) SI_UNIT ( .MILLI., .METRE. ) );
#36040=DIRECTION ( 'NONE',  ( 0.000000000000000000, 1.000000000000000000, 0.000000000000000000 ) ) ;
#36047=CIRCLE ( 'NONE', #33763, 0.2500000000000002220 ) ;
#36060=CYLINDRICAL_SURFACE ( 'NONE', #25933, 0.2500000000000002220 ) ;
#36065=EDGE_LOOP ( 'NONE', ( #26091, #7723, #59787 ) ) ;
#36084=EDGE_CURVE ( 'NONE', #52546, #58067, #59884, .T. ) ;
#36085=DIRECTION ( 'NONE',  ( 0.000000000000000000, 0.000000000000000000, -1.000000000000000000 ) ) ;
#36103=FACE_OUTER_BOUND ( 'NONE', #35166, .T. ) ;
#36145=EDGE_LOOP ( 'NONE', ( #63702, #4090, #69606, #22447 ) ) ;
#36160=EDGE_CURVE ( 'NONE', #19151, #43113, #26699, .T. ) ;
#36163=EDGE_CURVE ( 'NONE', #58121, #16885, #37501, .T. ) ;
#36184=AXIS2_PLACEMENT_3D ( 'NONE', #22590, #12709, #27825 ) ;
#36232=DIRECTION ( 'NONE',  ( -1.000000000000000000, 0.000000000000000000, 0.000000000000000000 ) ) ;
#36276=CARTESIAN_POINT ( 'NONE',  ( 24.75000000000000355, 36.75000000000000000, 4.000000000000000000 ) ) ;
#36312=CIRCLE ( 'NONE', #40759, 0.2500000000000002220 ) ;
#36321=DIRECTION ( 'NONE',  ( 0.000000000000000000, 0.000000000000000000, 1.000000000000000000 ) ) ;
#36328=CARTESIAN_POINT ( 'NONE',  ( 18.00000000000000711, 31.24999999999999289, 3.750000000000000000 ) ) ;
#36341=DIRECTION ( 'NONE',  ( -1.000000000000000000, 0.000000000000000000, 0.000000000000000000 ) ) ;
#36345=ORIENTED_EDGE ( 'NONE', *, *, #11612, .F. ) ;
#36370=CARTESIAN_POINT ( 'NONE',  ( -4.500000000000002665, 24.99999999999998579, 3.750000000000000000 ) ) ;
#36385=PLANE ( 'NONE',  #61261 ) ;
#36423=ADVANCED_FACE ( 'NONE', ( #28068 ), #6298, .T. ) ;
#36430=ADVANCED_FACE ( 'NONE', ( #16208 ), #59769, .T. ) ;
#36446=CARTESIAN_POINT ( 'NONE',  ( 25.00000000000000355, 36.75000000000000000, -3.750000000000000000 ) ) ;
#36462=ORIENTED_EDGE ( 'NONE', *, *, #66292, .T. ) ;
#36498=LINE ( 'NONE', #29787, #44983 ) ;
#36508=TOROIDAL_SURFACE ( 'NONE', #24104, 0.5000000000000000000, 0.2500000000000000000 ) ;
#36526=CIRCLE ( 'NONE', #6153, 0.2500000000000002220 ) ;
#36530=LINE ( 'NONE', #57952, #2835 ) ;
#36533=CARTESIAN_POINT ( 'NONE',  ( -17.75000000000000711, 31.24999999999999289, 3.750000000000000000 ) ) ;
#36540=LINE ( 'NONE', #63892, #65352 ) ;
#36618=CARTESIAN_POINT ( 'NONE',  ( 24.00000000000000000, 0.000000000000000000, 3.000000000000000000 ) ) ;
#36634=DIRECTION ( 'NONE',  ( -1.000000000000000000, 0.000000000000000000, 0.000000000000000000 ) ) ;
#36641=CARTESIAN_POINT ( 'NONE',  ( -24.00000000000000355, 36.75000000000000000, -3.000000000000000000 ) ) ;
#36642=ORIENTED_EDGE ( 'NONE', *, *, #3809, .T. ) ;
#36654=ORIENTED_EDGE ( 'NONE', *, *, #14642, .T. ) ;
#36655=VERTEX_POINT ( 'NONE', #41460 ) ;
#36660=FACE_OUTER_BOUND ( 'NONE', #29769, .T. ) ;
#36693=VERTEX_POINT ( 'NONE', #21347 ) ;
#36739=ORIENTED_EDGE ( 'NONE', *, *, #59631, .T. ) ;
#36816=ORIENTED_EDGE ( 'NONE', *, *, #21038, .F. ) ;
#36828=EDGE_CURVE ( 'NONE', #41176, #50598, #4957, .T. ) ;
#36848=DIRECTION ( 'NONE',  ( -0.000000000000000000, -0.000000000000000000, 1.000000000000000000 ) ) ;
#36859=ORIENTED_EDGE ( 'NONE', *, *, #52741, .T. ) ;
#36886=CARTESIAN_POINT ( 'NONE',  ( 22.25000000000000711, 34.24999999999999289, 4.000000000000000000 ) ) ;
#36894=DIRECTION ( 'NONE',  ( 1.000000000000000000, 0.000000000000000000, 0.000000000000000000 ) ) ;
#36928=ORIENTED_EDGE ( 'NONE', *, *, #47719, .F. ) ;
#36938=CARTESIAN_POINT ( 'NONE',  ( -8.750000000000001776, 24.99999999999998579, -3.750000000000000000 ) ) ;
#36939=AXIS2_PLACEMENT_3D ( 'NONE', #31557, #15425, #9790 ) ;
#36951=ORIENTED_EDGE ( 'NONE', *, *, #47378, .T. ) ;
#36955=CIRCLE ( 'NONE', #13296, 0.2500000000000002220 ) ;
#36976=CARTESIAN_POINT ( 'NONE',  ( -4.750000000000002665, 0.000000000000000000, 4.000000000000000000 ) ) ;
#36986=CARTESIAN_POINT ( 'NONE',  ( -4.750000000000002665, 22.24999999999998579, -3.750000000000000000 ) ) ;
#36994=ORIENTED_EDGE ( 'NONE', *, *, #16153, .F. ) ;
#37007=DIRECTION ( 'NONE',  ( -0.000000000000000000, 1.000000000000000000, -0.000000000000000000 ) ) ;
#37037=VERTEX_POINT ( 'NONE', #20946 ) ;
#37044=AXIS2_PLACEMENT_3D ( 'NONE', #19461, #40604, #9277 ) ;
#37152=ADVANCED_FACE ( 'NONE', ( #5771 ), #53635, .F. ) ;
#37155=VERTEX_POINT ( 'NONE', #26864 ) ;
#37180=ORIENTED_EDGE ( 'NONE', *, *, #59095, .F. ) ;
#37195=CARTESIAN_POINT ( 'NONE',  ( 25.00000000000000000, 0.000000000000000000, -3.000000000000000000 ) ) ;
#37291=EDGE_LOOP ( 'NONE', ( #39726, #36816, #59603, #227 ) ) ;
#37299=AXIS2_PLACEMENT_3D ( 'NONE', #57481, #67340, #51505 ) ;
#37305=ORIENTED_EDGE ( 'NONE', *, *, #13500, .F. ) ;
#37309=CIRCLE ( 'NONE', #38418, 0.2500000000000002220 ) ;
#37310=ADVANCED_FACE ( 'NONE', ( #65574 ), #18442, .T. ) ;
#37345=CARTESIAN_POINT ( 'NONE',  ( 22.25000000000000711, 34.24999999999999289, 4.000000000000000000 ) ) ;
#37352=CIRCLE ( 'NONE', #26038, 0.2500000000000002220 ) ;
#37362=AXIS2_PLACEMENT_3D ( 'NONE', #19412, #40910, #62328 ) ;
#37367=AXIS2_PLACEMENT_3D ( 'NONE', #64018, #15865, #16221 ) ;
#37371=DIRECTION ( 'NONE',  ( 0.000000000000000000, 0.000000000000000000, -1.000000000000000000 ) ) ;
#37372=ORIENTED_EDGE ( 'NONE', *, *, #61600, .F. ) ;
#37380=EDGE_CURVE ( 'NONE', #19151, #2325, #61190, .T. ) ;
#37400=EDGE_CURVE ( 'NONE', #9509, #22236, #28579, .T. ) ;
#37405=DIRECTION ( 'NONE',  ( -0.000000000000000000, -0.000000000000000000, 1.000000000000000000 ) ) ;
#37449=AXIS2_PLACEMENT_3D ( 'NONE', #4192, #69622, #15503 ) ;
#37462=CARTESIAN_POINT ( 'NONE',  ( 9.250000000000003553, 25.24999999999998934, -4.000000000000000000 ) ) ;
#37501=CIRCLE ( 'NONE', #23931, 4.499999999999976019 ) ;
#37505=DIRECTION ( 'NONE',  ( -0.000000000000000000, -0.000000000000000000, 1.000000000000000000 ) ) ;
#37527=ORIENTED_EDGE ( 'NONE', *, *, #7703, .T. ) ;
#37550=ADVANCED_FACE ( 'NONE', ( #41689 ), #46641, .T. ) ;
#37551=TOROIDAL_SURFACE ( 'NONE', #46533, 0.5000000000000000000, 0.2500000000000000000 ) ;
#37562=DIRECTION ( 'NONE',  ( 1.000000000000000000, -0.000000000000000000, 0.000000000000000000 ) ) ;
#37576=EDGE_LOOP ( 'NONE', ( #17804, #49882, #12486, #2296 ) ) ;
#37600=DIRECTION ( 'NONE',  ( 0.000000000000000000, 0.000000000000000000, -1.000000000000000000 ) ) ;
#37609=CARTESIAN_POINT ( 'NONE',  ( -18.25000000000000711, 33.99999999999999289, -3.750000000000000000 ) ) ;
#37620=CARTESIAN_POINT ( 'NONE',  ( -15.00000000000000000, 8.000000000000000000, 4.000000000000000000 ) ) ;
#37646=ORIENTED_EDGE ( 'NONE', *, *, #69661, .T. ) ;
#37693=VERTEX_POINT ( 'NONE', #5377 ) ;
#37769=CARTESIAN_POINT ( 'NONE',  ( 8.750000000000001776, 24.74999999999998579, 3.750000000000000000 ) ) ;
#37770=ORIENTED_EDGE ( 'NONE', *, *, #53158, .T. ) ;
#37803=VECTOR ( 'NONE', #12248, 1000.000000000000000 ) ;
#37806=CYLINDRICAL_SURFACE ( 'NONE', #66194, 1.000000000000000888 ) ;
#37820=CARTESIAN_POINT ( 'NONE',  ( -19.49999999999999645, 8.000000000000000000, 4.000000000000000000 ) ) ;
#37822=DIRECTION ( 'NONE',  ( 0.000000000000000000, 0.000000000000000000, -1.000000000000000000 ) ) ;
#37835=EDGE_LOOP ( 'NONE', ( #11773, #28077, #43891, #68849 ) ) ;
#37851=CARTESIAN_POINT ( 'NONE',  ( -13.75000000000000533, 30.74999999999999289, 4.000000000000000000 ) ) ;
#37867=CARTESIAN_POINT ( 'NONE',  ( 24.00000000000000000, 1.000000000000000000, -3.000000000000000000 ) ) ;
#37893=CIRCLE ( 'NONE', #18712, 0.2500000000000002220 ) ;
#37902=AXIS2_PLACEMENT_3D ( 'NONE', #48464, #23086, #21688 ) ;
#37911=CARTESIAN_POINT ( 'NONE',  ( 22.50000000000000711, 37.00000000000000000, 3.750000000000000000 ) ) ;
#37913=VERTEX_POINT ( 'NONE', #18034 ) ;
#37916=FACE_OUTER_BOUND ( 'NONE', #23950, .T. ) ;
#37921=CIRCLE ( 'NONE', #41273, 0.2500000000000002220 ) ;
#37922=CYLINDRICAL_SURFACE ( 'NONE', #6953, 0.2500000000000002220 ) ;
#37934=VERTEX_POINT ( 'NONE', #65530 ) ;
#37951=DIRECTION ( 'NONE',  ( -1.000000000000000000, 0.000000000000000000, 0.000000000000000000 ) ) ;
#37972=ADVANCED_FACE ( 'NONE', ( #54618 ), #47698, .F. ) ;
#37982=VECTOR ( 'NONE', #34066, 1000.000000000000000 ) ;
#38005=CIRCLE ( 'NONE', #14399, 0.2500000000000002220 ) ;
#38017=ADVANCED_FACE ( 'NONE', ( #30650 ), #37551, .T. ) ;
#38075=EDGE_CURVE ( 'NONE', #42335, #37934, #56618, .T. ) ;
#38106=ADVANCED_FACE ( 'NONE', ( #63710 ), #12771, .T. ) ;
#38121=DIRECTION ( 'NONE',  ( -1.000000000000000000, 0.000000000000000000, 0.000000000000000000 ) ) ;
#38126=DIRECTION ( 'NONE',  ( 0.000000000000000000, 0.000000000000000000, -1.000000000000000000 ) ) ;
#38137=CARTESIAN_POINT ( 'NONE',  ( 4.250000000000001776, 21.74999999999998579, 3.750000000000000000 ) ) ;
#38144=VECTOR ( 'NONE', #60744, 1000.000000000000000 ) ;
#38168=( NAMED_UNIT ( * ) PLANE_ANGLE_UNIT ( ) SI_UNIT ( $, .RADIAN. ) );
#38187=ORIENTED_EDGE ( 'NONE', *, *, #50693, .T. ) ;
#38190=AXIS2_PLACEMENT_3D ( 'NONE', #40509, #56664, #8491 ) ;
#38198=VECTOR ( 'NONE', #1806, 1000.000000000000000 ) ;
#38202=CIRCLE ( 'NONE', #55008, 1.000000000000000888 ) ;
#38244=EDGE_CURVE ( 'NONE', #1837, #16875, #31008, .T. ) ;
#38265=CARTESIAN_POINT ( 'NONE',  ( -22.75000000000000711, 34.24999999999999289, -3.750000000000000000 ) ) ;
#38275=ORIENTED_EDGE ( 'NONE', *, *, #12151, .T. ) ;
#38318=PLANE ( 'NONE',  #28176 ) ;
#38322=EDGE_LOOP ( 'NONE', ( #20429, #22886, #57593, #51715 ) ) ;
#38353=CARTESIAN_POINT ( 'NONE',  ( -4.750000000000002665, 24.74999999999998579, -3.750000000000000000 ) ) ;
#38376=DIRECTION ( 'NONE',  ( 0.000000000000000000, 1.000000000000000000, 0.000000000000000000 ) ) ;
#38404=AXIS2_PLACEMENT_3D ( 'NONE', #55227, #17301, #38761 ) ;
#38418=AXIS2_PLACEMENT_3D ( 'NONE', #60368, #65997, #33986 ) ;
#38442=VERTEX_POINT ( 'NONE', #66849 ) ;
#38484=DIRECTION ( 'NONE',  ( 0.000000000000000000, 0.000000000000000000, -1.000000000000000000 ) ) ;
#38494=DIRECTION ( 'NONE',  ( -0.000000000000000000, 0.000000000000000000, -1.000000000000000000 ) ) ;
#38521=FACE_OUTER_BOUND ( 'NONE', #40746, .T. ) ;
#38522=LINE ( 'NONE', #64152, #43280 ) ;
#38540=LINE ( 'NONE', #54654, #14353 ) ;
#38545=ORIENTED_EDGE ( 'NONE', *, *, #38580, .T. ) ;
#38560=ORIENTED_EDGE ( 'NONE', *, *, #14374, .F. ) ;
#38580=EDGE_CURVE ( 'NONE', #61196, #31124, #69271, .T. ) ;
#38599=VECTOR ( 'NONE', #21100, 1000.000000000000000 ) ;
#38637=CARTESIAN_POINT ( 'NONE',  ( 18.25000000000000711, 33.99999999999999289, -3.750000000000000000 ) ) ;
#38684=VERTEX_POINT ( 'NONE', #21764 ) ;
#38691=ORIENTED_EDGE ( 'NONE', *, *, #59631, .F. ) ;
#38750=DIRECTION ( 'NONE',  ( -1.000000000000000000, 0.000000000000000000, 0.000000000000000000 ) ) ;
#38761=DIRECTION ( 'NONE',  ( -1.000000000000000000, 0.000000000000000000, -0.000000000000000000 ) ) ;
#38762=CARTESIAN_POINT ( 'NONE',  ( -22.25000000000000711, 33.74999999999999289, 3.750000000000000000 ) ) ;
#38779=ORIENTED_EDGE ( 'NONE', *, *, #5292, .F. ) ;
#38789=DIRECTION ( 'NONE',  ( -1.000000000000000000, 0.000000000000000000, 0.000000000000000000 ) ) ;
#38795=DIRECTION ( 'NONE',  ( 9.376883653928687363E-17, -1.000000000000000000, 0.000000000000000000 ) ) ;
#38807=CARTESIAN_POINT ( 'NONE',  ( -8.750000000000001776, 25.24999999999998934, 4.000000000000000000 ) ) ;
#38838=FACE_OUTER_BOUND ( 'NONE', #8915, .T. ) ;
#38862=( NAMED_UNIT ( * ) SI_UNIT ( $, .STERADIAN. ) SOLID_ANGLE_UNIT ( ) );
#38885=VERTEX_POINT ( 'NONE', #52926 ) ;
#38893=ADVANCED_FACE ( 'NONE', ( #53602 ), #5062, .F. ) ;
#38905=DIRECTION ( 'NONE',  ( 1.000000000000000000, -0.000000000000000000, 0.000000000000000000 ) ) ;
#38920=AXIS2_PLACEMENT_3D ( 'NONE', #34240, #12768, #2521 ) ;
#38921=CIRCLE ( 'NONE', #29889, 0.2500000000000002220 ) ;
#38930=DIRECTION ( 'NONE',  ( -1.000000000000000000, 0.000000000000000000, 0.000000000000000000 ) ) ;
#38952=ORIENTED_EDGE ( 'NONE', *, *, #21926, .F. ) ;
#38969=EDGE_CURVE ( 'NONE', #8380, #31530, #41271, .T. ) ;
#38976=ADVANCED_FACE ( 'NONE', ( #46566 ), #66942, .T. ) ;
#38984=CARTESIAN_POINT ( 'NONE',  ( 0.000000000000000000, 24.74999999999998579, 4.000000000000000000 ) ) ;
#39018=EDGE_LOOP ( 'NONE', ( #30199, #63798, #64608, #47703 ) ) ;
#39043=LINE ( 'NONE', #33384, #45616 ) ;
#39056=DIRECTION ( 'NONE',  ( 1.000000000000000000, 0.000000000000000000, 0.000000000000000000 ) ) ;
#39060=EDGE_LOOP ( 'NONE', ( #65301, #57669, #41517, #32265 ) ) ;
#39062=ORIENTED_EDGE ( 'NONE', *, *, #62983, .F. ) ;
#39066=VERTEX_POINT ( 'NONE', #46914 ) ;
#39100=CARTESIAN_POINT ( 'NONE',  ( -22.50000000000000711, 37.00000000000000000, 3.750000000000000000 ) ) ;
#39110=EDGE_CURVE ( 'NONE', #69641, #47699, #52168, .T. ) ;
#39112=ORIENTED_EDGE ( 'NONE', *, *, #59363, .F. ) ;
#39133=ORIENTED_EDGE ( 'NONE', *, *, #15739, .T. ) ;
#39136=VERTEX_POINT ( 'NONE', #16611 ) ;
#39145=DIRECTION ( 'NONE',  ( -1.000000000000000000, 0.000000000000000000, 0.000000000000000000 ) ) ;
#39186=EDGE_CURVE ( 'NONE', #35021, #9250, #337, .T. ) ;
#39187=EDGE_CURVE ( 'NONE', #54390, #42335, #10618, .T. ) ;
#39189=LINE ( 'NONE', #22279, #38198 ) ;
#39201=CARTESIAN_POINT ( 'NONE',  ( 13.25000000000000355, 27.99999999999998934, -4.000000000000000000 ) ) ;
#39221=ADVANCED_FACE ( 'NONE', ( #49639 ), #45090, .T. ) ;
#39246=VECTOR ( 'NONE', #68800, 1000.000000000000000 ) ;
#39267=DIRECTION ( 'NONE',  ( 0.000000000000000000, 0.000000000000000000, 1.000000000000000000 ) ) ;
#39278=ORIENTED_EDGE ( 'NONE', *, *, #62341, .F. ) ;
#39316=EDGE_LOOP ( 'NONE', ( #67038, #61264 ) ) ;
#39318=LINE ( 'NONE', #43915, #45398 ) ;
#39342=LINE ( 'NONE', #24164, #38144 ) ;
#39403=ORIENTED_EDGE ( 'NONE', *, *, #18435, .T. ) ;
#39407=DIRECTION ( 'NONE',  ( -1.000000000000000000, 0.000000000000000000, 0.000000000000000000 ) ) ;
#39418=VECTOR ( 'NONE', #69496, 1000.000000000000000 ) ;
#39430=DIRECTION ( 'NONE',  ( -1.000000000000000000, 0.000000000000000000, 0.000000000000000000 ) ) ;
#39455=CARTESIAN_POINT ( 'NONE',  ( 13.25000000000000355, 27.74999999999998934, -4.000000000000000000 ) ) ;
#39472=CARTESIAN_POINT ( 'NONE',  ( 0.000000000000000000, 27.74999999999998934, 3.750000000000000000 ) ) ;
#39473=EDGE_LOOP ( 'NONE', ( #19871, #64093, #48741, #46188 ) ) ;
#39498=CIRCLE ( 'NONE', #18079, 0.2500000000000002220 ) ;
#39533=CARTESIAN_POINT ( 'NONE',  ( -15.00000000000000000, 8.000000000000000000, 3.500000000000003997 ) ) ;
#39535=DIRECTION ( 'NONE',  ( 0.000000000000000000, 0.000000000000000000, 1.000000000000000000 ) ) ;
#39542=DIRECTION ( 'NONE',  ( -1.000000000000000000, 0.000000000000000000, 0.000000000000000000 ) ) ;
#39559=AXIS2_PLACEMENT_3D ( 'NONE', #15513, #15856, #48223 ) ;
#39568=CIRCLE ( 'NONE', #9221, 0.2500000000000002220 ) ;
#39589=DIRECTION ( 'NONE',  ( 0.000000000000000000, 0.000000000000000000, -1.000000000000000000 ) ) ;
#39596=EDGE_LOOP ( 'NONE', ( #63876, #39403, #35042, #59118 ) ) ;
#39598=FACE_OUTER_BOUND ( 'NONE', #35082, .T. ) ;
#39621=EDGE_CURVE ( 'NONE', #12723, #63323, #18663, .T. ) ;
#39627=LINE ( 'NONE', #67367, #32211 ) ;
#39633=CARTESIAN_POINT ( 'NONE',  ( 8.750000000000001776, 24.99999999999998579, 3.750000000000000000 ) ) ;
#39653=ORIENTED_EDGE ( 'NONE', *, *, #53158, .F. ) ;
#39664=AXIS2_PLACEMENT_3D ( 'NONE', #29802, #68483, #9047 ) ;
#39699=VERTEX_POINT ( 'NONE', #27709 ) ;
#39724=CARTESIAN_POINT ( 'NONE',  ( -15.00000000000000000, 8.000000000000000000, 4.000000000000000000 ) ) ;
#39726=ORIENTED_EDGE ( 'NONE', *, *, #22009, .T. ) ;
#39728=LINE ( 'NONE', #33714, #8243 ) ;
#39760=FACE_OUTER_BOUND ( 'NONE', #39596, .T. ) ;
#39779=DIRECTION ( 'NONE',  ( -0.000000000000000000, -0.000000000000000000, 1.000000000000000000 ) ) ;
#39806=DIRECTION ( 'NONE',  ( -1.000000000000000000, 0.000000000000000000, 0.000000000000000000 ) ) ;
#39816=CARTESIAN_POINT ( 'NONE',  ( -25.00000000000000355, 36.75000000000000000, 3.000000000000000000 ) ) ;
#39829=CARTESIAN_POINT ( 'NONE',  ( 9.000000000000003553, 25.24999999999998934, -3.750000000000000000 ) ) ;
#39839=DIRECTION ( 'NONE',  ( -1.000000000000000000, 0.000000000000000000, 0.000000000000000000 ) ) ;
#39942=AXIS2_PLACEMENT_3D ( 'NONE', #33806, #34164, #55620 ) ;
#39954=DIRECTION ( 'NONE',  ( 0.000000000000000000, -1.000000000000000000, 0.000000000000000000 ) ) ;
#39961=EDGE_CURVE ( 'NONE', #20746, #39066, #34372, .T. ) ;
#39999=FACE_OUTER_BOUND ( 'NONE', #16948, .T. ) ;
#40009=CARTESIAN_POINT ( 'NONE',  ( -18.25000000000000711, 33.74999999999999289, 3.750000000000000000 ) ) ;
#40026=MECHANICAL_DESIGN_GEOMETRIC_PRESENTATION_REPRESENTATION('',(#69216),#600);
#40037=LINE ( 'NONE', #29429, #18526 ) ;
#40058=LINE ( 'NONE', #13268, #61222 ) ;
#40109=DIRECTION ( 'NONE',  ( 0.000000000000000000, -1.000000000000000000, 0.000000000000000000 ) ) ;
#40137=CARTESIAN_POINT ( 'NONE',  ( 18.25000000000000711, 31.24999999999999289, -4.000000000000000000 ) ) ;
#40140=VERTEX_POINT ( 'NONE', #20658 ) ;
#40169=ORIENTED_EDGE ( 'NONE', *, *, #1038, .T. ) ;
#40172=CARTESIAN_POINT ( 'NONE',  ( 9.250000000000003553, 27.74999999999998934, -4.000000000000000000 ) ) ;
#40174=VERTEX_POINT ( 'NONE', #49472 ) ;
#40208=CIRCLE ( 'NONE', #57015, 0.2500000000000002220 ) ;
#40214=EDGE_CURVE ( 'NONE', #55377, #35021, #52427, .T. ) ;
#40217=DIRECTION ( 'NONE',  ( 1.000000000000000000, 0.000000000000000000, 0.000000000000000000 ) ) ;
#40223=ORIENTED_EDGE ( 'NONE', *, *, #20702, .F. ) ;
#40236=VERTEX_POINT ( 'NONE', #54376 ) ;
#40248=ORIENTED_EDGE ( 'NONE', *, *, #4675, .T. ) ;
#40249=CARTESIAN_POINT ( 'NONE',  ( 9.250000000000003553, 25.24999999999998934, 4.000000000000000000 ) ) ;
#40253=FACE_OUTER_BOUND ( 'NONE', #6873, .T. ) ;
#40276=DIRECTION ( 'NONE',  ( -1.000000000000000000, 0.000000000000000000, 0.000000000000000000 ) ) ;
#40280=DIRECTION ( 'NONE',  ( 0.000000000000000000, -1.000000000000000000, -0.000000000000000000 ) ) ;
#40286=EDGE_CURVE ( 'NONE', #50552, #54902, #37893, .T. ) ;
#40297=AXIS2_PLACEMENT_3D ( 'NONE', #4700, #63455, #4322 ) ;
#40330=LINE ( 'NONE', #40689, #42047 ) ;
#40333=ADVANCED_FACE ( 'NONE', ( #13908 ), #2608, .T. ) ;
#40366=EDGE_CURVE ( 'NONE', #5580, #52546, #39627, .T. ) ;
#40377=TOROIDAL_SURFACE ( 'NONE', #37044, 0.5000000000000000000, 0.2500000000000000000 ) ;
#40418=AXIS2_PLACEMENT_3D ( 'NONE', #23296, #65866, #56332 ) ;
#40421=DIRECTION ( 'NONE',  ( -1.000000000000000000, 0.000000000000000000, 0.000000000000000000 ) ) ;
#40423=ORIENTED_EDGE ( 'NONE', *, *, #19996, .F. ) ;
#40439=CARTESIAN_POINT ( 'NONE',  ( 18.00000000000000711, 30.99999999999999289, 4.000000000000000000 ) ) ;
#40441=DIRECTION ( 'NONE',  ( 1.000000000000000000, -0.000000000000000000, -0.000000000000000000 ) ) ;
#40446=EDGE_CURVE ( 'NONE', #65737, #40140, #34465, .T. ) ;
#40509=CARTESIAN_POINT ( 'NONE',  ( 18.25000000000000711, 33.74999999999999289, -3.750000000000000000 ) ) ;
#40536=DIRECTION ( 'NONE',  ( -1.000000000000000000, 0.000000000000000000, 0.000000000000000000 ) ) ;
#40553=DIRECTION ( 'NONE',  ( 0.000000000000000000, 1.000000000000000000, 0.000000000000000000 ) ) ;
#40558=DIRECTION ( 'NONE',  ( 1.000000000000000000, 0.000000000000000000, 0.000000000000000000 ) ) ;
#40566=ORIENTED_EDGE ( 'NONE', *, *, #24233, .F. ) ;
#40572=ORIENTED_EDGE ( 'NONE', *, *, #44127, .F. ) ;
#40576=AXIS2_PLACEMENT_3D ( 'NONE', #31937, #26638, #9817 ) ;
#40585=FACE_OUTER_BOUND ( 'NONE', #10186, .T. ) ;
#40592=CARTESIAN_POINT ( 'NONE',  ( 4.250000000000001776, 21.74999999999998579, -4.000000000000000000 ) ) ;
#40604=DIRECTION ( 'NONE',  ( 0.000000000000000000, 0.000000000000000000, -1.000000000000000000 ) ) ;
#40611=DIRECTION ( 'NONE',  ( 0.000000000000000000, 1.000000000000000000, 0.000000000000000000 ) ) ;
#40623=CARTESIAN_POINT ( 'NONE',  ( 18.25000000000000711, 33.74999999999999289, 4.000000000000000000 ) ) ;
#40625=DIRECTION ( 'NONE',  ( -1.000000000000000000, 0.000000000000000000, 0.000000000000000000 ) ) ;
#40647=CARTESIAN_POINT ( 'NONE',  ( -22.50000000000000711, 33.99999999999999289, 3.750000000000000000 ) ) ;
#40658=DIRECTION ( 'NONE',  ( -1.000000000000000000, 0.000000000000000000, 0.000000000000000000 ) ) ;
#40685=LINE ( 'NONE', #67744, #12008 ) ;
#40688=DIRECTION ( 'NONE',  ( 0.000000000000000000, 1.000000000000000000, 0.000000000000000000 ) ) ;
#40689=CARTESIAN_POINT ( 'NONE',  ( 22.25000000000000711, 33.99999999999999289, -4.000000000000000000 ) ) ;
#40711=VECTOR ( 'NONE', #2168, 1000.000000000000000 ) ;
#40713=ADVANCED_FACE ( 'NONE', ( #50342 ), #50012, .F. ) ;
#40728=CIRCLE ( 'NONE', #9286, 0.2500000000000002220 ) ;
#40746=EDGE_LOOP ( 'NONE', ( #141, #61323, #57969 ) ) ;
#40747=AXIS2_PLACEMENT_3D ( 'NONE', #41134, #30879, #47830 ) ;
#40759=AXIS2_PLACEMENT_3D ( 'NONE', #25675, #57713, #56671 ) ;
#40764=EDGE_LOOP ( 'NONE', ( #900, #43597, #40887, #46206 ) ) ;
#40771=AXIS2_PLACEMENT_3D ( 'NONE', #57980, #53393, #69224 ) ;
#40799=DIRECTION ( 'NONE',  ( -5.782411586589351722E-16, -1.000000000000000000, 0.000000000000000000 ) ) ;
#40820=DIRECTION ( 'NONE',  ( -1.000000000000000000, 0.000000000000000000, 0.000000000000000000 ) ) ;
#40828=DIRECTION ( 'NONE',  ( -1.000000000000000000, 0.000000000000000000, 0.000000000000000000 ) ) ;
#40829=DIRECTION ( 'NONE',  ( -1.000000000000000000, 0.000000000000000000, 0.000000000000000000 ) ) ;
#40842=DIRECTION ( 'NONE',  ( 0.000000000000000000, 1.000000000000000000, 0.000000000000000000 ) ) ;
#40843=AXIS2_PLACEMENT_3D ( 'NONE', #24620, #21801, #16550 ) ;
#40861=DIRECTION ( 'NONE',  ( -0.7071067811865474617, 8.659560562354932858E-17, 0.7071067811865474617 ) ) ;
#40869=AXIS2_PLACEMENT_3D ( 'NONE', #54069, #53056, #49172 ) ;
#40887=ORIENTED_EDGE ( 'NONE', *, *, #66292, .F. ) ;
#40910=DIRECTION ( 'NONE',  ( 1.000000000000000000, 0.000000000000000000, 0.000000000000000000 ) ) ;
#40950=VECTOR ( 'NONE', #53289, 999.9999999999998863 ) ;
#40952=CYLINDRICAL_SURFACE ( 'NONE', #31876, 0.2500000000000002220 ) ;
#40963=LINE ( 'NONE', #62017, #40711 ) ;
#40971=DIRECTION ( 'NONE',  ( 1.000000000000000000, -0.000000000000000000, 0.000000000000000000 ) ) ;
#40988=DIRECTION ( 'NONE',  ( 0.000000000000000000, 0.000000000000000000, -1.000000000000000000 ) ) ;
#41001=DIRECTION ( 'NONE',  ( 0.000000000000000000, 1.000000000000000000, -0.000000000000000000 ) ) ;
#41016=ORIENTED_EDGE ( 'NONE', *, *, #38075, .T. ) ;
#41033=CIRCLE ( 'NONE', #5046, 0.2500000000000002220 ) ;
#41061=DIRECTION ( 'NONE',  ( 0.000000000000000000, -1.000000000000000000, 0.000000000000000000 ) ) ;
#41064=DIRECTION ( 'NONE',  ( 0.000000000000000000, 0.000000000000000000, -1.000000000000000000 ) ) ;
#41065=LINE ( 'NONE', #61764, #53971 ) ;
#41088=EDGE_CURVE ( 'NONE', #33026, #65139, #23180, .T. ) ;
#41092=ADVANCED_FACE ( 'NONE', ( #55522 ), #17238, .T. ) ;
#41097=CARTESIAN_POINT ( 'NONE',  ( 18.00000000000000711, 33.74999999999999289, 4.000000000000000000 ) ) ;
#41098=EDGE_CURVE ( 'NONE', #68401, #37913, #42452, .T. ) ;
#41120=VERTEX_POINT ( 'NONE', #12950 ) ;
#41134=CARTESIAN_POINT ( 'NONE',  ( 13.25000000000000355, 28.24999999999998934, -3.750000000000000000 ) ) ;
#41136=DIRECTION ( 'NONE',  ( -1.000000000000000000, 0.000000000000000000, 0.000000000000000000 ) ) ;
#41149=EDGE_CURVE ( 'NONE', #48589, #61721, #60104, .T. ) ;
#41150=LINE ( 'NONE', #24917, #16759 ) ;
#41171=EDGE_CURVE ( 'NONE', #58314, #58151, #44711, .T. ) ;
#41174=COLOUR_RGB ( '', 0.72549020, 0.75294118, 0.79215686) ;
#41176=VERTEX_POINT ( 'NONE', #45012 ) ;
#41183=DIRECTION ( 'NONE',  ( 0.000000000000000000, -0.000000000000000000, -1.000000000000000000 ) ) ;
#41216=EDGE_LOOP ( 'NONE', ( #47902, #67195, #63203, #19600 ) ) ;
#41238=CARTESIAN_POINT ( 'NONE',  ( 22.75000000000000711, 34.24999999999999289, -4.000000000000000000 ) ) ;
#41271=LINE ( 'NONE', #14492, #23082 ) ;
#41273=AXIS2_PLACEMENT_3D ( 'NONE', #35381, #56836, #67375 ) ;
#41307=EDGE_CURVE ( 'NONE', #66039, #35189, #8765, .T. ) ;
#41310=LINE ( 'NONE', #30704, #34982 ) ;
#41316=CIRCLE ( 'NONE', #55896, 0.2500000000000002220 ) ;
#41320=CARTESIAN_POINT ( 'NONE',  ( 18.25000000000000711, 33.74999999999999289, 3.750000000000000000 ) ) ;
#41321=ORIENTED_EDGE ( 'NONE', *, *, #47634, .T. ) ;
#41332=ADVANCED_FACE ( 'NONE', ( #60328 ), #66298, .T. ) ;
#41362=LINE ( 'NONE', #4354, #40950 ) ;
#41365=DIRECTION ( 'NONE',  ( 0.000000000000000000, 0.000000000000000000, -1.000000000000000000 ) ) ;
#41366=EDGE_CURVE ( 'NONE', #30380, #12003, #57889, .T. ) ;
#41376=CARTESIAN_POINT ( 'NONE',  ( -25.00000000000000355, 37.00000000000000000, 4.000000000000000000 ) ) ;
#41406=DIRECTION ( 'NONE',  ( -1.000000000000000000, 0.000000000000000000, 0.000000000000000000 ) ) ;
#41429=AXIS2_PLACEMENT_3D ( 'NONE', #23288, #2465, #12363 ) ;
#41440=AXIS2_PLACEMENT_3D ( 'NONE', #25277, #68202, #19980 ) ;
#41442=DIRECTION ( 'NONE',  ( 0.000000000000000000, 0.000000000000000000, -1.000000000000000000 ) ) ;
#41447=DIRECTION ( 'NONE',  ( -1.000000000000000000, 0.000000000000000000, 0.000000000000000000 ) ) ;
#41460=CARTESIAN_POINT ( 'NONE',  ( -18.25000000000000711, 33.99999999999999289, 3.750000000000000000 ) ) ;
#41466=CIRCLE ( 'NONE', #34698, 0.2500000000000002220 ) ;
#41469=DIRECTION ( 'NONE',  ( 0.000000000000000000, 0.000000000000000000, -1.000000000000000000 ) ) ;
#41470=CARTESIAN_POINT ( 'NONE',  ( 4.750000000000002665, 24.74999999999998579, -4.000000000000000000 ) ) ;
#41491=CARTESIAN_POINT ( 'NONE',  ( -13.75000000000000533, 30.99999999999999289, 4.000000000000000000 ) ) ;
#41501=EDGE_LOOP ( 'NONE', ( #58896, #69228, #40423, #31174 ) ) ;
#41505=VECTOR ( 'NONE', #43684, 1000.000000000000000 ) ;
#41517=ORIENTED_EDGE ( 'NONE', *, *, #67171, .T. ) ;
#41552=AXIS2_PLACEMENT_3D ( 'NONE', #6102, #18401, #54959 ) ;
#41584=ORIENTED_EDGE ( 'NONE', *, *, #63999, .F. ) ;
#41618=ORIENTED_EDGE ( 'NONE', *, *, #47378, .F. ) ;
#41633=CARTESIAN_POINT ( 'NONE',  ( -13.25000000000000355, 27.74999999999998934, -4.000000000000000000 ) ) ;
#41667=DIRECTION ( 'NONE',  ( 0.000000000000000000, 0.000000000000000000, 1.000000000000000000 ) ) ;
#41677=CARTESIAN_POINT ( 'NONE',  ( 13.25000000000000355, 27.74999999999998934, 3.750000000000000000 ) ) ;
#41689=FACE_OUTER_BOUND ( 'NONE', #60969, .T. ) ;
#41695=CARTESIAN_POINT ( 'NONE',  ( -4.750000000000002665, 24.74999999999998579, -4.000000000000000000 ) ) ;
#41705=LINE ( 'NONE', #32154, #56318 ) ;
#41708=ORIENTED_EDGE ( 'NONE', *, *, #49261, .T. ) ;
#41713=ORIENTED_EDGE ( 'NONE', *, *, #41915, .F. ) ;
#41716=ORIENTED_EDGE ( 'NONE', *, *, #52659, .T. ) ;
#41748=ADVANCED_FACE ( 'NONE', ( #24718 ), #14908, .T. ) ;
#41755=VECTOR ( 'NONE', #54194, 1000.000000000000000 ) ;
#41798=EDGE_LOOP ( 'NONE', ( #61397, #28610, #27314, #63328 ) ) ;
#41843=AXIS2_PLACEMENT_3D ( 'NONE', #60076, #11538, #54099 ) ;
#41884=ORIENTED_EDGE ( 'NONE', *, *, #62341, .T. ) ;
#41906=EDGE_CURVE ( 'NONE', #58037, #12723, #11, .T. ) ;
#41915=EDGE_CURVE ( 'NONE', #9166, #8380, #14443, .T. ) ;
#41928=ADVANCED_FACE ( 'NONE', ( #17683 ), #44778, .F. ) ;
#41931=VERTEX_POINT ( 'NONE', #60541 ) ;
#41932=CARTESIAN_POINT ( 'NONE',  ( 22.25000000000000711, 34.24999999999999289, -3.750000000000000000 ) ) ;
#41941=DIRECTION ( 'NONE',  ( 0.000000000000000000, 0.000000000000000000, -1.000000000000000000 ) ) ;
#41977=CARTESIAN_POINT ( 'NONE',  ( 22.50000000000000711, 33.99999999999999289, 3.750000000000000000 ) ) ;
#42031=DIRECTION ( 'NONE',  ( 0.000000000000000000, 0.000000000000000000, -1.000000000000000000 ) ) ;
#42047=VECTOR ( 'NONE', #7603, 1000.000000000000000 ) ;
#42065=VERTEX_POINT ( 'NONE', #34866 ) ;
#42075=EDGE_CURVE ( 'NONE', #41931, #61564, #9799, .T. ) ;
#42096=CARTESIAN_POINT ( 'NONE',  ( -18.00000000000000711, 33.74999999999999289, 3.750000000000000000 ) ) ;
#42105=CARTESIAN_POINT ( 'NONE',  ( -25.00000000000000355, 37.00000000000000000, 3.000000000000000000 ) ) ;
#42117=CARTESIAN_POINT ( 'NONE',  ( 4.250000000000001776, 21.74999999999998579, -3.750000000000000000 ) ) ;
#42155=VECTOR ( 'NONE', #22038, 1000.000000000000000 ) ;
#42179=AXIS2_PLACEMENT_3D ( 'NONE', #5807, #32920, #17109 ) ;
#42222=AXIS2_PLACEMENT_3D ( 'NONE', #51111, #40217, #63026 ) ;
#42231=CARTESIAN_POINT ( 'NONE',  ( -9.250000000000003553, 0.000000000000000000, 3.750000000000000000 ) ) ;
#42250=EDGE_CURVE ( 'NONE', #55864, #50411, #4317, .T. ) ;
#42267=DIRECTION ( 'NONE',  ( -0.000000000000000000, -0.000000000000000000, 1.000000000000000000 ) ) ;
#42288=DIRECTION ( 'NONE',  ( 0.000000000000000000, -1.000000000000000000, 0.000000000000000000 ) ) ;
#42325=ORIENTED_EDGE ( 'NONE', *, *, #4109, .T. ) ;
#42335=VERTEX_POINT ( 'NONE', #2975 ) ;
#42351=AXIS2_PLACEMENT_3D ( 'NONE', #47891, #69290, #21083 ) ;
#42366=ORIENTED_EDGE ( 'NONE', *, *, #32884, .T. ) ;
#42388=DIRECTION ( 'NONE',  ( 0.000000000000000000, 0.000000000000000000, -1.000000000000000000 ) ) ;
#42417=ORIENTED_EDGE ( 'NONE', *, *, #57437, .T. ) ;
#42426=ORIENTED_EDGE ( 'NONE', *, *, #43793, .F. ) ;
#42447=DIRECTION ( 'NONE',  ( -1.000000000000000000, 0.000000000000000000, 0.000000000000000000 ) ) ;
#42449=LINE ( 'NONE', #67753, #65478 ) ;
#42452=CIRCLE ( 'NONE', #3018, 0.2500000000000002220 ) ;
#42455=DIRECTION ( 'NONE',  ( 0.000000000000000000, 1.000000000000000000, 0.000000000000000000 ) ) ;
#42460=ADVANCED_FACE ( 'NONE', ( #23788 ), #24464, .F. ) ;
#42462=CARTESIAN_POINT ( 'NONE',  ( 4.750000000000002665, 24.99999999999998579, 3.750000000000000000 ) ) ;
#42470=UNCERTAINTY_MEASURE_WITH_UNIT (LENGTH_MEASURE( 1.000000000000000082E-05 ), #67001, 'distance_accuracy_value', 'NONE');
#42532=DIRECTION ( 'NONE',  ( -1.000000000000000000, 0.000000000000000000, 0.000000000000000000 ) ) ;
#42556=AXIS2_PLACEMENT_3D ( 'NONE', #59868, #6395, #65849 ) ;
#42558=CARTESIAN_POINT ( 'NONE',  ( 13.25000000000000355, 28.24999999999998934, 3.750000000000000000 ) ) ;
#42570=LINE ( 'NONE', #8789, #65544 ) ;
#42571=ORIENTED_EDGE ( 'NONE', *, *, #22332, .F. ) ;
#42595=DIRECTION ( 'NONE',  ( 0.000000000000000000, 0.000000000000000000, -1.000000000000000000 ) ) ;
#42604=VECTOR ( 'NONE', #45897, 1000.000000000000114 ) ;
#42609=CYLINDRICAL_SURFACE ( 'NONE', #37367, 0.2500000000000002220 ) ;
#42629=CIRCLE ( 'NONE', #12223, 0.5000000000000004441 ) ;
#42652=CARTESIAN_POINT ( 'NONE',  ( 13.25000000000000355, 27.74999999999998934, -3.750000000000000000 ) ) ;
#42698=EDGE_CURVE ( 'NONE', #43549, #58151, #60519, .T. ) ;
#42710=VECTOR ( 'NONE', #10393, 1000.000000000000000 ) ;
#42731=EDGE_LOOP ( 'NONE', ( #34134, #46902, #15917, #22932 ) ) ;
#42738=DIRECTION ( 'NONE',  ( 0.000000000000000000, 0.000000000000000000, 1.000000000000000000 ) ) ;
#42757=DIRECTION ( 'NONE',  ( 0.000000000000000000, -1.000000000000000000, 0.000000000000000000 ) ) ;
#42761=CONICAL_SURFACE ( 'NONE', #2211, 4.000000000000000000, 0.7853981633974482790 ) ;
#42769=DIRECTION ( 'NONE',  ( 1.000000000000000000, -0.000000000000000000, 0.000000000000000000 ) ) ;
#42829=DIRECTION ( 'NONE',  ( -1.000000000000000000, 0.000000000000000000, 0.000000000000000000 ) ) ;
#42832=DIRECTION ( 'NONE',  ( -1.000000000000000000, 0.000000000000000000, 0.000000000000000000 ) ) ;
#42840=AXIS2_PLACEMENT_3D ( 'NONE', #59977, #7217, #49786 ) ;
#42843=ORIENTED_EDGE ( 'NONE', *, *, #25453, .T. ) ;
#42845=DIRECTION ( 'NONE',  ( 0.000000000000000000, 0.000000000000000000, -1.000000000000000000 ) ) ;
#42874=AXIS2_PLACEMENT_3D ( 'NONE', #46996, #15652, #52598 ) ;
#42883=VERTEX_POINT ( 'NONE', #4299 ) ;
#42896=ORIENTED_EDGE ( 'NONE', *, *, #66217, .T. ) ;
#42912=DIRECTION ( 'NONE',  ( -1.000000000000000000, 0.000000000000000000, 0.000000000000000000 ) ) ;
#42928=ORIENTED_EDGE ( 'NONE', *, *, #49802, .F. ) ;
#42935=ORIENTED_EDGE ( 'NONE', *, *, #8831, .F. ) ;
#42939=EDGE_CURVE ( 'NONE', #9250, #61196, #14547, .T. ) ;
#42952=DIRECTION ( 'NONE',  ( 0.000000000000000000, -1.000000000000000000, 0.000000000000000000 ) ) ;
#42957=DIRECTION ( 'NONE',  ( 0.000000000000000000, 0.000000000000000000, -1.000000000000000000 ) ) ;
#42984=CIRCLE ( 'NONE', #56373, 0.2500000000000002220 ) ;
#43040=CIRCLE ( 'NONE', #35148, 0.7499999999999997780 ) ;
#43059=ORIENTED_EDGE ( 'NONE', *, *, #41088, .F. ) ;
#43080=VECTOR ( 'NONE', #40861, 1000.000000000000114 ) ;
#43101=CARTESIAN_POINT ( 'NONE',  ( 13.75000000000000533, 30.74999999999999289, 3.750000000000000000 ) ) ;
#43113=VERTEX_POINT ( 'NONE', #716 ) ;
#43127=EDGE_LOOP ( 'NONE', ( #28755, #68230, #58196, #12712 ) ) ;
#43138=VERTEX_POINT ( 'NONE', #44783 ) ;
#43147=CIRCLE ( 'NONE', #26209, 0.5000000000000004441 ) ;
#43153=CARTESIAN_POINT ( 'NONE',  ( -22.75000000000000711, 34.24999999999999289, -4.000000000000000000 ) ) ;
#43167=CARTESIAN_POINT ( 'NONE',  ( 4.750000000000002665, 22.24999999999998579, 3.750000000000000000 ) ) ;
#43191=EDGE_CURVE ( 'NONE', #58659, #67644, #26765, .T. ) ;
#43213=ORIENTED_EDGE ( 'NONE', *, *, #53475, .F. ) ;
#43227=CIRCLE ( 'NONE', #63417, 0.2500000000000002220 ) ;
#43265=CARTESIAN_POINT ( 'NONE',  ( -22.75000000000000711, 36.75000000000000000, 4.000000000000000000 ) ) ;
#43267=AXIS2_PLACEMENT_3D ( 'NONE', #40009, #40688, #46327 ) ;
#43273=CARTESIAN_POINT ( 'NONE',  ( 18.25000000000000711, 33.74999999999999289, 3.750000000000000000 ) ) ;
#43278=EDGE_CURVE ( 'NONE', #4438, #43113, #50396, .T. ) ;
#43280=VECTOR ( 'NONE', #43786, 1000.000000000000000 ) ;
#43284=DIRECTION ( 'NONE',  ( 0.000000000000000000, 0.000000000000000000, -1.000000000000000000 ) ) ;
#43298=CONICAL_SURFACE ( 'NONE', #12901, 4.499999999999976019, 0.7853981633974412846 ) ;
#43313=ORIENTED_EDGE ( 'NONE', *, *, #51958, .F. ) ;
#43317=CARTESIAN_POINT ( 'NONE',  ( -18.25000000000000711, 33.74999999999999289, -3.750000000000000000 ) ) ;
#43334=CARTESIAN_POINT ( 'NONE',  ( -25.00000000000000000, 0.000000000000000000, 3.000000000000000000 ) ) ;
#43336=AXIS2_PLACEMENT_3D ( 'NONE', #33471, #2070, #29572 ) ;
#43337=DIRECTION ( 'NONE',  ( 0.000000000000000000, 1.000000000000000000, 0.000000000000000000 ) ) ;
#43340=CARTESIAN_POINT ( 'NONE',  ( -4.250000000000001776, 22.24999999999998579, 3.750000000000000000 ) ) ;
#43370=EDGE_CURVE ( 'NONE', #40236, #67406, #21164, .T. ) ;
#43402=CYLINDRICAL_SURFACE ( 'NONE', #55371, 1.000000000000000888 ) ;
#43410=CARTESIAN_POINT ( 'NONE',  ( -19.00000000000000000, 8.000000000000000000, 4.000000000000000000 ) ) ;
#43425=FACE_OUTER_BOUND ( 'NONE', #35130, .T. ) ;
#43430=AXIS2_PLACEMENT_3D ( 'NONE', #47169, #20748, #31627 ) ;
#43446=ORIENTED_EDGE ( 'NONE', *, *, #32884, .F. ) ;
#43469=CARTESIAN_POINT ( 'NONE',  ( 18.25000000000000711, 33.74999999999999289, 3.750000000000000000 ) ) ;
#43479=ORIENTED_EDGE ( 'NONE', *, *, #69557, .F. ) ;
#43488=ORIENTED_EDGE ( 'NONE', *, *, #5464, .T. ) ;
#43512=ADVANCED_FACE ( 'NONE', ( #67860 ), #14369, .F. ) ;
#43521=CARTESIAN_POINT ( 'NONE',  ( 4.750000000000002665, 0.000000000000000000, 4.000000000000000000 ) ) ;
#43525=CIRCLE ( 'NONE', #37902, 0.2500000000000002220 ) ;
#43536=DIRECTION ( 'NONE',  ( -1.000000000000000000, 0.000000000000000000, 0.000000000000000000 ) ) ;
#43549=VERTEX_POINT ( 'NONE', #8426 ) ;
#43571=DIRECTION ( 'NONE',  ( -1.000000000000000000, 0.000000000000000000, 0.000000000000000000 ) ) ;
#43574=EDGE_CURVE ( 'NONE', #52546, #34410, #14482, .T. ) ;
#43587=LINE ( 'NONE', #43928, #36027 ) ;
#43597=ORIENTED_EDGE ( 'NONE', *, *, #10768, .F. ) ;
#43609=ORIENTED_EDGE ( 'NONE', *, *, #60652, .F. ) ;
#43614=EDGE_LOOP ( 'NONE', ( #60102, #62080, #39062, #23308 ) ) ;
#43634=EDGE_CURVE ( 'NONE', #22236, #65737, #10150, .T. ) ;
#43648=CIRCLE ( 'NONE', #60403, 0.2500000000000002220 ) ;
#43684=DIRECTION ( 'NONE',  ( 1.000000000000000000, -0.000000000000000000, -0.000000000000000000 ) ) ;
#43727=ADVANCED_FACE ( 'NONE', ( #28975 ), #22082, .T. ) ;
#43760=DIRECTION ( 'NONE',  ( 0.000000000000000000, 0.000000000000000000, -1.000000000000000000 ) ) ;
#43764=EDGE_LOOP ( 'NONE', ( #2729, #43899, #22026 ) ) ;
#43783=SPHERICAL_SURFACE ( 'NONE', #59914, 0.2500000000000000000 ) ;
#43786=DIRECTION ( 'NONE',  ( -5.782411586589351722E-16, 1.000000000000000000, 0.000000000000000000 ) ) ;
#43793=EDGE_CURVE ( 'NONE', #65002, #37693, #18462, .T. ) ;
#43795=VERTEX_POINT ( 'NONE', #40623 ) ;
#43812=LINE ( 'NONE', #22318, #10324 ) ;
#43850=VECTOR ( 'NONE', #61569, 1000.000000000000000 ) ;
#43870=LINE ( 'NONE', #33280, #56264 ) ;
#43881=CARTESIAN_POINT ( 'NONE',  ( -8.750000000000001776, 25.24999999999998934, -4.000000000000000000 ) ) ;
#43891=ORIENTED_EDGE ( 'NONE', *, *, #63786, .F. ) ;
#43896=DIRECTION ( 'NONE',  ( -5.782411586589351722E-16, -1.000000000000000000, 0.000000000000000000 ) ) ;
#43899=ORIENTED_EDGE ( 'NONE', *, *, #18459, .T. ) ;
#43901=CARTESIAN_POINT ( 'NONE',  ( -13.50000000000000355, 27.99999999999998934, 4.000000000000000000 ) ) ;
#43915=CARTESIAN_POINT ( 'NONE',  ( -22.75000000000000711, 36.75000000000000000, -4.000000000000000000 ) ) ;
#43928=CARTESIAN_POINT ( 'NONE',  ( -22.75000000000000711, 34.24999999999999289, -4.000000000000000000 ) ) ;
#43952=CARTESIAN_POINT ( 'NONE',  ( 13.50000000000000355, 27.74999999999998934, -3.750000000000000000 ) ) ;
#43972=FACE_OUTER_BOUND ( 'NONE', #48144, .T. ) ;
#43978=AXIS2_PLACEMENT_3D ( 'NONE', #8370, #51607, #3366 ) ;
#43979=ADVANCED_FACE ( 'NONE', ( #9656 ), #69081, .T. ) ;
#43997=ORIENTED_EDGE ( 'NONE', *, *, #27065, .F. ) ;
#44028=DIRECTION ( 'NONE',  ( 0.000000000000000000, 0.000000000000000000, 1.000000000000000000 ) ) ;
#44040=EDGE_LOOP ( 'NONE', ( #49820, #10256, #67091, #51883 ) ) ;
#44053=CARTESIAN_POINT ( 'NONE',  ( -15.00000000000000000, 8.000000000000000000, -3.500000000000017764 ) ) ;
#44079=ORIENTED_EDGE ( 'NONE', *, *, #60170, .F. ) ;
#44091=CIRCLE ( 'NONE', #37362, 0.2500000000000002220 ) ;
#44103=AXIS2_PLACEMENT_3D ( 'NONE', #49412, #63583, #1495 ) ;
#44114=DIRECTION ( 'NONE',  ( 1.000000000000000000, -0.000000000000000000, 0.000000000000000000 ) ) ;
#44124=VERTEX_POINT ( 'NONE', #64484 ) ;
#44127=EDGE_CURVE ( 'NONE', #30006, #17294, #54606, .T. ) ;
#44134=DIRECTION ( 'NONE',  ( -1.000000000000000000, 0.000000000000000000, 0.000000000000000000 ) ) ;
#44137=ADVANCED_FACE ( 'NONE', ( #58862 ), #37806, .T. ) ;
#44140=CARTESIAN_POINT ( 'NONE',  ( 4.250000000000001776, 21.74999999999998579, -4.000000000000000000 ) ) ;
#44153=( LENGTH_UNIT ( ) NAMED_UNIT ( * ) SI_UNIT ( .MILLI., .METRE. ) );
#44164=DIRECTION ( 'NONE',  ( -1.000000000000000000, 0.000000000000000000, 0.000000000000000000 ) ) ;
#44189=DIRECTION ( 'NONE',  ( 0.000000000000000000, 0.000000000000000000, -1.000000000000000000 ) ) ;
#44209=DIRECTION ( 'NONE',  ( 1.000000000000000000, 0.000000000000000000, 0.000000000000000000 ) ) ;
#44217=ADVANCED_FACE ( 'NONE', ( #66191 ), #2158, .F. ) ;
#44239=CIRCLE ( 'NONE', #40869, 4.499999999999997335 ) ;
#44268=AXIS2_PLACEMENT_3D ( 'NONE', #25128, #24416, #68060 ) ;
#44285=VECTOR ( 'NONE', #28379, 1000.000000000000000 ) ;
#44300=DIRECTION ( 'NONE',  ( 0.000000000000000000, 0.000000000000000000, 1.000000000000000000 ) ) ;
#44306=ORIENTED_EDGE ( 'NONE', *, *, #17862, .F. ) ;
#44309=ADVANCED_FACE ( 'NONE', ( #23985 ), #19748, .T. ) ;
#44350=FACE_OUTER_BOUND ( 'NONE', #3486, .T. ) ;
#44363=ORIENTED_EDGE ( 'NONE', *, *, #11696, .F. ) ;
#44370=EDGE_CURVE ( 'NONE', #15255, #68401, #67599, .T. ) ;
#44391=CARTESIAN_POINT ( 'NONE',  ( -9.250000000000003553, 27.99999999999998934, -3.750000000000000000 ) ) ;
#44395=DIRECTION ( 'NONE',  ( 0.000000000000000000, 0.000000000000000000, 1.000000000000000000 ) ) ;
#44408=DIRECTION ( 'NONE',  ( -0.000000000000000000, -0.000000000000000000, -1.000000000000000000 ) ) ;
#44447=DIRECTION ( 'NONE',  ( 0.000000000000000000, 0.000000000000000000, -1.000000000000000000 ) ) ;
#44450=AXIS2_PLACEMENT_3D ( 'NONE', #36886, #58304, #22063 ) ;
#44454=CYLINDRICAL_SURFACE ( 'NONE', #58625, 0.2500000000000002220 ) ;
#44497=AXIS2_PLACEMENT_3D ( 'NONE', #60322, #28283, #56706 ) ;
#44611=CARTESIAN_POINT ( 'NONE',  ( -8.750000000000001776, 25.24999999999998934, 4.000000000000000000 ) ) ;
#44655=CARTESIAN_POINT ( 'NONE',  ( 22.25000000000000711, 34.24999999999999289, 3.750000000000000000 ) ) ;
#44711=CIRCLE ( 'NONE', #7594, 0.2500000000000002220 ) ;
#44717=CARTESIAN_POINT ( 'NONE',  ( -4.500000000000002665, 21.74999999999998579, -3.750000000000000000 ) ) ;
#44729=ORIENTED_EDGE ( 'NONE', *, *, #61417, .F. ) ;
#44749=LINE ( 'NONE', #17650, #62033 ) ;
#44778=CYLINDRICAL_SURFACE ( 'NONE', #52665, 0.2500000000000002220 ) ;
#44783=CARTESIAN_POINT ( 'NONE',  ( -9.250000000000003553, 27.74999999999998934, 4.000000000000000000 ) ) ;
#44793=CIRCLE ( 'NONE', #40297, 0.2500000000000002220 ) ;
#44797=DIRECTION ( 'NONE',  ( -1.000000000000000000, 0.000000000000000000, 0.000000000000000000 ) ) ;
#44802=LINE ( 'NONE', #17704, #9664 ) ;
#44819=CARTESIAN_POINT ( 'NONE',  ( 18.25000000000000711, 33.74999999999999289, -3.750000000000000000 ) ) ;
#44845=VERTEX_POINT ( 'NONE', #9482 ) ;
#44935=CARTESIAN_POINT ( 'NONE',  ( -13.75000000000000533, 30.74999999999999289, 3.750000000000000000 ) ) ;
#44944=EDGE_LOOP ( 'NONE', ( #6699, #63335, #35465, #15226 ) ) ;
#44955=EDGE_LOOP ( 'NONE', ( #51294, #33723, #32652, #554 ) ) ;
#44983=VECTOR ( 'NONE', #41064, 1000.000000000000000 ) ;
#44993=ORIENTED_EDGE ( 'NONE', *, *, #39186, .T. ) ;
#45005=FACE_OUTER_BOUND ( 'NONE', #18832, .T. ) ;
#45008=ADVANCED_FACE ( 'NONE', ( #30303 ), #42761, .F. ) ;
#45012=CARTESIAN_POINT ( 'NONE',  ( -13.50000000000000533, 30.74999999999999289, 3.750000000000000000 ) ) ;
#45015=ORIENTED_EDGE ( 'NONE', *, *, #3976, .T. ) ;
#45017=SPHERICAL_SURFACE ( 'NONE', #57641, 0.2500000000000000000 ) ;
#45073=ORIENTED_EDGE ( 'NONE', *, *, #12867, .T. ) ;
#45083=CARTESIAN_POINT ( 'NONE',  ( 18.25000000000000711, 33.99999999999999289, -3.750000000000000000 ) ) ;
#45084=CARTESIAN_POINT ( 'NONE',  ( -9.250000000000003553, 27.99999999999998934, 4.000000000000000000 ) ) ;
#45089=DIRECTION ( 'NONE',  ( 0.000000000000000000, -1.000000000000000000, 0.000000000000000000 ) ) ;
#45090=CYLINDRICAL_SURFACE ( 'NONE', #66922, 0.2500000000000002220 ) ;
#45121=FACE_OUTER_BOUND ( 'NONE', #47466, .T. ) ;
#45140=DIRECTION ( 'NONE',  ( 0.000000000000000000, 0.000000000000000000, 1.000000000000000000 ) ) ;
#45165=DIRECTION ( 'NONE',  ( -0.000000000000000000, -1.000000000000000000, -0.000000000000000000 ) ) ;
#45196=ORIENTED_EDGE ( 'NONE', *, *, #50823, .F. ) ;
#45203=DIRECTION ( 'NONE',  ( -1.000000000000000000, 0.000000000000000000, 0.000000000000000000 ) ) ;
#45206=CARTESIAN_POINT ( 'NONE',  ( 4.750000000000002665, 24.99999999999998579, 4.000000000000000000 ) ) ;
#45222=ORIENTED_EDGE ( 'NONE', *, *, #61964, .T. ) ;
#45230=DIRECTION ( 'NONE',  ( 0.000000000000000000, 0.000000000000000000, -1.000000000000000000 ) ) ;
#45231=AXIS2_PLACEMENT_3D ( 'NONE', #37345, #26711, #47205 ) ;
#45238=CARTESIAN_POINT ( 'NONE',  ( -9.250000000000003553, 27.99999999999998934, 3.750000000000000000 ) ) ;
#45240=VECTOR ( 'NONE', #55350, 1000.000000000000000 ) ;
#45257=DIRECTION ( 'NONE',  ( 5.782411586589351722E-16, -1.000000000000000000, -0.000000000000000000 ) ) ;
#45279=AXIS2_PLACEMENT_3D ( 'NONE', #33652, #27657, #49166 ) ;
#45297=ORIENTED_EDGE ( 'NONE', *, *, #17603, .F. ) ;
#45305=CYLINDRICAL_SURFACE ( 'NONE', #3252, 0.2500000000000002220 ) ;
#45321=AXIS2_PLACEMENT_3D ( 'NONE', #27387, #617, #1665 ) ;
#45328=EDGE_CURVE ( 'NONE', #17866, #64410, #36047, .T. ) ;
#45374=ORIENTED_EDGE ( 'NONE', *, *, #26606, .F. ) ;
#45386=AXIS2_PLACEMENT_3D ( 'NONE', #42558, #69264, #10522 ) ;
#45390=FACE_OUTER_BOUND ( 'NONE', #4355, .T. ) ;
#45398=VECTOR ( 'NONE', #1597, 1000.000000000000000 ) ;
#45405=ADVANCED_FACE ( 'NONE', ( #23580 ), #15814, .T. ) ;
#45440=ORIENTED_EDGE ( 'NONE', *, *, #26904, .T. ) ;
#45441=DIRECTION ( 'NONE',  ( 0.000000000000000000, 0.000000000000000000, -1.000000000000000000 ) ) ;
#45444=AXIS2_PLACEMENT_3D ( 'NONE', #51725, #24974, #46484 ) ;
#45455=CARTESIAN_POINT ( 'NONE',  ( -25.00000000000000355, 37.00000000000000000, 4.000000000000000000 ) ) ;
#45460=DIRECTION ( 'NONE',  ( 0.000000000000000000, 0.000000000000000000, 1.000000000000000000 ) ) ;
#45464=CARTESIAN_POINT ( 'NONE',  ( -24.00000000000000000, 1.000000000000000000, 3.000000000000000000 ) ) ;
#45473=DIRECTION ( 'NONE',  ( -0.000000000000000000, -1.000000000000000000, -0.000000000000000000 ) ) ;
#45513=CARTESIAN_POINT ( 'NONE',  ( -22.75000000000000711, 36.75000000000000000, -3.750000000000000000 ) ) ;
#45527=CIRCLE ( 'NONE', #5053, 0.2500000000000002220 ) ;
#45529=ORIENTED_EDGE ( 'NONE', *, *, #53483, .T. ) ;
#45533=DIRECTION ( 'NONE',  ( -0.000000000000000000, -0.000000000000000000, 1.000000000000000000 ) ) ;
#45558=CARTESIAN_POINT ( 'NONE',  ( -13.75000000000000533, 30.74999999999999289, 3.750000000000000000 ) ) ;
#45592=SHAPE_DEFINITION_REPRESENTATION ( #58577, #15001 ) ;
#45599=LINE ( 'NONE', #51183, #51719 ) ;
#45611=DIRECTION ( 'NONE',  ( 0.000000000000000000, 1.000000000000000000, 0.000000000000000000 ) ) ;
#45614=VECTOR ( 'NONE', #20472, 1000.000000000000000 ) ;
#45616=VECTOR ( 'NONE', #27724, 1000.000000000000000 ) ;
#45638=SPHERICAL_SURFACE ( 'NONE', #43267, 0.2500000000000000000 ) ;
#45646=DIRECTION ( 'NONE',  ( 0.000000000000000000, 0.000000000000000000, -1.000000000000000000 ) ) ;
#45655=VERTEX_POINT ( 'NONE', #27630 ) ;
#45664=DIRECTION ( 'NONE',  ( 0.000000000000000000, 0.000000000000000000, -1.000000000000000000 ) ) ;
#45668=CIRCLE ( 'NONE', #17444, 0.2500000000000002220 ) ;
#45710=DIRECTION ( 'NONE',  ( -0.000000000000000000, -0.000000000000000000, -1.000000000000000000 ) ) ;
#45719=DIRECTION ( 'NONE',  ( 0.000000000000000000, 0.000000000000000000, -1.000000000000000000 ) ) ;
#45737=CARTESIAN_POINT ( 'NONE',  ( 13.74999999999998757, -7.950815931560351124E-15, 4.000000000000000000 ) ) ;
#45758=ORIENTED_EDGE ( 'NONE', *, *, #63167, .F. ) ;
#45768=ORIENTED_EDGE ( 'NONE', *, *, #56948, .T. ) ;
#45771=ORIENTED_EDGE ( 'NONE', *, *, #23212, .T. ) ;
#45805=EDGE_CURVE ( 'NONE', #45655, #49491, #67569, .T. ) ;
#45820=CARTESIAN_POINT ( 'NONE',  ( -24.00000000000000000, 1.000000000000000000, 4.000000000000000000 ) ) ;
#45834=CARTESIAN_POINT ( 'NONE',  ( -4.750000000000002665, 24.99999999999998579, 3.750000000000000000 ) ) ;
#45864=ORIENTED_EDGE ( 'NONE', *, *, #47883, .T. ) ;
#45889=AXIS2_PLACEMENT_3D ( 'NONE', #32444, #44114, #16667 ) ;
#45897=DIRECTION ( 'NONE',  ( 0.7071067811865474617, 0.000000000000000000, 0.7071067811865474617 ) ) ;
#45910=DIRECTION ( 'NONE',  ( -1.000000000000000000, 0.000000000000000000, 0.000000000000000000 ) ) ;
#45960=DIRECTION ( 'NONE',  ( 0.000000000000000000, 0.000000000000000000, -1.000000000000000000 ) ) ;
#45963=FACE_OUTER_BOUND ( 'NONE', #32705, .T. ) ;
#45969=ORIENTED_EDGE ( 'NONE', *, *, #22578, .F. ) ;
#45974=DIRECTION ( 'NONE',  ( 9.376883653928687363E-17, -1.000000000000000000, 0.000000000000000000 ) ) ;
#46013=DIRECTION ( 'NONE',  ( 0.000000000000000000, 0.000000000000000000, -1.000000000000000000 ) ) ;
#46021=EDGE_CURVE ( 'NONE', #58067, #4438, #14887, .T. ) ;
#46052=ADVANCED_FACE ( 'NONE', ( #31032 ), #15253, .T. ) ;
#46055=CARTESIAN_POINT ( 'NONE',  ( -17.75000000000000711, 30.99999999999999289, 3.750000000000000000 ) ) ;
#46057=DIRECTION ( 'NONE',  ( 0.000000000000000000, 0.000000000000000000, -1.000000000000000000 ) ) ;
#46106=CARTESIAN_POINT ( 'NONE',  ( 9.000000000000003553, 25.24999999999998934, 4.000000000000000000 ) ) ;
#46117=ORIENTED_EDGE ( 'NONE', *, *, #68305, .T. ) ;
#46136=ORIENTED_EDGE ( 'NONE', *, *, #56333, .F. ) ;
#46141=DIRECTION ( 'NONE',  ( -1.000000000000000000, 0.000000000000000000, 0.000000000000000000 ) ) ;
#46158=CARTESIAN_POINT ( 'NONE',  ( -9.250000000000003553, 27.74999999999998934, 3.750000000000000000 ) ) ;
#46188=ORIENTED_EDGE ( 'NONE', *, *, #61964, .F. ) ;
#46206=ORIENTED_EDGE ( 'NONE', *, *, #24435, .F. ) ;
#46258=VECTOR ( 'NONE', #40553, 1000.000000000000000 ) ;
#46268=( NAMED_UNIT ( * ) SI_UNIT ( $, .STERADIAN. ) SOLID_ANGLE_UNIT ( ) );
#46276=DIRECTION ( 'NONE',  ( -1.000000000000000000, 0.000000000000000000, 0.000000000000000000 ) ) ;
#46277=CYLINDRICAL_SURFACE ( 'NONE', #12530, 0.2500000000000002220 ) ;
#46283=EDGE_CURVE ( 'NONE', #39066, #44845, #16029, .T. ) ;
#46287=VERTEX_POINT ( 'NONE', #9532 ) ;
#46288=VECTOR ( 'NONE', #51061, 1000.000000000000000 ) ;
#46310=CARTESIAN_POINT ( 'NONE',  ( -13.25000000000000355, 27.74999999999998934, 4.000000000000000000 ) ) ;
#46315=AXIS2_PLACEMENT_3D ( 'NONE', #49476, #49143, #11124 ) ;
#46327=DIRECTION ( 'NONE',  ( -1.000000000000000000, 0.000000000000000000, 0.000000000000000000 ) ) ;
#46347=CARTESIAN_POINT ( 'NONE',  ( 4.750000000000002665, 24.74999999999998579, 4.000000000000000000 ) ) ;
#46369=VERTEX_POINT ( 'NONE', #68259 ) ;
#46385=ORIENTED_EDGE ( 'NONE', *, *, #61687, .T. ) ;
#46409=CARTESIAN_POINT ( 'NONE',  ( 0.000000000000000000, 27.74999999999998934, 3.750000000000000000 ) ) ;
#46414=CARTESIAN_POINT ( 'NONE',  ( 24.00000000000000000, 1.000000000000000888, 4.000000000000000000 ) ) ;
#46434=DIRECTION ( 'NONE',  ( 1.000000000000000000, -0.000000000000000000, -0.000000000000000000 ) ) ;
#46445=DIRECTION ( 'NONE',  ( 0.000000000000000000, 0.000000000000000000, -1.000000000000000000 ) ) ;
#46467=DIRECTION ( 'NONE',  ( -1.000000000000000000, 0.000000000000000000, 0.000000000000000000 ) ) ;
#46468=ORIENTED_EDGE ( 'NONE', *, *, #48042, .T. ) ;
#46471=LINE ( 'NONE', #14778, #66816 ) ;
#46478=AXIS2_PLACEMENT_3D ( 'NONE', #49930, #32339, #42957 ) ;
#46484=DIRECTION ( 'NONE',  ( 0.000000000000000000, 0.000000000000000000, 1.000000000000000000 ) ) ;
#46491=DIRECTION ( 'NONE',  ( 0.000000000000000000, 0.000000000000000000, -1.000000000000000000 ) ) ;
#46496=ORIENTED_EDGE ( 'NONE', *, *, #39961, .F. ) ;
#46533=AXIS2_PLACEMENT_3D ( 'NONE', #62657, #14481, #51792 ) ;
#46540=VERTEX_POINT ( 'NONE', #7349 ) ;
#46560=FACE_OUTER_BOUND ( 'NONE', #9416, .T. ) ;
#46566=FACE_OUTER_BOUND ( 'NONE', #9911, .T. ) ;
#46579=CYLINDRICAL_SURFACE ( 'NONE', #69266, 0.2500000000000002220 ) ;
#46600=CARTESIAN_POINT ( 'NONE',  ( -4.250000000000001776, 21.74999999999998579, 4.000000000000000000 ) ) ;
#46607=VERTEX_POINT ( 'NONE', #51636 ) ;
#46627=AXIS2_PLACEMENT_3D ( 'NONE', #24107, #45611, #67029 ) ;
#46635=AXIS2_PLACEMENT_3D ( 'NONE', #12798, #12098, #50116 ) ;
#46641=SPHERICAL_SURFACE ( 'NONE', #44268, 0.2500000000000000000 ) ;
#46657=CIRCLE ( 'NONE', #26406, 4.000000000000000000 ) ;
#46678=CARTESIAN_POINT ( 'NONE',  ( 22.75000000000000711, 37.00000000000000000, 4.000000000000000000 ) ) ;
#46703=CARTESIAN_POINT ( 'NONE',  ( 4.250000000000001776, 22.24999999999998579, 3.750000000000000000 ) ) ;
#46709=ORIENTED_EDGE ( 'NONE', *, *, #49830, .F. ) ;
#46711=CARTESIAN_POINT ( 'NONE',  ( 8.750000000000001776, 25.24999999999998934, 4.000000000000000000 ) ) ;
#46753=ORIENTED_EDGE ( 'NONE', *, *, #13114, .F. ) ;
#46782=ORIENTED_EDGE ( 'NONE', *, *, #30727, .F. ) ;
#46870=DIRECTION ( 'NONE',  ( 0.000000000000000000, -0.000000000000000000, -1.000000000000000000 ) ) ;
#46902=ORIENTED_EDGE ( 'NONE', *, *, #24363, .F. ) ;
#46914=CARTESIAN_POINT ( 'NONE',  ( 24.75000000000000355, 37.00000000000000000, -3.000000000000000000 ) ) ;
#46958=DIRECTION ( 'NONE',  ( 0.000000000000000000, 0.000000000000000000, -1.000000000000000000 ) ) ;
#46960=CARTESIAN_POINT ( 'NONE',  ( -24.00000000000000355, 37.00000000000000000, 3.000000000000000000 ) ) ;
#46971=FILL_AREA_STYLE_COLOUR ( '', #13556 ) ;
#46996=CARTESIAN_POINT ( 'NONE',  ( 4.750000000000002665, 24.74999999999998579, 3.750000000000000000 ) ) ;
#47031=CYLINDRICAL_SURFACE ( 'NONE', #67739, 0.2500000000000002220 ) ;
#47040=EDGE_LOOP ( 'NONE', ( #60769, #61255, #47471, #32414 ) ) ;
#47042=LINE ( 'NONE', #20966, #54939 ) ;
#47086=AXIS2_PLACEMENT_3D ( 'NONE', #34294, #40276, #7556 ) ;
#47155=CIRCLE ( 'NONE', #16809, 0.2500000000000002220 ) ;
#47167=EDGE_LOOP ( 'NONE', ( #27104, #51178, #48402, #28403 ) ) ;
#47169=CARTESIAN_POINT ( 'NONE',  ( 22.25000000000000711, 33.74999999999999289, -3.750000000000000000 ) ) ;
#47192=DIRECTION ( 'NONE',  ( 0.000000000000000000, 0.000000000000000000, 1.000000000000000000 ) ) ;
#47200=FACE_OUTER_BOUND ( 'NONE', #9357, .T. ) ;
#47205=DIRECTION ( 'NONE',  ( 1.000000000000000000, 0.000000000000000000, 0.000000000000000000 ) ) ;
#47208=ORIENTED_EDGE ( 'NONE', *, *, #6646, .T. ) ;
#47243=AXIS2_PLACEMENT_3D ( 'NONE', #13606, #67085, #35070 ) ;
#47247=CARTESIAN_POINT ( 'NONE',  ( -9.250000000000003553, 27.74999999999998934, -3.750000000000000000 ) ) ;
#47253=CARTESIAN_POINT ( 'NONE',  ( -4.750000000000002665, 24.74999999999998579, -4.000000000000000000 ) ) ;
#47265=EDGE_LOOP ( 'NONE', ( #59078, #41321, #68426, #35977 ) ) ;
#47269=CARTESIAN_POINT ( 'NONE',  ( 9.250000000000003553, 27.74999999999998934, 3.750000000000000000 ) ) ;
#47335=EDGE_LOOP ( 'NONE', ( #12958, #49394, #46496, #21818 ) ) ;
#47354=DIRECTION ( 'NONE',  ( 0.000000000000000000, 0.000000000000000000, -1.000000000000000000 ) ) ;
#47363=DIRECTION ( 'NONE',  ( 0.000000000000000000, 0.000000000000000000, -1.000000000000000000 ) ) ;
#47367=DIRECTION ( 'NONE',  ( 0.000000000000000000, 0.000000000000000000, -1.000000000000000000 ) ) ;
#47378=EDGE_CURVE ( 'NONE', #68529, #29481, #21655, .T. ) ;
#47386=SPHERICAL_SURFACE ( 'NONE', #33651, 0.2500000000000000000 ) ;
#47393=DIRECTION ( 'NONE',  ( -0.000000000000000000, -0.000000000000000000, 1.000000000000000000 ) ) ;
#47416=CYLINDRICAL_SURFACE ( 'NONE', #39664, 4.000000000000000000 ) ;
#47421=ADVANCED_FACE ( 'NONE', ( #22148 ), #22851, .T. ) ;
#47424=CIRCLE ( 'NONE', #14813, 0.2500000000000002220 ) ;
#47430=DIRECTION ( 'NONE',  ( -1.000000000000000000, 0.000000000000000000, 0.000000000000000000 ) ) ;
#47466=EDGE_LOOP ( 'NONE', ( #64603, #62401, #17508, #15731 ) ) ;
#47471=ORIENTED_EDGE ( 'NONE', *, *, #34306, .F. ) ;
#47472=ADVANCED_FACE ( 'NONE', ( #11939 ), #27400, .T. ) ;
#47479=VERTEX_POINT ( 'NONE', #49939 ) ;
#47492=VECTOR ( 'NONE', #504, 1000.000000000000000 ) ;
#47506=CARTESIAN_POINT ( 'NONE',  ( -24.75000000000000355, 37.00000000000000000, 4.000000000000000000 ) ) ;
#47508=ORIENTED_EDGE ( 'NONE', *, *, #55976, .T. ) ;
#47564=CARTESIAN_POINT ( 'NONE',  ( -13.25000000000000355, 27.74999999999998934, -3.750000000000000000 ) ) ;
#47591=AXIS2_PLACEMENT_3D ( 'NONE', #52796, #30963, #14814 ) ;
#47634=EDGE_CURVE ( 'NONE', #37913, #14152, #2720, .T. ) ;
#47637=CIRCLE ( 'NONE', #31844, 0.2500000000000002220 ) ;
#47679=ORIENTED_EDGE ( 'NONE', *, *, #9722, .T. ) ;
#47685=CARTESIAN_POINT ( 'NONE',  ( -22.50000000000000711, 36.75000000000000000, 4.000000000000000000 ) ) ;
#47698=CONICAL_SURFACE ( 'NONE', #66718, 4.499999999999976019, 0.7853981633974412846 ) ;
#47699=VERTEX_POINT ( 'NONE', #69547 ) ;
#47703=ORIENTED_EDGE ( 'NONE', *, *, #54325, .T. ) ;
#47704=AXIS2_PLACEMENT_3D ( 'NONE', #44935, #61735, #45960 ) ;
#47719=EDGE_CURVE ( 'NONE', #4438, #58900, #4831, .T. ) ;
#47731=CARTESIAN_POINT ( 'NONE',  ( 4.500000000000002665, 24.74999999999998579, -3.750000000000000000 ) ) ;
#47752=EDGE_LOOP ( 'NONE', ( #14127, #40223, #61087, #37180 ) ) ;
#47759=CARTESIAN_POINT ( 'NONE',  ( -13.75000000000000533, 30.74999999999999289, -3.750000000000000000 ) ) ;
#47777=CARTESIAN_POINT ( 'NONE',  ( 13.25000000000000355, 28.24999999999998934, -4.000000000000000000 ) ) ;
#47783=CIRCLE ( 'NONE', #19650, 0.2500000000000002220 ) ;
#47830=DIRECTION ( 'NONE',  ( -1.000000000000000000, 0.000000000000000000, 0.000000000000000000 ) ) ;
#47862=AXIS2_PLACEMENT_3D ( 'NONE', #13166, #34623, #45230 ) ;
#47883=EDGE_CURVE ( 'NONE', #40174, #33741, #28399, .T. ) ;
#47891=CARTESIAN_POINT ( 'NONE',  ( 22.50000000000000711, 37.00000000000000000, 4.000000000000000000 ) ) ;
#47902=ORIENTED_EDGE ( 'NONE', *, *, #51958, .T. ) ;
#47911=AXIS2_PLACEMENT_3D ( 'NONE', #38137, #31776, #43760 ) ;
#47921=CARTESIAN_POINT ( 'NONE',  ( 4.750000000000002665, 0.000000000000000000, 3.750000000000000000 ) ) ;
#47970=ORIENTED_EDGE ( 'NONE', *, *, #44370, .F. ) ;
#48021=FACE_OUTER_BOUND ( 'NONE', #67228, .T. ) ;
#48036=DIRECTION ( 'NONE',  ( -5.782411586589351722E-16, -1.000000000000000000, 0.000000000000000000 ) ) ;
#48041=CARTESIAN_POINT ( 'NONE',  ( -24.00000000000000355, 36.75000000000000000, 4.000000000000000000 ) ) ;
#48042=EDGE_CURVE ( 'NONE', #58037, #5366, #58774, .T. ) ;
#48093=CARTESIAN_POINT ( 'NONE',  ( 24.00000000000000000, 1.000000000000000000, -3.000000000000000000 ) ) ;
#48111=CIRCLE ( 'NONE', #45889, 0.2500000000000002220 ) ;
#48133=ORIENTED_EDGE ( 'NONE', *, *, #63999, .T. ) ;
#48144=EDGE_LOOP ( 'NONE', ( #21332, #28888, #13283, #48197 ) ) ;
#48148=CARTESIAN_POINT ( 'NONE',  ( -22.25000000000000711, 34.24999999999999289, 3.750000000000000000 ) ) ;
#48151=ORIENTED_EDGE ( 'NONE', *, *, #22717, .F. ) ;
#48189=AXIS2_PLACEMENT_3D ( 'NONE', #43901, #65310, #17155 ) ;
#48197=ORIENTED_EDGE ( 'NONE', *, *, #7661, .T. ) ;
#48207=CARTESIAN_POINT ( 'NONE',  ( -22.75000000000000711, 37.00000000000000000, 3.750000000000000000 ) ) ;
#48223=DIRECTION ( 'NONE',  ( -1.000000000000000000, 0.000000000000000000, 0.000000000000000000 ) ) ;
#48230=ORIENTED_EDGE ( 'NONE', *, *, #18379, .F. ) ;
#48240=EDGE_LOOP ( 'NONE', ( #12238, #29675, #48315, #58850 ) ) ;
#48263=DIRECTION ( 'NONE',  ( -0.000000000000000000, -0.000000000000000000, 1.000000000000000000 ) ) ;
#48293=AXIS2_PLACEMENT_3D ( 'NONE', #3959, #20139, #62700 ) ;
#48303=EDGE_LOOP ( 'NONE', ( #36642, #14405, #2864, #54037 ) ) ;
#48315=ORIENTED_EDGE ( 'NONE', *, *, #58370, .T. ) ;
#48319=ORIENTED_EDGE ( 'NONE', *, *, #1085, .F. ) ;
#48339=AXIS2_PLACEMENT_3D ( 'NONE', #66126, #27094, #44395 ) ;
#48344=ORIENTED_EDGE ( 'NONE', *, *, #62077, .T. ) ;
#48358=CARTESIAN_POINT ( 'NONE',  ( -25.00000000000000000, 1.000000000000000000, 3.000000000000000000 ) ) ;
#48378=SURFACE_STYLE_FILL_AREA ( #1108 ) ;
#48401=EDGE_CURVE ( 'NONE', #17294, #46540, #53314, .T. ) ;
#48402=ORIENTED_EDGE ( 'NONE', *, *, #53531, .T. ) ;
#48416=DIRECTION ( 'NONE',  ( 0.000000000000000000, 0.000000000000000000, -1.000000000000000000 ) ) ;
#48433=VECTOR ( 'NONE', #40799, 1000.000000000000000 ) ;
#48451=AXIS2_PLACEMENT_3D ( 'NONE', #66740, #25208, #2287 ) ;
#48464=CARTESIAN_POINT ( 'NONE',  ( -18.25000000000000711, 33.74999999999999289, 3.750000000000000000 ) ) ;
#48492=VECTOR ( 'NONE', #40280, 1000.000000000000000 ) ;
#48525=DIRECTION ( 'NONE',  ( 0.000000000000000000, 0.000000000000000000, -1.000000000000000000 ) ) ;
#48548=ORIENTED_EDGE ( 'NONE', *, *, #39110, .T. ) ;
#48560=CARTESIAN_POINT ( 'NONE',  ( -13.25000000000000355, 28.24999999999998934, -4.000000000000000000 ) ) ;
#48589=VERTEX_POINT ( 'NONE', #69440 ) ;
#48598=EDGE_LOOP ( 'NONE', ( #64000, #8180, #20207, #42571 ) ) ;
#48663=FACE_OUTER_BOUND ( 'NONE', #39473, .T. ) ;
#48676=ORIENTED_EDGE ( 'NONE', *, *, #18330, .F. ) ;
#48736=CARTESIAN_POINT ( 'NONE',  ( -9.000000000000003553, 27.99999999999998934, 4.000000000000000000 ) ) ;
#48741=ORIENTED_EDGE ( 'NONE', *, *, #55976, .F. ) ;
#48807=EDGE_CURVE ( 'NONE', #64274, #37913, #46471, .T. ) ;
#48808=ORIENTED_EDGE ( 'NONE', *, *, #66235, .F. ) ;
#48811=CARTESIAN_POINT ( 'NONE',  ( 17.75000000000000711, 31.24999999999999289, 3.750000000000000000 ) ) ;
#48823=EDGE_LOOP ( 'NONE', ( #31189, #26607, #28924 ) ) ;
#48842=ORIENTED_EDGE ( 'NONE', *, *, #23649, .T. ) ;
#48852=FACE_OUTER_BOUND ( 'NONE', #41501, .T. ) ;
#48875=FACE_OUTER_BOUND ( 'NONE', #36145, .T. ) ;
#48876=DIRECTION ( 'NONE',  ( -0.7071067811865425767, 0.000000000000000000, -0.7071067811865525687 ) ) ;
#48912=ORIENTED_EDGE ( 'NONE', *, *, #42698, .T. ) ;
#48914=CARTESIAN_POINT ( 'NONE',  ( 13.50000000000000355, 27.99999999999998934, 3.750000000000000000 ) ) ;
#48925=AXIS2_PLACEMENT_3D ( 'NONE', #31534, #42845, #69519 ) ;
#48970=VECTOR ( 'NONE', #10822, 1000.000000000000000 ) ;
#48974=FACE_OUTER_BOUND ( 'NONE', #67566, .T. ) ;
#48982=ORIENTED_EDGE ( 'NONE', *, *, #12377, .T. ) ;
#48990=ORIENTED_EDGE ( 'NONE', *, *, #67595, .F. ) ;
#49003=ORIENTED_EDGE ( 'NONE', *, *, #5292, .T. ) ;
#49012=CARTESIAN_POINT ( 'NONE',  ( -18.00000000000000711, 31.24999999999999289, -4.000000000000000000 ) ) ;
#49058=FACE_OUTER_BOUND ( 'NONE', #36005, .T. ) ;
#49083=ORIENTED_EDGE ( 'NONE', *, *, #65289, .T. ) ;
#49106=CARTESIAN_POINT ( 'NONE',  ( -9.250000000000003553, 27.74999999999998934, -3.750000000000000000 ) ) ;
#49128=CARTESIAN_POINT ( 'NONE',  ( 18.25000000000000711, 33.74999999999999289, -4.000000000000000000 ) ) ;
#49143=DIRECTION ( 'NONE',  ( 1.000000000000000000, 0.000000000000000000, 0.000000000000000000 ) ) ;
#49166=DIRECTION ( 'NONE',  ( 1.000000000000000000, 0.000000000000000000, 0.000000000000000000 ) ) ;
#49172=DIRECTION ( 'NONE',  ( -1.000000000000000000, 0.000000000000000000, 0.000000000000000000 ) ) ;
#49189=FACE_OUTER_BOUND ( 'NONE', #23228, .T. ) ;
#49196=EDGE_CURVE ( 'NONE', #17573, #46287, #40058, .T. ) ;
#49218=ORIENTED_EDGE ( 'NONE', *, *, #2834, .F. ) ;
#49223=AXIS2_PLACEMENT_3D ( 'NONE', #7609, #19554, #18846 ) ;
#49251=DIRECTION ( 'NONE',  ( -0.000000000000000000, 1.000000000000000000, -0.000000000000000000 ) ) ;
#49261=EDGE_CURVE ( 'NONE', #39699, #15837, #10789, .T. ) ;
#49272=ORIENTED_EDGE ( 'NONE', *, *, #49196, .F. ) ;
#49279=LINE ( 'NONE', #988, #28251 ) ;
#49345=ADVANCED_FACE ( 'NONE', ( #68498 ), #25906, .F. ) ;
#49349=EDGE_CURVE ( 'NONE', #59451, #31383, #36530, .T. ) ;
#49358=ORIENTED_EDGE ( 'NONE', *, *, #8077, .F. ) ;
#49359=FACE_OUTER_BOUND ( 'NONE', #35988, .T. ) ;
#49377=CARTESIAN_POINT ( 'NONE',  ( -4.750000000000002665, 24.99999999999998579, -3.750000000000000000 ) ) ;
#49394=ORIENTED_EDGE ( 'NONE', *, *, #46283, .F. ) ;
#49412=CARTESIAN_POINT ( 'NONE',  ( -22.25000000000000711, 34.24999999999999289, -4.000000000000000000 ) ) ;
#49450=DIRECTION ( 'NONE',  ( 0.000000000000000000, -1.000000000000000000, 0.000000000000000000 ) ) ;
#49454=CARTESIAN_POINT ( 'NONE',  ( 13.50000000000000355, 28.24999999999998934, 4.000000000000000000 ) ) ;
#49472=CARTESIAN_POINT ( 'NONE',  ( -24.00000000000000000, 0.000000000000000000, -3.000000000000000000 ) ) ;
#49476=CARTESIAN_POINT ( 'NONE',  ( 9.250000000000003553, 27.74999999999998934, 3.750000000000000000 ) ) ;
#49491=VERTEX_POINT ( 'NONE', #30067 ) ;
#49547=ORIENTED_EDGE ( 'NONE', *, *, #50456, .F. ) ;
#49556=EDGE_CURVE ( 'NONE', #51168, #5580, #16371, .T. ) ;
#49560=DIRECTION ( 'NONE',  ( 1.000000000000000000, -0.000000000000000000, 0.000000000000000000 ) ) ;
#49564=DIRECTION ( 'NONE',  ( 0.000000000000000000, 0.000000000000000000, -1.000000000000000000 ) ) ;
#49568=DIRECTION ( 'NONE',  ( 0.000000000000000000, -1.000000000000000000, 0.000000000000000000 ) ) ;
#49604=AXIS2_PLACEMENT_3D ( 'NONE', #12193, #41061, #18857 ) ;
#49608=AXIS2_PLACEMENT_3D ( 'NONE', #15970, #42031, #15282 ) ;
#49637=ORIENTED_EDGE ( 'NONE', *, *, #2293, .F. ) ;
#49639=FACE_OUTER_BOUND ( 'NONE', #44955, .T. ) ;
#49657=AXIS2_PLACEMENT_3D ( 'NONE', #16658, #38126, #6750 ) ;
#49663=ORIENTED_EDGE ( 'NONE', *, *, #63786, .T. ) ;
#49696=CIRCLE ( 'NONE', #41843, 0.5000000000000004441 ) ;
#49768=ORIENTED_EDGE ( 'NONE', *, *, #56954, .T. ) ;
#49770=CARTESIAN_POINT ( 'NONE',  ( 0.000000000000000000, 21.74999999999998579, 4.000000000000000000 ) ) ;
#49786=DIRECTION ( 'NONE',  ( 1.000000000000000000, 0.000000000000000000, 0.000000000000000000 ) ) ;
#49802=EDGE_CURVE ( 'NONE', #61721, #59451, #54971, .T. ) ;
#49805=MANIFOLD_SOLID_BREP ( 'Chamfer1', #17188 ) ;
#49820=ORIENTED_EDGE ( 'NONE', *, *, #24897, .T. ) ;
#49830=EDGE_CURVE ( 'NONE', #21095, #5051, #53501, .T. ) ;
#49878=AXIS2_PLACEMENT_3D ( 'NONE', #16054, #472, #32903 ) ;
#49882=ORIENTED_EDGE ( 'NONE', *, *, #57514, .F. ) ;
#49893=ORIENTED_EDGE ( 'NONE', *, *, #38075, .F. ) ;
#49930=CARTESIAN_POINT ( 'NONE',  ( 22.75000000000000711, 0.000000000000000000, 3.750000000000000000 ) ) ;
#49939=CARTESIAN_POINT ( 'NONE',  ( 22.75000000000000711, 37.00000000000000000, 3.750000000000000000 ) ) ;
#49959=LINE ( 'NONE', #33412, #7961 ) ;
#49973=CARTESIAN_POINT ( 'NONE',  ( -13.75000000000000533, 30.74999999999999289, -3.750000000000000000 ) ) ;
#49987=CIRCLE ( 'NONE', #44450, 0.5000000000000004441 ) ;
#50012=PLANE ( 'NONE',  #9783 ) ;
#50017=CYLINDRICAL_SURFACE ( 'NONE', #18564, 0.2500000000000002220 ) ;
#50039=CARTESIAN_POINT ( 'NONE',  ( 0.000000000000000000, 33.74999999999999289, 4.000000000000000000 ) ) ;
#50060=ADVANCED_FACE ( 'NONE', ( #25072 ), #46579, .T. ) ;
#50116=DIRECTION ( 'NONE',  ( 0.000000000000000000, 0.000000000000000000, -1.000000000000000000 ) ) ;
#50119=DIRECTION ( 'NONE',  ( -1.000000000000000000, 0.000000000000000000, -0.000000000000000000 ) ) ;
#50153=EDGE_CURVE ( 'NONE', #46287, #12301, #51039, .T. ) ;
#50159=ORIENTED_EDGE ( 'NONE', *, *, #49802, .T. ) ;
#50166=FACE_OUTER_BOUND ( 'NONE', #47167, .T. ) ;
#50185=EDGE_LOOP ( 'NONE', ( #18207, #55356, #36928, #60367 ) ) ;
#50187=DIRECTION ( 'NONE',  ( 0.000000000000000000, -1.000000000000000000, 0.000000000000000000 ) ) ;
#50229=CARTESIAN_POINT ( 'NONE',  ( 13.25000000000000355, 27.74999999999998934, -4.000000000000000000 ) ) ;
#50244=ORIENTED_EDGE ( 'NONE', *, *, #53577, .T. ) ;
#50249=ORIENTED_EDGE ( 'NONE', *, *, #27819, .T. ) ;
#50260=DIRECTION ( 'NONE',  ( -1.000000000000000000, 0.000000000000000000, 0.000000000000000000 ) ) ;
#50288=VERTEX_POINT ( 'NONE', #32953 ) ;
#50301=CARTESIAN_POINT ( 'NONE',  ( -22.25000000000000711, 33.99999999999999289, -3.750000000000000000 ) ) ;
#50302=LINE ( 'NONE', #22526, #4678 ) ;
#50331=VERTEX_POINT ( 'NONE', #39633 ) ;
#50342=FACE_OUTER_BOUND ( 'NONE', #3361, .T. ) ;
#50364=EDGE_CURVE ( 'NONE', #8679, #11393, #64790, .T. ) ;
#50380=AXIS2_PLACEMENT_3D ( 'NONE', #56434, #62410, #18121 ) ;
#50383=CYLINDRICAL_SURFACE ( 'NONE', #68318, 0.2500000000000002220 ) ;
#50387=AXIS2_PLACEMENT_3D ( 'NONE', #60804, #65766, #39407 ) ;
#50396=CIRCLE ( 'NONE', #35781, 0.2500000000000002220 ) ;
#50411=VERTEX_POINT ( 'NONE', #46310 ) ;
#50415=DIRECTION ( 'NONE',  ( 0.000000000000000000, 0.000000000000000000, -1.000000000000000000 ) ) ;
#50438=EDGE_CURVE ( 'NONE', #32928, #21392, #37921, .T. ) ;
#50440=ORIENTED_EDGE ( 'NONE', *, *, #63538, .F. ) ;
#50446=DIRECTION ( 'NONE',  ( 0.000000000000000000, 0.000000000000000000, -1.000000000000000000 ) ) ;
#50456=EDGE_CURVE ( 'NONE', #58700, #64993, #68303, .T. ) ;
#50466=ORIENTED_EDGE ( 'NONE', *, *, #42250, .F. ) ;
#50474=CYLINDRICAL_SURFACE ( 'NONE', #47086, 0.2500000000000002220 ) ;
#50504=CARTESIAN_POINT ( 'NONE',  ( -18.25000000000000711, 33.74999999999999289, 3.750000000000000000 ) ) ;
#50527=ORIENTED_EDGE ( 'NONE', *, *, #40366, .T. ) ;
#50551=AXIS2_PLACEMENT_3D ( 'NONE', #33726, #45719, #18614 ) ;
#50552=VERTEX_POINT ( 'NONE', #42096 ) ;
#50554=AXIS2_PLACEMENT_3D ( 'NONE', #45820, #35598, #3523 ) ;
#50578=EDGE_LOOP ( 'NONE', ( #9497, #31633, #67020, #45297 ) ) ;
#50589=ORIENTED_EDGE ( 'NONE', *, *, #60364, .T. ) ;
#50598=VERTEX_POINT ( 'NONE', #37851 ) ;
#50606=DIRECTION ( 'NONE',  ( -0.000000000000000000, -0.000000000000000000, -1.000000000000000000 ) ) ;
#50613=CYLINDRICAL_SURFACE ( 'NONE', #15765, 0.2500000000000002220 ) ;
#50630=PRODUCT_DEFINITION_FORMATION_WITH_SPECIFIED_SOURCE ( 'ANY', '', #20359, .NOT_KNOWN. ) ;
#50693=EDGE_CURVE ( 'NONE', #15233, #54902, #38540, .T. ) ;
#50695=DIRECTION ( 'NONE',  ( 1.000000000000000000, 0.000000000000000000, 0.000000000000000000 ) ) ;
#50704=EDGE_CURVE ( 'NONE', #53882, #61196, #21091, .T. ) ;
#50767=LINE ( 'NONE', #61992, #42155 ) ;
#50778=ORIENTED_EDGE ( 'NONE', *, *, #32623, .F. ) ;
#50781=FACE_OUTER_BOUND ( 'NONE', #68680, .T. ) ;
#50792=DIRECTION ( 'NONE',  ( 1.000000000000000000, 0.000000000000000000, 0.000000000000000000 ) ) ;
#50807=CARTESIAN_POINT ( 'NONE',  ( -9.000000000000003553, 27.74999999999998934, 3.750000000000000000 ) ) ;
#50814=ORIENTED_EDGE ( 'NONE', *, *, #22324, .F. ) ;
#50817=PRESENTATION_STYLE_ASSIGNMENT (( #14565 ) ) ;
#50823=EDGE_CURVE ( 'NONE', #49491, #45655, #25638, .T. ) ;
#50868=ORIENTED_EDGE ( 'NONE', *, *, #3485, .T. ) ;
#50874=DIRECTION ( 'NONE',  ( 1.000000000000000000, -0.000000000000000000, -0.000000000000000000 ) ) ;
#50883=DIRECTION ( 'NONE',  ( -1.000000000000000000, 0.000000000000000000, 0.000000000000000000 ) ) ;
#50886=DIRECTION ( 'NONE',  ( 0.000000000000000000, -1.000000000000000000, 0.000000000000000000 ) ) ;
#50888=AXIS2_PLACEMENT_3D ( 'NONE', #22496, #11586, #628 ) ;
#50905=UNCERTAINTY_MEASURE_WITH_UNIT (LENGTH_MEASURE( 1.000000000000000082E-05 ), #36036, 'distance_accuracy_value', 'NONE');
#50963=ORIENTED_EDGE ( 'NONE', *, *, #1556, .F. ) ;
#50989=AXIS2_PLACEMENT_3D ( 'NONE', #4888, #25990, #41183 ) ;
#51039=LINE ( 'NONE', #61919, #16473 ) ;
#51043=CARTESIAN_POINT ( 'NONE',  ( 11.00000000000000000, 8.000000000000000000, 3.500000000000003997 ) ) ;
#51045=LINE ( 'NONE', #39829, #29134 ) ;
#51056=LINE ( 'NONE', #28528, #59706 ) ;
#51061=DIRECTION ( 'NONE',  ( -1.000000000000000000, 0.000000000000000000, 0.000000000000000000 ) ) ;
#51097=LINE ( 'NONE', #23644, #17103 ) ;
#51099=AXIS2_PLACEMENT_3D ( 'NONE', #48811, #45533, #39542 ) ;
#51111=CARTESIAN_POINT ( 'NONE',  ( -9.000000000000003553, 24.74999999999998579, -3.750000000000000000 ) ) ;
#51151=FACE_BOUND ( 'NONE', #58208, .T. ) ;
#51168=VERTEX_POINT ( 'NONE', #7220 ) ;
#51174=DIRECTION ( 'NONE',  ( -1.000000000000000000, 0.000000000000000000, 0.000000000000000000 ) ) ;
#51178=ORIENTED_EDGE ( 'NONE', *, *, #18513, .T. ) ;
#51181=AXIS2_PLACEMENT_3D ( 'NONE', #60718, #34357, #1594 ) ;
#51183=CARTESIAN_POINT ( 'NONE',  ( -13.50000000000000355, 27.99999999999998934, 3.750000000000000000 ) ) ;
#51186=ORIENTED_EDGE ( 'NONE', *, *, #13114, .T. ) ;
#51202=VECTOR ( 'NONE', #15237, 1000.000000000000000 ) ;
#51208=FACE_OUTER_BOUND ( 'NONE', #56907, .T. ) ;
#51232=CARTESIAN_POINT ( 'NONE',  ( 0.000000000000000000, 36.75000000000000000, 4.000000000000000000 ) ) ;
#51235=ADVANCED_FACE ( 'NONE', ( #12826 ), #50474, .T. ) ;
#51277=DIRECTION ( 'NONE',  ( 0.000000000000000000, 0.000000000000000000, 1.000000000000000000 ) ) ;
#51294=ORIENTED_EDGE ( 'NONE', *, *, #10650, .T. ) ;
#51324=EDGE_CURVE ( 'NONE', #47479, #20521, #11628, .T. ) ;
#51357=ORIENTED_EDGE ( 'NONE', *, *, #57841, .F. ) ;
#51374=ORIENTED_EDGE ( 'NONE', *, *, #56954, .F. ) ;
#51382=CYLINDRICAL_SURFACE ( 'NONE', #40843, 0.2500000000000002220 ) ;
#51428=LINE ( 'NONE', #66201, #46258 ) ;
#51429=ORIENTED_EDGE ( 'NONE', *, *, #63538, .T. ) ;
#51451=DIRECTION ( 'NONE',  ( 0.000000000000000000, 1.000000000000000000, 0.000000000000000000 ) ) ;
#51504=CYLINDRICAL_SURFACE ( 'NONE', #53724, 4.000000000000000000 ) ;
#51505=DIRECTION ( 'NONE',  ( -1.000000000000000000, 0.000000000000000000, 0.000000000000000000 ) ) ;
#51556=ADVANCED_FACE ( 'NONE', ( #48875 ), #30256, .T. ) ;
#51557=LINE ( 'NONE', #56844, #39246 ) ;
#51600=FACE_OUTER_BOUND ( 'NONE', #34638, .T. ) ;
#51607=DIRECTION ( 'NONE',  ( 0.000000000000000000, 1.000000000000000000, 0.000000000000000000 ) ) ;
#51610=ADVANCED_FACE ( 'NONE', ( #4511 ), #21752, .T. ) ;
#51620=ORIENTED_EDGE ( 'NONE', *, *, #43793, .T. ) ;
#51636=CARTESIAN_POINT ( 'NONE',  ( 18.25000000000000711, 31.24999999999999289, 4.000000000000000000 ) ) ;
#51654=EDGE_LOOP ( 'NONE', ( #60697, #25240, #21025 ) ) ;
#51658=CARTESIAN_POINT ( 'NONE',  ( 22.75000000000000711, 36.75000000000000000, 3.750000000000000000 ) ) ;
#51665=AXIS2_PLACEMENT_3D ( 'NONE', #45464, #23605, #55625 ) ;
#51669=EDGE_CURVE ( 'NONE', #35195, #61564, #38202, .T. ) ;
#51695=AXIS2_PLACEMENT_3D ( 'NONE', #21831, #41667, #32713 ) ;
#51715=ORIENTED_EDGE ( 'NONE', *, *, #5321, .T. ) ;
#51719=VECTOR ( 'NONE', #68063, 1000.000000000000000 ) ;
#51720=VECTOR ( 'NONE', #60493, 1000.000000000000000 ) ;
#51724=EDGE_LOOP ( 'NONE', ( #62944, #9955, #32158 ) ) ;
#51725=CARTESIAN_POINT ( 'NONE',  ( 4.750000000000002665, 24.74999999999998579, 3.750000000000000000 ) ) ;
#51748=ORIENTED_EDGE ( 'NONE', *, *, #10650, .F. ) ;
#51757=VERTEX_POINT ( 'NONE', #62488 ) ;
#51760=ORIENTED_EDGE ( 'NONE', *, *, #21126, .T. ) ;
#51769=CARTESIAN_POINT ( 'NONE',  ( -18.25000000000000711, 31.24999999999999289, 4.000000000000000000 ) ) ;
#51792=DIRECTION ( 'NONE',  ( -1.000000000000000000, 0.000000000000000000, 0.000000000000000000 ) ) ;
#51793=CARTESIAN_POINT ( 'NONE',  ( 22.75000000000000711, 36.75000000000000000, -3.750000000000000000 ) ) ;
#51861=DIRECTION ( 'NONE',  ( -1.000000000000000000, 0.000000000000000000, 0.000000000000000000 ) ) ;
#51883=ORIENTED_EDGE ( 'NONE', *, *, #15739, .F. ) ;
#51903=EDGE_LOOP ( 'NONE', ( #51186, #60860, #7142, #45771 ) ) ;
#51913=DIRECTION ( 'NONE',  ( -1.000000000000000000, 0.000000000000000000, 0.000000000000000000 ) ) ;
#51942=ORIENTED_EDGE ( 'NONE', *, *, #8958, .F. ) ;
#51945=DIRECTION ( 'NONE',  ( -0.000000000000000000, -0.000000000000000000, 1.000000000000000000 ) ) ;
#51958=EDGE_CURVE ( 'NONE', #40174, #41931, #59270, .T. ) ;
#51961=AXIS2_PLACEMENT_3D ( 'NONE', #35378, #2950, #67036 ) ;
#51977=VERTEX_POINT ( 'NONE', #491 ) ;
#51982=DIRECTION ( 'NONE',  ( 1.000000000000000000, 0.000000000000000000, 0.000000000000000000 ) ) ;
#51993=DIRECTION ( 'NONE',  ( 0.000000000000000000, 1.000000000000000000, 0.000000000000000000 ) ) ;
#52021=ORIENTED_EDGE ( 'NONE', *, *, #1980, .T. ) ;
#52049=CARTESIAN_POINT ( 'NONE',  ( -4.750000000000002665, 24.74999999999998579, 3.750000000000000000 ) ) ;
#52052=EDGE_CURVE ( 'NONE', #34405, #58037, #17788, .T. ) ;
#52067=DIRECTION ( 'NONE',  ( -0.000000000000000000, -0.000000000000000000, 1.000000000000000000 ) ) ;
#52071=ORIENTED_EDGE ( 'NONE', *, *, #29555, .T. ) ;
#52104=ORIENTED_EDGE ( 'NONE', *, *, #29879, .F. ) ;
#52140=DIRECTION ( 'NONE',  ( -0.000000000000000000, 1.000000000000000000, -0.000000000000000000 ) ) ;
#52157=AXIS2_PLACEMENT_3D ( 'NONE', #11860, #50886, #17171 ) ;
#52167=LINE ( 'NONE', #57060, #5437 ) ;
#52168=LINE ( 'NONE', #31017, #9598 ) ;
#52256=VERTEX_POINT ( 'NONE', #45238 ) ;
#52262=CIRCLE ( 'NONE', #26362, 0.2500000000000002220 ) ;
#52300=EDGE_CURVE ( 'NONE', #68529, #55377, #2586, .T. ) ;
#52332=CYLINDRICAL_SURFACE ( 'NONE', #43978, 0.2500000000000002220 ) ;
#52391=DIRECTION ( 'NONE',  ( 0.000000000000000000, 0.000000000000000000, -1.000000000000000000 ) ) ;
#52427=CIRCLE ( 'NONE', #6343, 0.5000000000000004441 ) ;
#52447=ADVANCED_FACE ( 'NONE', ( #12054 ), #27176, .T. ) ;
#52499=ORIENTED_EDGE ( 'NONE', *, *, #9476, .F. ) ;
#52500=EDGE_LOOP ( 'NONE', ( #17671, #62096, #59486, #7236 ) ) ;
#52505=DIRECTION ( 'NONE',  ( 0.000000000000000000, 0.000000000000000000, 1.000000000000000000 ) ) ;
#52531=DIRECTION ( 'NONE',  ( 0.000000000000000000, -1.000000000000000000, 0.000000000000000000 ) ) ;
#52540=DIRECTION ( 'NONE',  ( 0.000000000000000000, 0.000000000000000000, -1.000000000000000000 ) ) ;
#52543=EDGE_CURVE ( 'NONE', #9166, #50552, #3180, .T. ) ;
#52546=VERTEX_POINT ( 'NONE', #45834 ) ;
#52556=AXIS2_PLACEMENT_3D ( 'NONE', #39724, #6620, #50260 ) ;
#52558=DIRECTION ( 'NONE',  ( 0.000000000000000000, 0.000000000000000000, -1.000000000000000000 ) ) ;
#52598=DIRECTION ( 'NONE',  ( 0.000000000000000000, 0.000000000000000000, -1.000000000000000000 ) ) ;
#52614=VERTEX_POINT ( 'NONE', #64056 ) ;
#52615=DIRECTION ( 'NONE',  ( -1.000000000000000000, 0.000000000000000000, 0.000000000000000000 ) ) ;
#52622=EDGE_LOOP ( 'NONE', ( #31531, #25328 ) ) ;
#52633=CARTESIAN_POINT ( 'NONE',  ( -18.25000000000000711, 31.24999999999999289, -3.750000000000000000 ) ) ;
#52637=DIRECTION ( 'NONE',  ( 0.000000000000000000, 0.000000000000000000, 1.000000000000000000 ) ) ;
#52643=FACE_OUTER_BOUND ( 'NONE', #22343, .T. ) ;
#52659=EDGE_CURVE ( 'NONE', #9871, #59451, #39498, .T. ) ;
#52663=CARTESIAN_POINT ( 'NONE',  ( 4.250000000000001776, 22.24999999999998579, -3.750000000000000000 ) ) ;
#52665=AXIS2_PLACEMENT_3D ( 'NONE', #38807, #13065, #28533 ) ;
#52671=ORIENTED_EDGE ( 'NONE', *, *, #59335, .T. ) ;
#52705=ORIENTED_EDGE ( 'NONE', *, *, #33168, .F. ) ;
#52711=CARTESIAN_POINT ( 'NONE',  ( -22.50000000000000711, 34.24999999999999289, -3.750000000000000000 ) ) ;
#52741=EDGE_CURVE ( 'NONE', #35195, #529, #24175, .T. ) ;
#52748=ORIENTED_EDGE ( 'NONE', *, *, #47634, .F. ) ;
#52749=CARTESIAN_POINT ( 'NONE',  ( 18.25000000000000711, 33.74999999999999289, -3.750000000000000000 ) ) ;
#52796=CARTESIAN_POINT ( 'NONE',  ( -9.250000000000003553, 27.74999999999998934, -3.750000000000000000 ) ) ;
#52822=CARTESIAN_POINT ( 'NONE',  ( -15.00000000000000000, 8.000000000000000000, -3.500000000000017764 ) ) ;
#52833=ADVANCED_FACE ( 'NONE', ( #14679 ), #52332, .T. ) ;
#52902=EDGE_CURVE ( 'NONE', #36693, #39699, #24885, .T. ) ;
#52926=CARTESIAN_POINT ( 'NONE',  ( 4.500000000000002665, 22.24999999999998579, -3.750000000000000000 ) ) ;
#52928=DIRECTION ( 'NONE',  ( 0.000000000000000000, -1.000000000000000000, -8.673617379884034486E-16 ) ) ;
#52970=DIRECTION ( 'NONE',  ( -0.000000000000000000, -0.000000000000000000, 1.000000000000000000 ) ) ;
#52975=AXIS2_PLACEMENT_3D ( 'NONE', #58198, #10022, #31442 ) ;
#52991=CARTESIAN_POINT ( 'NONE',  ( -18.25000000000000711, 33.74999999999999289, -4.000000000000000000 ) ) ;
#53017=ORIENTED_EDGE ( 'NONE', *, *, #38580, .F. ) ;
#53034=AXIS2_PLACEMENT_3D ( 'NONE', #35315, #50446, #50119 ) ;
#53046=DIRECTION ( 'NONE',  ( -0.000000000000000000, -0.000000000000000000, 1.000000000000000000 ) ) ;
#53056=DIRECTION ( 'NONE',  ( 0.000000000000000000, 0.000000000000000000, -1.000000000000000000 ) ) ;
#53074=ADVANCED_FACE ( 'NONE', ( #30732 ), #46277, .T. ) ;
#53078=EDGE_CURVE ( 'NONE', #16885, #58121, #10311, .T. ) ;
#53096=DIRECTION ( 'NONE',  ( 0.000000000000000000, 0.000000000000000000, -1.000000000000000000 ) ) ;
#53139=DIRECTION ( 'NONE',  ( 0.000000000000000000, 0.000000000000000000, -1.000000000000000000 ) ) ;
#53158=EDGE_CURVE ( 'NONE', #16845, #10966, #56088, .T. ) ;
#53186=CARTESIAN_POINT ( 'NONE',  ( 0.000000000000000000, 36.75000000000000000, 3.750000000000000000 ) ) ;
#53212=CARTESIAN_POINT ( 'NONE',  ( 13.75000000000000355, 28.24999999999998934, -3.750000000000000000 ) ) ;
#53215=AXIS2_PLACEMENT_3D ( 'NONE', #52749, #4522, #32304 ) ;
#53226=EDGE_CURVE ( 'NONE', #9250, #66411, #67008, .T. ) ;
#53254=TOROIDAL_SURFACE ( 'NONE', #52157, 0.7500000000000000000, 0.2500000000000000000 ) ;
#53263=AXIS2_PLACEMENT_3D ( 'NONE', #31879, #5143, #26587 ) ;
#53289=DIRECTION ( 'NONE',  ( -0.7071067811865425767, 0.000000000000000000, -0.7071067811865525687 ) ) ;
#53296=PRODUCT_DEFINITION ( 'UNKNOWN', '', #50630, #2925 ) ;
#53311=DIRECTION ( 'NONE',  ( -9.376883653928687363E-17, 1.000000000000000000, -0.000000000000000000 ) ) ;
#53314=CIRCLE ( 'NONE', #54379, 1.000000000000000888 ) ;
#53324=LINE ( 'NONE', #10748, #62648 ) ;
#53383=CARTESIAN_POINT ( 'NONE',  ( 8.750000000000001776, 24.74999999999998579, -4.000000000000000000 ) ) ;
#53392=CIRCLE ( 'NONE', #7294, 0.2500000000000002220 ) ;
#53393=DIRECTION ( 'NONE',  ( 0.000000000000000000, -1.000000000000000000, 0.000000000000000000 ) ) ;
#53399=DIRECTION ( 'NONE',  ( 1.000000000000000000, 0.000000000000000000, 0.000000000000000000 ) ) ;
#53438=DIRECTION ( 'NONE',  ( 0.000000000000000000, 1.000000000000000000, 0.000000000000000000 ) ) ;
#53449=ORIENTED_EDGE ( 'NONE', *, *, #49830, .T. ) ;
#53474=VECTOR ( 'NONE', #11910, 1000.000000000000000 ) ;
#53475=EDGE_CURVE ( 'NONE', #52256, #43138, #26048, .T. ) ;
#53481=ORIENTED_EDGE ( 'NONE', *, *, #32025, .T. ) ;
#53483=EDGE_CURVE ( 'NONE', #59464, #42883, #51097, .T. ) ;
#53491=VERTEX_POINT ( 'NONE', #30286 ) ;
#53501=CIRCLE ( 'NONE', #38920, 0.2500000000000002220 ) ;
#53527=ADVANCED_FACE ( 'NONE', ( #25043 ), #32792, .T. ) ;
#53531=EDGE_CURVE ( 'NONE', #27999, #64410, #56344, .T. ) ;
#53544=EDGE_CURVE ( 'NONE', #1454, #56729, #42984, .T. ) ;
#53577=EDGE_CURVE ( 'NONE', #20521, #17573, #44091, .T. ) ;
#53602=FACE_OUTER_BOUND ( 'NONE', #22394, .T. ) ;
#53618=EDGE_LOOP ( 'NONE', ( #55837, #59140, #13025, #38275 ) ) ;
#53624=ADVANCED_FACE ( 'NONE', ( #6260 ), #38318, .F. ) ;
#53635=PLANE ( 'NONE',  #13991 ) ;
#53651=ORIENTED_EDGE ( 'NONE', *, *, #63152, .T. ) ;
#53673=EDGE_LOOP ( 'NONE', ( #15082, #65282, #1959 ) ) ;
#53707=CARTESIAN_POINT ( 'NONE',  ( -8.750000000000001776, 25.24999999999998934, -3.750000000000000000 ) ) ;
#53711=CARTESIAN_POINT ( 'NONE',  ( 24.00000000000000355, 36.75000000000000000, -4.000000000000000000 ) ) ;
#53722=CARTESIAN_POINT ( 'NONE',  ( -22.25000000000000711, 33.99999999999999289, 4.000000000000000000 ) ) ;
#53724=AXIS2_PLACEMENT_3D ( 'NONE', #3265, #24752, #46276 ) ;
#53744=ORIENTED_EDGE ( 'NONE', *, *, #36160, .T. ) ;
#53764=ADVANCED_FACE ( 'NONE', ( #22799 ), #17206, .F. ) ;
#53768=ORIENTED_EDGE ( 'NONE', *, *, #14311, .F. ) ;
#53778=EDGE_LOOP ( 'NONE', ( #51429, #8467, #48676 ) ) ;
#53796=AXIS2_PLACEMENT_3D ( 'NONE', #59024, #64651, #52391 ) ;
#53800=EDGE_LOOP ( 'NONE', ( #30237, #34612, #27101, #11046 ) ) ;
#53809=PLANE ( 'NONE',  #16721 ) ;
#53813=DIRECTION ( 'NONE',  ( 0.000000000000000000, 0.000000000000000000, 1.000000000000000000 ) ) ;
#53882=VERTEX_POINT ( 'NONE', #25893 ) ;
#53914=VECTOR ( 'NONE', #27944, 1000.000000000000000 ) ;
#53945=FILL_AREA_STYLE_COLOUR ( '', #41174 ) ;
#53953=EDGE_LOOP ( 'NONE', ( #8409, #2683, #43446, #57770 ) ) ;
#53971=VECTOR ( 'NONE', #18548, 1000.000000000000000 ) ;
#53998=DIRECTION ( 'NONE',  ( 0.000000000000000000, 0.000000000000000000, -1.000000000000000000 ) ) ;
#54037=ORIENTED_EDGE ( 'NONE', *, *, #15768, .F. ) ;
#54051=DIRECTION ( 'NONE',  ( 0.000000000000000000, 0.000000000000000000, -1.000000000000000000 ) ) ;
#54055=FACE_OUTER_BOUND ( 'NONE', #43127, .T. ) ;
#54066=ORIENTED_EDGE ( 'NONE', *, *, #41307, .F. ) ;
#54069=CARTESIAN_POINT ( 'NONE',  ( -15.00000000000000000, 8.000000000000000000, 4.000000000000000000 ) ) ;
#54075=ORIENTED_EDGE ( 'NONE', *, *, #28737, .F. ) ;
#54077=ADVANCED_FACE ( 'NONE', ( #58963 ), #22025, .T. ) ;
#54090=DIRECTION ( 'NONE',  ( 0.000000000000000000, 0.000000000000000000, 1.000000000000000000 ) ) ;
#54098=AXIS2_PLACEMENT_3D ( 'NONE', #4886, #53438, #20015 ) ;
#54099=DIRECTION ( 'NONE',  ( -1.000000000000000000, 0.000000000000000000, 0.000000000000000000 ) ) ;
#54106=DIRECTION ( 'NONE',  ( -1.000000000000000000, 0.000000000000000000, 0.000000000000000000 ) ) ;
#54157=AXIS2_PLACEMENT_3D ( 'NONE', #61708, #19158, #29007 ) ;
#54159=AXIS2_PLACEMENT_3D ( 'NONE', #7340, #66773, #28769 ) ;
#54164=ADVANCED_FACE ( 'NONE', ( #1182 ), #34990, .F. ) ;
#54169=CARTESIAN_POINT ( 'NONE',  ( 4.750000000000002665, 24.74999999999998579, -3.750000000000000000 ) ) ;
#54180=ORIENTED_EDGE ( 'NONE', *, *, #52300, .T. ) ;
#54187=ORIENTED_EDGE ( 'NONE', *, *, #345, .F. ) ;
#54194=DIRECTION ( 'NONE',  ( 0.000000000000000000, 0.000000000000000000, -1.000000000000000000 ) ) ;
#54212=ORIENTED_EDGE ( 'NONE', *, *, #2834, .T. ) ;
#54285=LINE ( 'NONE', #20910, #25078 ) ;
#54325=EDGE_CURVE ( 'NONE', #2782, #36655, #8963, .T. ) ;
#54343=ORIENTED_EDGE ( 'NONE', *, *, #20239, .F. ) ;
#54346=DIRECTION ( 'NONE',  ( -1.000000000000000000, 0.000000000000000000, 0.000000000000000000 ) ) ;
#54359=FACE_OUTER_BOUND ( 'NONE', #34330, .T. ) ;
#54376=CARTESIAN_POINT ( 'NONE',  ( 4.500000000000002665, 24.74999999999998579, 3.750000000000000000 ) ) ;
#54379=AXIS2_PLACEMENT_3D ( 'NONE', #10781, #32932, #11807 ) ;
#54390=VERTEX_POINT ( 'NONE', #61548 ) ;
#54459=ORIENTED_EDGE ( 'NONE', *, *, #45805, .F. ) ;
#54460=EDGE_CURVE ( 'NONE', #5580, #12869, #26044, .T. ) ;
#54498=FACE_OUTER_BOUND ( 'NONE', #53673, .T. ) ;
#54505=LINE ( 'NONE', #43334, #26157 ) ;
#54550=ADVANCED_FACE ( 'NONE', ( #43972 ), #6985, .T. ) ;
#54561=EDGE_CURVE ( 'NONE', #9250, #53882, #65425, .T. ) ;
#54594=AXIS2_PLACEMENT_3D ( 'NONE', #61748, #29043, #23117 ) ;
#54606=LINE ( 'NONE', #11005, #12256 ) ;
#54618=FACE_OUTER_BOUND ( 'NONE', #3511, .T. ) ;
#54654=CARTESIAN_POINT ( 'NONE',  ( -18.25000000000000711, 0.000000000000000000, 4.000000000000000000 ) ) ;
#54677=AXIS2_PLACEMENT_3D ( 'NONE', #29396, #61736, #67387 ) ;
#54720=ORIENTED_EDGE ( 'NONE', *, *, #52300, .F. ) ;
#54741=CARTESIAN_POINT ( 'NONE',  ( -4.250000000000001776, 21.99999999999998579, -3.750000000000000000 ) ) ;
#54781=ADVANCED_FACE ( 'NONE', ( #40585 ), #30678, .F. ) ;
#54787=ORIENTED_EDGE ( 'NONE', *, *, #61840, .F. ) ;
#54802=DIRECTION ( 'NONE',  ( -1.000000000000000000, 0.000000000000000000, 0.000000000000000000 ) ) ;
#54804=ORIENTED_EDGE ( 'NONE', *, *, #25453, .F. ) ;
#54806=CARTESIAN_POINT ( 'NONE',  ( 4.750000000000002665, 24.74999999999998579, -3.750000000000000000 ) ) ;
#54812=DIRECTION ( 'NONE',  ( -1.000000000000000000, 0.000000000000000000, 0.000000000000000000 ) ) ;
#54815=DIRECTION ( 'NONE',  ( -1.000000000000000000, 0.000000000000000000, 0.000000000000000000 ) ) ;
#54841=DIRECTION ( 'NONE',  ( 0.7071067811865425767, 8.659560562354873694E-17, -0.7071067811865525687 ) ) ;
#54850=VECTOR ( 'NONE', #69363, 1000.000000000000000 ) ;
#54874=CIRCLE ( 'NONE', #884, 0.2500000000000002220 ) ;
#54884=ORIENTED_EDGE ( 'NONE', *, *, #32096, .F. ) ;
#54888=CARTESIAN_POINT ( 'NONE',  ( 15.00000000000000000, 8.000000000000000000, 3.500000000000003997 ) ) ;
#54902=VERTEX_POINT ( 'NONE', #35290 ) ;
#54905=EDGE_CURVE ( 'NONE', #50331, #30753, #8184, .T. ) ;
#54939=VECTOR ( 'NONE', #58590, 1000.000000000000000 ) ;
#54959=DIRECTION ( 'NONE',  ( 0.000000000000000000, 0.000000000000000000, -1.000000000000000000 ) ) ;
#54971=LINE ( 'NONE', #39201, #30991 ) ;
#54990=VERTEX_POINT ( 'NONE', #31728 ) ;
#54997=FACE_OUTER_BOUND ( 'NONE', #61327, .T. ) ;
#55000=CIRCLE ( 'NONE', #11239, 0.2500000000000002220 ) ;
#55008=AXIS2_PLACEMENT_3D ( 'NONE', #33681, #60402, #65695 ) ;
#55021=VERTEX_POINT ( 'NONE', #6382 ) ;
#55052=VERTEX_POINT ( 'NONE', #65833 ) ;
#55065=AXIS2_PLACEMENT_3D ( 'NONE', #60149, #7384, #61183 ) ;
#55069=CIRCLE ( 'NONE', #68617, 0.2500000000000002220 ) ;
#55112=EDGE_CURVE ( 'NONE', #61213, #52614, #3487, .T. ) ;
#55170=ORIENTED_EDGE ( 'NONE', *, *, #19717, .T. ) ;
#55174=CARTESIAN_POINT ( 'NONE',  ( -4.750000000000002665, 24.74999999999998579, 4.000000000000000000 ) ) ;
#55201=AXIS2_PLACEMENT_3D ( 'NONE', #36019, #29688, #56410 ) ;
#55222=ORIENTED_EDGE ( 'NONE', *, *, #53577, .F. ) ;
#55226=AXIS2_PLACEMENT_3D ( 'NONE', #46409, #56569, #8401 ) ;
#55227=CARTESIAN_POINT ( 'NONE',  ( 0.000000000000000000, 0.000000000000000000, 4.000000000000000000 ) ) ;
#55251=EDGE_LOOP ( 'NONE', ( #50244, #30941, #30481, #52705 ) ) ;
#55261=ADVANCED_FACE ( 'NONE', ( #2803 ), #51382, .T. ) ;
#55266=ORIENTED_EDGE ( 'NONE', *, *, #62970, .F. ) ;
#55313=EDGE_CURVE ( 'NONE', #21392, #23152, #12679, .T. ) ;
#55316=CARTESIAN_POINT ( 'NONE',  ( -4.750000000000002665, 24.74999999999998579, -3.750000000000000000 ) ) ;
#55322=VECTOR ( 'NONE', #56404, 1000.000000000000000 ) ;
#55324=AXIS2_PLACEMENT_3D ( 'NONE', #7964, #45646, #61747 ) ;
#55350=DIRECTION ( 'NONE',  ( 1.000000000000000000, -0.000000000000000000, -0.000000000000000000 ) ) ;
#55356=ORIENTED_EDGE ( 'NONE', *, *, #55415, .F. ) ;
#55367=CYLINDRICAL_SURFACE ( 'NONE', #12272, 0.2500000000000002220 ) ;
#55368=CARTESIAN_POINT ( 'NONE',  ( -4.250000000000001776, 22.24999999999998579, -3.750000000000000000 ) ) ;
#55371=AXIS2_PLACEMENT_3D ( 'NONE', #12341, #38795, #23270 ) ;
#55377=VERTEX_POINT ( 'NONE', #266 ) ;
#55415=EDGE_CURVE ( 'NONE', #58900, #34410, #5588, .T. ) ;
#55426=EDGE_CURVE ( 'NONE', #42065, #36018, #39728, .T. ) ;
#55436=ADVANCED_FACE ( 'NONE', ( #65396 ), #33048, .T. ) ;
#55439=DIRECTION ( 'NONE',  ( -0.000000000000000000, -0.000000000000000000, -1.000000000000000000 ) ) ;
#55471=FACE_OUTER_BOUND ( 'NONE', #12496, .T. ) ;
#55480=DIRECTION ( 'NONE',  ( -1.000000000000000000, 0.000000000000000000, 0.000000000000000000 ) ) ;
#55496=ADVANCED_FACE ( 'NONE', ( #12603 ), #45017, .T. ) ;
#55522=FACE_OUTER_BOUND ( 'NONE', #51724, .T. ) ;
#55529=ORIENTED_EDGE ( 'NONE', *, *, #41915, .T. ) ;
#55546=EDGE_LOOP ( 'NONE', ( #29459, #55266, #5943, #67216 ) ) ;
#55563=VECTOR ( 'NONE', #45165, 1000.000000000000000 ) ;
#55567=ADVANCED_BREP_SHAPE_REPRESENTATION ( '', ( #49805, #42840 ), #18040 ) ;
#55620=DIRECTION ( 'NONE',  ( 0.000000000000000000, -0.000000000000000000, -1.000000000000000000 ) ) ;
#55625=DIRECTION ( 'NONE',  ( 0.000000000000000000, 0.000000000000000000, 1.000000000000000000 ) ) ;
#55629=ORIENTED_EDGE ( 'NONE', *, *, #28737, .T. ) ;
#55664=ORIENTED_EDGE ( 'NONE', *, *, #65749, .F. ) ;
#55665=DIRECTION ( 'NONE',  ( -1.000000000000000000, 0.000000000000000000, 0.000000000000000000 ) ) ;
#55697=PLANE ( 'NONE',  #69241 ) ;
#55700=ORIENTED_EDGE ( 'NONE', *, *, #69589, .F. ) ;
#55709=ORIENTED_EDGE ( 'NONE', *, *, #3191, .T. ) ;
#55739=CARTESIAN_POINT ( 'NONE',  ( 13.75000000000000533, 30.99999999999999289, -3.750000000000000000 ) ) ;
#55783=CARTESIAN_POINT ( 'NONE',  ( 13.75000000000000533, 30.74999999999999289, 3.750000000000000000 ) ) ;
#55801=ORIENTED_EDGE ( 'NONE', *, *, #40214, .T. ) ;
#55805=DIRECTION ( 'NONE',  ( 0.000000000000000000, -1.000000000000000000, 0.000000000000000000 ) ) ;
#55807=EDGE_LOOP ( 'NONE', ( #32963, #41708, #29453, #22376 ) ) ;
#55837=ORIENTED_EDGE ( 'NONE', *, *, #41366, .T. ) ;
#55864=VERTEX_POINT ( 'NONE', #67740 ) ;
#55873=CARTESIAN_POINT ( 'NONE',  ( -24.00000000000000000, 1.000000000000000000, -3.000000000000000000 ) ) ;
#55892=ORIENTED_EDGE ( 'NONE', *, *, #37380, .F. ) ;
#55896=AXIS2_PLACEMENT_3D ( 'NONE', #26370, #57708, #47192 ) ;
#55925=ORIENTED_EDGE ( 'NONE', *, *, #29203, .T. ) ;
#55934=ORIENTED_EDGE ( 'NONE', *, *, #68287, .T. ) ;
#55937=ADVANCED_FACE ( 'NONE', ( #30781 ), #25193, .T. ) ;
#55972=DIRECTION ( 'NONE',  ( 0.000000000000000000, 0.000000000000000000, -1.000000000000000000 ) ) ;
#55976=EDGE_CURVE ( 'NONE', #17294, #6425, #68104, .T. ) ;
#56001=CARTESIAN_POINT ( 'NONE',  ( -24.00000000000000355, 36.75000000000000000, 3.000000000000000000 ) ) ;
#56015=AXIS2_PLACEMENT_3D ( 'NONE', #67901, #45089, #45441 ) ;
#56036=CARTESIAN_POINT ( 'NONE',  ( 13.25000000000000355, 28.24999999999998934, 4.000000000000000000 ) ) ;
#56070=AXIS2_PLACEMENT_3D ( 'NONE', #61002, #18107, #40625 ) ;
#56078=CARTESIAN_POINT ( 'NONE',  ( 24.00000000000000355, 37.00000000000000000, 3.750000000000000000 ) ) ;
#56088=LINE ( 'NONE', #14230, #34994 ) ;
#56094=CYLINDRICAL_SURFACE ( 'NONE', #20265, 0.2500000000000002220 ) ;
#56130=CARTESIAN_POINT ( 'NONE',  ( 4.250000000000001776, 22.24999999999998579, 4.000000000000000000 ) ) ;
#56135=ORIENTED_EDGE ( 'NONE', *, *, #17518, .F. ) ;
#56149=ORIENTED_EDGE ( 'NONE', *, *, #45328, .F. ) ;
#56158=DIRECTION ( 'NONE',  ( -0.000000000000000000, -0.000000000000000000, 1.000000000000000000 ) ) ;
#56187=DIRECTION ( 'NONE',  ( -0.000000000000000000, -0.000000000000000000, 1.000000000000000000 ) ) ;
#56212=EDGE_LOOP ( 'NONE', ( #47679, #20693, #49768, #30744 ) ) ;
#56220=ORIENTED_EDGE ( 'NONE', *, *, #50364, .T. ) ;
#56264=VECTOR ( 'NONE', #23399, 1000.000000000000000 ) ;
#56272=DIRECTION ( 'NONE',  ( 0.000000000000000000, 0.000000000000000000, -1.000000000000000000 ) ) ;
#56313=ADVANCED_FACE ( 'NONE', ( #21957 ), #69441, .T. ) ;
#56318=VECTOR ( 'NONE', #20203, 1000.000000000000000 ) ;
#56319=FACE_OUTER_BOUND ( 'NONE', #14783, .T. ) ;
#56325=AXIS2_PLACEMENT_3D ( 'NONE', #30834, #24498, #46013 ) ;
#56326=DIRECTION ( 'NONE',  ( 0.000000000000000000, 0.000000000000000000, -1.000000000000000000 ) ) ;
#56330=CIRCLE ( 'NONE', #3520, 0.2500000000000002220 ) ;
#56332=DIRECTION ( 'NONE',  ( 1.000000000000000000, 0.000000000000000000, 0.000000000000000000 ) ) ;
#56333=EDGE_CURVE ( 'NONE', #23842, #50598, #38522, .T. ) ;
#56342=LINE ( 'NONE', #3173, #68546 ) ;
#56344=LINE ( 'NONE', #19045, #2391 ) ;
#56348=DIRECTION ( 'NONE',  ( -0.000000000000000000, -0.000000000000000000, 1.000000000000000000 ) ) ;
#56373=AXIS2_PLACEMENT_3D ( 'NONE', #45513, #3176, #55665 ) ;
#56404=DIRECTION ( 'NONE',  ( -0.000000000000000000, -0.000000000000000000, 1.000000000000000000 ) ) ;
#56408=CIRCLE ( 'NONE', #26073, 0.2500000000000002220 ) ;
#56410=DIRECTION ( 'NONE',  ( -1.000000000000000000, 0.000000000000000000, 0.000000000000000000 ) ) ;
#56434=CARTESIAN_POINT ( 'NONE',  ( -15.00000000000000000, 8.000000000000000000, 4.000000000000000000 ) ) ;
#56471=EDGE_CURVE ( 'NONE', #58037, #55052, #45527, .T. ) ;
#56486=CARTESIAN_POINT ( 'NONE',  ( -18.00000000000000711, 30.99999999999999289, 3.750000000000000000 ) ) ;
#56494=DIRECTION ( 'NONE',  ( 0.000000000000000000, 1.000000000000000000, 0.000000000000000000 ) ) ;
#56569=DIRECTION ( 'NONE',  ( -1.000000000000000000, 0.000000000000000000, 0.000000000000000000 ) ) ;
#56570=ORIENTED_EDGE ( 'NONE', *, *, #22798, .F. ) ;
#56576=DIRECTION ( 'NONE',  ( 0.000000000000000000, 0.000000000000000000, -1.000000000000000000 ) ) ;
#56579=TOROIDAL_SURFACE ( 'NONE', #22906, 0.5000000000000000000, 0.2500000000000000000 ) ;
#56598=LINE ( 'NONE', #8062, #13571 ) ;
#56614=ORIENTED_EDGE ( 'NONE', *, *, #12368, .F. ) ;
#56618=CIRCLE ( 'NONE', #19501, 0.2500000000000002220 ) ;
#56622=DIRECTION ( 'NONE',  ( 0.000000000000000000, -0.000000000000000000, 1.000000000000000000 ) ) ;
#56625=ORIENTED_EDGE ( 'NONE', *, *, #28203, .F. ) ;
#56635=ORIENTED_EDGE ( 'NONE', *, *, #36828, .F. ) ;
#56664=DIRECTION ( 'NONE',  ( 0.000000000000000000, 1.000000000000000000, 0.000000000000000000 ) ) ;
#56671=DIRECTION ( 'NONE',  ( 0.000000000000000000, 0.000000000000000000, -1.000000000000000000 ) ) ;
#56676=EDGE_LOOP ( 'NONE', ( #56755, #49218, #5335, #26471 ) ) ;
#56706=DIRECTION ( 'NONE',  ( 0.000000000000000000, 0.000000000000000000, -1.000000000000000000 ) ) ;
#56711=DIRECTION ( 'NONE',  ( 0.000000000000000000, 0.000000000000000000, -1.000000000000000000 ) ) ;
#56724=VECTOR ( 'NONE', #50874, 1000.000000000000000 ) ;
#56729=VERTEX_POINT ( 'NONE', #339 ) ;
#56742=CIRCLE ( 'NONE', #17450, 1.000000000000000000 ) ;
#56755=ORIENTED_EDGE ( 'NONE', *, *, #14311, .T. ) ;
#56760=DIRECTION ( 'NONE',  ( 1.000000000000000000, 0.000000000000000000, 0.000000000000000000 ) ) ;
#56763=VERTEX_POINT ( 'NONE', #20835 ) ;
#56798=CARTESIAN_POINT ( 'NONE',  ( 9.250000000000003553, 27.99999999999998934, -3.750000000000000000 ) ) ;
#56836=DIRECTION ( 'NONE',  ( 0.000000000000000000, -0.000000000000000000, 1.000000000000000000 ) ) ;
#56844=CARTESIAN_POINT ( 'NONE',  ( 18.00000000000000711, 30.99999999999999289, 3.750000000000000000 ) ) ;
#56907=EDGE_LOOP ( 'NONE', ( #36951, #8989, #43997 ) ) ;
#56932=CARTESIAN_POINT ( 'NONE',  ( 9.250000000000003553, 27.74999999999998934, 4.000000000000000000 ) ) ;
#56948=EDGE_CURVE ( 'NONE', #33026, #46607, #25345, .T. ) ;
#56954=EDGE_CURVE ( 'NONE', #57180, #27282, #68591, .T. ) ;
#56970=ORIENTED_EDGE ( 'NONE', *, *, #49349, .F. ) ;
#57015=AXIS2_PLACEMENT_3D ( 'NONE', #15379, #47393, #11083 ) ;
#57017=ORIENTED_EDGE ( 'NONE', *, *, #33077, .F. ) ;
#57060=CARTESIAN_POINT ( 'NONE',  ( -24.00000000000000000, 0.000000000000000000, 4.000000000000000000 ) ) ;
#57154=ORIENTED_EDGE ( 'NONE', *, *, #1927, .F. ) ;
#57166=EDGE_CURVE ( 'NONE', #65417, #17573, #918, .T. ) ;
#57180=VERTEX_POINT ( 'NONE', #7335 ) ;
#57185=DIRECTION ( 'NONE',  ( 0.000000000000000000, -0.000000000000000000, -1.000000000000000000 ) ) ;
#57186=LINE ( 'NONE', #19895, #7732 ) ;
#57265=DIRECTION ( 'NONE',  ( 0.000000000000000000, 0.000000000000000000, -1.000000000000000000 ) ) ;
#57299=AXIS2_PLACEMENT_3D ( 'NONE', #16248, #15890, #37371 ) ;
#57317=ORIENTED_EDGE ( 'NONE', *, *, #23212, .F. ) ;
#57346=ORIENTED_EDGE ( 'NONE', *, *, #60667, .T. ) ;
#57402=DIRECTION ( 'NONE',  ( -1.000000000000000000, 0.000000000000000000, 0.000000000000000000 ) ) ;
#57412=ORIENTED_EDGE ( 'NONE', *, *, #24142, .T. ) ;
#57422=ORIENTED_EDGE ( 'NONE', *, *, #63152, .F. ) ;
#57437=EDGE_CURVE ( 'NONE', #68501, #65417, #10710, .T. ) ;
#57443=ORIENTED_EDGE ( 'NONE', *, *, #39961, .T. ) ;
#57476=( NAMED_UNIT ( * ) PLANE_ANGLE_UNIT ( ) SI_UNIT ( $, .RADIAN. ) );
#57481=CARTESIAN_POINT ( 'NONE',  ( -15.00000000000000000, 8.000000000000000000, -4.000000000000000000 ) ) ;
#57502=FACE_OUTER_BOUND ( 'NONE', #8281, .T. ) ;
#57514=EDGE_CURVE ( 'NONE', #26708, #65395, #45668, .T. ) ;
#57564=AXIS2_PLACEMENT_3D ( 'NONE', #43273, #26999, #59043 ) ;
#57593=ORIENTED_EDGE ( 'NONE', *, *, #9785, .F. ) ;
#57621=CYLINDRICAL_SURFACE ( 'NONE', #55226, 0.2500000000000002220 ) ;
#57641=AXIS2_PLACEMENT_3D ( 'NONE', #18242, #22840, #54812 ) ;
#57664=CARTESIAN_POINT ( 'NONE',  ( -25.00000000000000000, 1.000000000000000000, -4.000000000000000000 ) ) ;
#57669=ORIENTED_EDGE ( 'NONE', *, *, #42075, .F. ) ;
#57677=ADVANCED_FACE ( 'NONE', ( #67292 ), #55697, .F. ) ;
#57708=DIRECTION ( 'NONE',  ( 0.000000000000000000, 1.000000000000000000, -0.000000000000000000 ) ) ;
#57713=DIRECTION ( 'NONE',  ( 0.000000000000000000, -1.000000000000000000, 0.000000000000000000 ) ) ;
#57716=CARTESIAN_POINT ( 'NONE',  ( -17.75000000000000711, 30.99999999999999289, -3.750000000000000000 ) ) ;
#57755=DIRECTION ( 'NONE',  ( -1.000000000000000000, 0.000000000000000000, 0.000000000000000000 ) ) ;
#57770=ORIENTED_EDGE ( 'NONE', *, *, #8587, .T. ) ;
#57788=CARTESIAN_POINT ( 'NONE',  ( -13.75000000000000533, 30.99999999999999289, -3.750000000000000000 ) ) ;
#57804=EDGE_LOOP ( 'NONE', ( #35075, #38560, #51620, #69469 ) ) ;
#57841=EDGE_CURVE ( 'NONE', #69641, #28845, #16338, .T. ) ;
#57861=CARTESIAN_POINT ( 'NONE',  ( -24.00000000000000355, 37.00000000000000000, -3.750000000000000000 ) ) ;
#57889=LINE ( 'NONE', #62782, #63785 ) ;
#57952=CARTESIAN_POINT ( 'NONE',  ( 9.250000000000003553, 27.99999999999998934, -3.750000000000000000 ) ) ;
#57969=ORIENTED_EDGE ( 'NONE', *, *, #64148, .F. ) ;
#57976=CIRCLE ( 'NONE', #54594, 0.5000000000000004441 ) ;
#57980=CARTESIAN_POINT ( 'NONE',  ( -4.750000000000002665, 22.24999999999998579, 3.750000000000000000 ) ) ;
#57984=ORIENTED_EDGE ( 'NONE', *, *, #68140, .T. ) ;
#57989=ADVANCED_FACE ( 'NONE', ( #7441 ), #60521, .F. ) ;
#58015=DIRECTION ( 'NONE',  ( -1.000000000000000000, 0.000000000000000000, 0.000000000000000000 ) ) ;
#58021=ORIENTED_EDGE ( 'NONE', *, *, #20239, .T. ) ;
#58037=VERTEX_POINT ( 'NONE', #28516 ) ;
#58039=EDGE_LOOP ( 'NONE', ( #64720, #66046, #28771, #24183 ) ) ;
#58049=ADVANCED_FACE ( 'NONE', ( #28862 ), #50017, .T. ) ;
#58067=VERTEX_POINT ( 'NONE', #23263 ) ;
#58080=ADVANCED_FACE ( 'NONE', ( #66879 ), #12691, .F. ) ;
#58099=UNCERTAINTY_MEASURE_WITH_UNIT (LENGTH_MEASURE( 1.000000000000000082E-05 ), #44153, 'distance_accuracy_value', 'NONE');
#58104=CARTESIAN_POINT ( 'NONE',  ( 22.50000000000000711, 36.75000000000000000, 3.750000000000000000 ) ) ;
#58117=CARTESIAN_POINT ( 'NONE',  ( 9.000000000000003553, 27.74999999999998934, 3.750000000000000000 ) ) ;
#58121=VERTEX_POINT ( 'NONE', #14103 ) ;
#58149=CARTESIAN_POINT ( 'NONE',  ( 4.250000000000001776, 22.24999999999998579, -3.750000000000000000 ) ) ;
#58151=VERTEX_POINT ( 'NONE', #3125 ) ;
#58196=ORIENTED_EDGE ( 'NONE', *, *, #12485, .F. ) ;
#58197=AXIS2_PLACEMENT_3D ( 'NONE', #3339, #51945, #41406 ) ;
#58198=CARTESIAN_POINT ( 'NONE',  ( -4.250000000000001776, 22.24999999999998579, 4.000000000000000000 ) ) ;
#58202=ORIENTED_EDGE ( 'NONE', *, *, #35110, .F. ) ;
#58208=EDGE_LOOP ( 'NONE', ( #64692, #8193 ) ) ;
#58304=DIRECTION ( 'NONE',  ( 0.000000000000000000, 0.000000000000000000, -1.000000000000000000 ) ) ;
#58314=VERTEX_POINT ( 'NONE', #17241 ) ;
#58331=AXIS2_PLACEMENT_3D ( 'NONE', #21996, #32190, #42447 ) ;
#58334=DIRECTION ( 'NONE',  ( 0.000000000000000000, 0.000000000000000000, -1.000000000000000000 ) ) ;
#58339=EDGE_CURVE ( 'NONE', #14152, #44124, #65734, .T. ) ;
#58341=ORIENTED_EDGE ( 'NONE', *, *, #67674, .F. ) ;
#58342=CARTESIAN_POINT ( 'NONE',  ( -4.250000000000001776, 22.24999999999998579, 3.750000000000000000 ) ) ;
#58350=DIRECTION ( 'NONE',  ( -1.000000000000000000, 0.000000000000000000, 0.000000000000000000 ) ) ;
#58354=AXIS2_PLACEMENT_3D ( 'NONE', #10413, #5434, #52637 ) ;
#58357=ORIENTED_EDGE ( 'NONE', *, *, #67281, .T. ) ;
#58370=EDGE_CURVE ( 'NONE', #21095, #55864, #39043, .T. ) ;
#58383=EDGE_LOOP ( 'NONE', ( #45222, #21133, #3015 ) ) ;
#58386=EDGE_LOOP ( 'NONE', ( #56625, #45440, #59866, #13031 ) ) ;
#58399=DIRECTION ( 'NONE',  ( 0.000000000000000000, -1.000000000000000000, 0.000000000000000000 ) ) ;
#58409=DIRECTION ( 'NONE',  ( -1.000000000000000000, 0.000000000000000000, 0.000000000000000000 ) ) ;
#58444=EDGE_CURVE ( 'NONE', #60451, #17311, #5301, .T. ) ;
#58473=DIRECTION ( 'NONE',  ( 0.000000000000000000, 1.000000000000000000, 0.000000000000000000 ) ) ;
#58544=EDGE_LOOP ( 'NONE', ( #26035, #18601, #29160, #14321 ) ) ;
#58577=PRODUCT_DEFINITION_SHAPE ( 'NONE', 'NONE',  #53296 ) ;
#58580=CIRCLE ( 'NONE', #55201, 0.2500000000000002220 ) ;
#58584=FACE_OUTER_BOUND ( 'NONE', #41798, .T. ) ;
#58590=DIRECTION ( 'NONE',  ( 1.000000000000000000, -0.000000000000000000, -0.000000000000000000 ) ) ;
#58607=DIRECTION ( 'NONE',  ( -1.000000000000000000, -5.782411586589331015E-16, 0.000000000000000000 ) ) ;
#58625=AXIS2_PLACEMENT_3D ( 'NONE', #11694, #23626, #38484 ) ;
#58647=DIRECTION ( 'NONE',  ( 1.000000000000000000, 0.000000000000000000, 0.000000000000000000 ) ) ;
#58653=DIRECTION ( 'NONE',  ( 0.000000000000000000, 0.000000000000000000, -1.000000000000000000 ) ) ;
#58659=VERTEX_POINT ( 'NONE', #53383 ) ;
#58661=DIRECTION ( 'NONE',  ( -0.000000000000000000, -0.000000000000000000, 1.000000000000000000 ) ) ;
#58671=FACE_OUTER_BOUND ( 'NONE', #3009, .T. ) ;
#58693=ADVANCED_FACE ( 'NONE', ( #27643 ), #33305, .T. ) ;
#58700=VERTEX_POINT ( 'NONE', #65650 ) ;
#58764=CIRCLE ( 'NONE', #61003, 0.2500000000000002220 ) ;
#58774=CIRCLE ( 'NONE', #53215, 0.2500000000000002220 ) ;
#58849=AXIS2_PLACEMENT_3D ( 'NONE', #52822, #15542, #69337 ) ;
#58850=ORIENTED_EDGE ( 'NONE', *, *, #21157, .T. ) ;
#58854=CIRCLE ( 'NONE', #27334, 0.5000000000000004441 ) ;
#58862=FACE_OUTER_BOUND ( 'NONE', #64859, .T. ) ;
#58896=ORIENTED_EDGE ( 'NONE', *, *, #54905, .T. ) ;
#58900=VERTEX_POINT ( 'NONE', #13921 ) ;
#58902=CARTESIAN_POINT ( 'NONE',  ( 15.00000000000000000, 8.000000000000000000, -4.000000000000000000 ) ) ;
#58934=ADVANCED_FACE ( 'NONE', ( #39999 ), #19878, .F. ) ;
#58963=FACE_OUTER_BOUND ( 'NONE', #34083, .T. ) ;
#58978=VERTEX_POINT ( 'NONE', #26857 ) ;
#58996=LINE ( 'NONE', #65309, #59638 ) ;
#59014=EDGE_CURVE ( 'NONE', #50552, #17866, #22666, .T. ) ;
#59024=CARTESIAN_POINT ( 'NONE',  ( -4.750000000000002665, 24.74999999999998579, 3.750000000000000000 ) ) ;
#59035=DIRECTION ( 'NONE',  ( -0.000000000000000000, 0.000000000000000000, -1.000000000000000000 ) ) ;
#59043=DIRECTION ( 'NONE',  ( 0.000000000000000000, 0.000000000000000000, 1.000000000000000000 ) ) ;
#59060=TOROIDAL_SURFACE ( 'NONE', #28718, 0.5000000000000000000, 0.2500000000000000000 ) ;
#59078=ORIENTED_EDGE ( 'NONE', *, *, #48807, .T. ) ;
#59093=ORIENTED_EDGE ( 'NONE', *, *, #6267, .F. ) ;
#59095=EDGE_CURVE ( 'NONE', #67644, #13443, #7776, .T. ) ;
#59103=VECTOR ( 'NONE', #61524, 1000.000000000000000 ) ;
#59104=ADVANCED_FACE ( 'NONE', ( #47200 ), #62973, .F. ) ;
#59118=ORIENTED_EDGE ( 'NONE', *, *, #61376, .F. ) ;
#59140=ORIENTED_EDGE ( 'NONE', *, *, #20702, .T. ) ;
#59216=FACE_OUTER_BOUND ( 'NONE', #56212, .T. ) ;
#59222=ADVANCED_FACE ( 'NONE', ( #23517 ), #12259, .T. ) ;
#59227=AXIS2_PLACEMENT_3D ( 'NONE', #28691, #43896, #2246 ) ;
#59234=ADVANCED_FACE ( 'NONE', ( #44350 ), #50613, .T. ) ;
#59237=DIRECTION ( 'NONE',  ( 0.000000000000000000, 0.000000000000000000, -1.000000000000000000 ) ) ;
#59260=CARTESIAN_POINT ( 'NONE',  ( 18.00000000000000711, 31.24999999999999289, 4.000000000000000000 ) ) ;
#59265=CARTESIAN_POINT ( 'NONE',  ( 22.50000000000000711, 34.24999999999999289, -3.750000000000000000 ) ) ;
#59270=LINE ( 'NONE', #37195, #14619 ) ;
#59271=CIRCLE ( 'NONE', #60439, 0.2500000000000002220 ) ;
#59300=ADVANCED_FACE ( 'NONE', ( #3407 ), #29839, .T. ) ;
#59320=ORIENTED_EDGE ( 'NONE', *, *, #33168, .T. ) ;
#59322=EDGE_LOOP ( 'NONE', ( #69022, #41713, #16132 ) ) ;
#59335=EDGE_CURVE ( 'NONE', #59464, #20746, #68575, .T. ) ;
#59353=VECTOR ( 'NONE', #53046, 1000.000000000000000 ) ;
#59363=EDGE_CURVE ( 'NONE', #66883, #41176, #7901, .T. ) ;
#59367=FACE_OUTER_BOUND ( 'NONE', #21864, .T. ) ;
#59411=ORIENTED_EDGE ( 'NONE', *, *, #44370, .T. ) ;
#59419=CARTESIAN_POINT ( 'NONE',  ( 9.000000000000003553, 27.99999999999998934, 4.000000000000000000 ) ) ;
#59425=DIRECTION ( 'NONE',  ( -1.000000000000000000, 0.000000000000000000, 0.000000000000000000 ) ) ;
#59446=CIRCLE ( 'NONE', #51695, 4.000000000000000000 ) ;
#59451=VERTEX_POINT ( 'NONE', #31564 ) ;
#59464=VERTEX_POINT ( 'NONE', #53711 ) ;
#59486=ORIENTED_EDGE ( 'NONE', *, *, #27051, .F. ) ;
#59498=ORIENTED_EDGE ( 'NONE', *, *, #50438, .F. ) ;
#59520=DIRECTION ( 'NONE',  ( -0.000000000000000000, -0.000000000000000000, -1.000000000000000000 ) ) ;
#59574=AXIS2_PLACEMENT_3D ( 'NONE', #2930, #41001, #4332 ) ;
#59603=ORIENTED_EDGE ( 'NONE', *, *, #15448, .F. ) ;
#59621=LINE ( 'NONE', #59260, #39418 ) ;
#59626=AXIS2_PLACEMENT_3D ( 'NONE', #69100, #20901, #37822 ) ;
#59631=EDGE_CURVE ( 'NONE', #54902, #43549, #61872, .T. ) ;
#59638=VECTOR ( 'NONE', #11840, 1000.000000000000000 ) ;
#59676=DIRECTION ( 'NONE',  ( 0.000000000000000000, 0.000000000000000000, -1.000000000000000000 ) ) ;
#59679=AXIS2_PLACEMENT_3D ( 'NONE', #21665, #16077, #58607 ) ;
#59692=DIRECTION ( 'NONE',  ( -0.7071067811865474617, 8.659560562354932858E-17, 0.7071067811865474617 ) ) ;
#59701=ADVANCED_FACE ( 'NONE', ( #49189 ), #64668, .T. ) ;
#59702=DIRECTION ( 'NONE',  ( 5.782411586589351722E-16, 1.000000000000000000, 0.000000000000000000 ) ) ;
#59706=VECTOR ( 'NONE', #39839, 1000.000000000000000 ) ;
#59723=AXIS2_PLACEMENT_3D ( 'NONE', #24392, #9644, #68367 ) ;
#59737=CARTESIAN_POINT ( 'NONE',  ( 13.25000000000000355, 27.99999999999998934, 3.750000000000000000 ) ) ;
#59769=CYLINDRICAL_SURFACE ( 'NONE', #46478, 0.2500000000000002220 ) ;
#59777=AXIS2_PLACEMENT_3D ( 'NONE', #16923, #1350, #44028 ) ;
#59782=AXIS2_PLACEMENT_3D ( 'NONE', #23407, #7585, #8986 ) ;
#59787=ORIENTED_EDGE ( 'NONE', *, *, #47883, .F. ) ;
#59825=CARTESIAN_POINT ( 'NONE',  ( -22.75000000000000711, 37.00000000000000000, 4.000000000000000000 ) ) ;
#59836=AXIS2_PLACEMENT_3D ( 'NONE', #51793, #37405, #69369 ) ;
#59866=ORIENTED_EDGE ( 'NONE', *, *, #9722, .F. ) ;
#59868=CARTESIAN_POINT ( 'NONE',  ( -18.25000000000000711, 33.74999999999999289, -3.750000000000000000 ) ) ;
#59876=FACE_OUTER_BOUND ( 'NONE', #65481, .T. ) ;
#59884=CIRCLE ( 'NONE', #67777, 0.2500000000000002220 ) ;
#59886=VECTOR ( 'NONE', #20768, 1000.000000000000000 ) ;
#59914=AXIS2_PLACEMENT_3D ( 'NONE', #24265, #66855, #18316 ) ;
#59931=DIRECTION ( 'NONE',  ( 0.000000000000000000, -1.000000000000000000, 0.000000000000000000 ) ) ;
#59932=DIRECTION ( 'NONE',  ( -0.000000000000000000, -0.000000000000000000, 1.000000000000000000 ) ) ;
#59949=VECTOR ( 'NONE', #29560, 1000.000000000000000 ) ;
#59958=ORIENTED_EDGE ( 'NONE', *, *, #26733, .T. ) ;
#59959=EDGE_CURVE ( 'NONE', #1454, #23924, #26149, .T. ) ;
#59968=ADVANCED_FACE ( 'NONE', ( #48021 ), #67083, .T. ) ;
#59977=CARTESIAN_POINT ( 'NONE',  ( 0.000000000000000000, 0.000000000000000000, 0.000000000000000000 ) ) ;
#60027=CARTESIAN_POINT ( 'NONE',  ( 22.50000000000000711, 33.74999999999999289, -3.750000000000000000 ) ) ;
#60041=DIRECTION ( 'NONE',  ( -1.000000000000000000, 0.000000000000000000, 0.000000000000000000 ) ) ;
#60052=DIRECTION ( 'NONE',  ( -1.000000000000000000, 0.000000000000000000, 0.000000000000000000 ) ) ;
#60070=CARTESIAN_POINT ( 'NONE',  ( 4.750000000000002665, 22.24999999999998579, 4.000000000000000000 ) ) ;
#60076=CARTESIAN_POINT ( 'NONE',  ( 17.75000000000000711, 31.24999999999999289, -4.000000000000000000 ) ) ;
#60102=ORIENTED_EDGE ( 'NONE', *, *, #58339, .F. ) ;
#60104=LINE ( 'NONE', #48914, #37982 ) ;
#60116=CARTESIAN_POINT ( 'NONE',  ( 24.00000000000000000, 1.000000000000000000, 3.000000000000000000 ) ) ;
#60149=CARTESIAN_POINT ( 'NONE',  ( 25.00000000000000355, 37.00000000000000000, 4.000000000000000000 ) ) ;
#60170=EDGE_CURVE ( 'NONE', #66608, #43138, #51428, .T. ) ;
#60175=ORIENTED_EDGE ( 'NONE', *, *, #19717, .F. ) ;
#60279=DIRECTION ( 'NONE',  ( -1.000000000000000000, 0.000000000000000000, 0.000000000000000000 ) ) ;
#60297=DIRECTION ( 'NONE',  ( 0.000000000000000000, 0.000000000000000000, -1.000000000000000000 ) ) ;
#60305=CIRCLE ( 'NONE', #21046, 1.000000000000000000 ) ;
#60322=CARTESIAN_POINT ( 'NONE',  ( -22.75000000000000711, 36.75000000000000000, 3.750000000000000000 ) ) ;
#60328=FACE_OUTER_BOUND ( 'NONE', #68982, .T. ) ;
#60340=LINE ( 'NONE', #37911, #47492 ) ;
#60364=EDGE_CURVE ( 'NONE', #38885, #37037, #49279, .T. ) ;
#60367=ORIENTED_EDGE ( 'NONE', *, *, #46021, .F. ) ;
#60368=CARTESIAN_POINT ( 'NONE',  ( -4.250000000000001776, 21.74999999999998579, 3.750000000000000000 ) ) ;
#60381=FACE_OUTER_BOUND ( 'NONE', #11989, .T. ) ;
#60397=VECTOR ( 'NONE', #49450, 1000.000000000000000 ) ;
#60402=DIRECTION ( 'NONE',  ( 0.000000000000000000, -0.000000000000000000, -1.000000000000000000 ) ) ;
#60403=AXIS2_PLACEMENT_3D ( 'NONE', #41677, #69417, #42388 ) ;
#60418=VERTEX_POINT ( 'NONE', #66487 ) ;
#60439=AXIS2_PLACEMENT_3D ( 'NONE', #52633, #15364, #26876 ) ;
#60446=CARTESIAN_POINT ( 'NONE',  ( -10.50000000000002309, 8.000000000000000000, -4.000000000000000000 ) ) ;
#60451=VERTEX_POINT ( 'NONE', #61521 ) ;
#60490=ORIENTED_EDGE ( 'NONE', *, *, #66388, .F. ) ;
#60492=ORIENTED_EDGE ( 'NONE', *, *, #8007, .T. ) ;
#60493=DIRECTION ( 'NONE',  ( -0.000000000000000000, -1.000000000000000000, -0.000000000000000000 ) ) ;
#60519=CIRCLE ( 'NONE', #58331, 0.5000000000000004441 ) ;
#60521=CYLINDRICAL_SURFACE ( 'NONE', #43336, 0.2500000000000002220 ) ;
#60541=CARTESIAN_POINT ( 'NONE',  ( 24.00000000000000000, 0.000000000000000000, -3.000000000000000000 ) ) ;
#60549=ORIENTED_EDGE ( 'NONE', *, *, #34142, .T. ) ;
#60596=SURFACE_STYLE_USAGE ( .BOTH. , #27882 ) ;
#60599=FACE_OUTER_BOUND ( 'NONE', #63747, .T. ) ;
#60623=DIRECTION ( 'NONE',  ( 1.000000000000000000, 0.000000000000000000, 0.000000000000000000 ) ) ;
#60652=EDGE_CURVE ( 'NONE', #65139, #43795, #60914, .T. ) ;
#60667=EDGE_CURVE ( 'NONE', #36693, #34405, #49696, .T. ) ;
#60671=VECTOR ( 'NONE', #22713, 1000.000000000000000 ) ;
#60680=LINE ( 'NONE', #12148, #8367 ) ;
#60688=FACE_OUTER_BOUND ( 'NONE', #32311, .T. ) ;
#60697=ORIENTED_EDGE ( 'NONE', *, *, #61687, .F. ) ;
#60718=CARTESIAN_POINT ( 'NONE',  ( -9.250000000000003553, 27.99999999999998934, -3.750000000000000000 ) ) ;
#60721=CARTESIAN_POINT ( 'NONE',  ( -24.00000000000000000, 1.000000000000000000, 4.000000000000000000 ) ) ;
#60744=DIRECTION ( 'NONE',  ( -1.000000000000000000, 0.000000000000000000, 0.000000000000000000 ) ) ;
#60746=CARTESIAN_POINT ( 'NONE',  ( -22.50000000000000711, 37.00000000000000000, 4.000000000000000000 ) ) ;
#60754=VECTOR ( 'NONE', #37007, 1000.000000000000000 ) ;
#60769=ORIENTED_EDGE ( 'NONE', *, *, #41171, .T. ) ;
#60774=ORIENTED_EDGE ( 'NONE', *, *, #6056, .T. ) ;
#60785=CARTESIAN_POINT ( 'NONE',  ( -13.50000000000000533, 30.99999999999999289, 4.000000000000000000 ) ) ;
#60793=CARTESIAN_POINT ( 'NONE',  ( -8.750000000000001776, 24.99999999999998579, 4.000000000000000000 ) ) ;
#60804=CARTESIAN_POINT ( 'NONE',  ( 15.00000000000000000, 8.000000000000000000, -4.000000000000000000 ) ) ;
#60821=ADVANCED_FACE ( 'NONE', ( #51600 ), #47416, .F. ) ;
#60860=ORIENTED_EDGE ( 'NONE', *, *, #69557, .T. ) ;
#60914=CIRCLE ( 'NONE', #57564, 0.2500000000000002220 ) ;
#60969=EDGE_LOOP ( 'NONE', ( #8647, #31881, #55664 ) ) ;
#60974=ORIENTED_EDGE ( 'NONE', *, *, #41366, .F. ) ;
#60979=CARTESIAN_POINT ( 'NONE',  ( 4.250000000000001776, 22.24999999999998579, -4.000000000000000000 ) ) ;
#61002=CARTESIAN_POINT ( 'NONE',  ( 13.75000000000000533, 30.74999999999999289, 4.000000000000000000 ) ) ;
#61003=AXIS2_PLACEMENT_3D ( 'NONE', #46158, #9557, #58409 ) ;
#61018=DIRECTION ( 'NONE',  ( -1.000000000000000000, 0.000000000000000000, 0.000000000000000000 ) ) ;
#61035=CARTESIAN_POINT ( 'NONE',  ( -8.750000000000001776, 25.24999999999998934, 3.750000000000000000 ) ) ;
#61043=VECTOR ( 'NONE', #58661, 1000.000000000000000 ) ;
#61081=CARTESIAN_POINT ( 'NONE',  ( 9.000000000000003553, 25.24999999999998934, -3.750000000000000000 ) ) ;
#61087=ORIENTED_EDGE ( 'NONE', *, *, #63509, .F. ) ;
#61088=AXIS2_PLACEMENT_3D ( 'NONE', #15352, #47363, #9711 ) ;
#61090=CARTESIAN_POINT ( 'NONE',  ( -13.50000000000000355, 28.24999999999998934, 3.750000000000000000 ) ) ;
#61122=DIRECTION ( 'NONE',  ( 0.000000000000000000, 0.000000000000000000, -1.000000000000000000 ) ) ;
#61183=DIRECTION ( 'NONE',  ( -9.376883653928687363E-17, -1.000000000000000000, 0.000000000000000000 ) ) ;
#61190=CIRCLE ( 'NONE', #64566, 0.2500000000000002220 ) ;
#61192=CYLINDRICAL_SURFACE ( 'NONE', #59777, 0.2500000000000002220 ) ;
#61196=VERTEX_POINT ( 'NONE', #35000 ) ;
#61198=CIRCLE ( 'NONE', #23051, 0.2500000000000002220 ) ;
#61204=VERTEX_POINT ( 'NONE', #57861 ) ;
#61213=VERTEX_POINT ( 'NONE', #30384 ) ;
#61222=VECTOR ( 'NONE', #34722, 1000.000000000000000 ) ;
#61255=ORIENTED_EDGE ( 'NONE', *, *, #42698, .F. ) ;
#61261=AXIS2_PLACEMENT_3D ( 'NONE', #69055, #63062, #30007 ) ;
#61264=ORIENTED_EDGE ( 'NONE', *, *, #53078, .T. ) ;
#61283=ORIENTED_EDGE ( 'NONE', *, *, #29777, .T. ) ;
#61315=ORIENTED_EDGE ( 'NONE', *, *, #8958, .T. ) ;
#61323=ORIENTED_EDGE ( 'NONE', *, *, #19040, .T. ) ;
#61327=EDGE_LOOP ( 'NONE', ( #30722, #1262, #67427, #23101 ) ) ;
#61340=CARTESIAN_POINT ( 'NONE',  ( -22.25000000000000711, 34.24999999999999289, 3.750000000000000000 ) ) ;
#61359=DIRECTION ( 'NONE',  ( 0.000000000000000000, 0.000000000000000000, -1.000000000000000000 ) ) ;
#61376=EDGE_CURVE ( 'NONE', #35195, #65417, #65497, .T. ) ;
#61383=DIRECTION ( 'NONE',  ( 0.000000000000000000, 0.000000000000000000, -1.000000000000000000 ) ) ;
#61392=ORIENTED_EDGE ( 'NONE', *, *, #24233, .T. ) ;
#61397=ORIENTED_EDGE ( 'NONE', *, *, #35205, .T. ) ;
#61416=ORIENTED_EDGE ( 'NONE', *, *, #23054, .T. ) ;
#61417=EDGE_CURVE ( 'NONE', #55021, #28845, #54285, .T. ) ;
#61418=DIRECTION ( 'NONE',  ( -1.000000000000000000, 0.000000000000000000, 0.000000000000000000 ) ) ;
#61444=CARTESIAN_POINT ( 'NONE',  ( 4.750000000000002665, 22.24999999999998579, -4.000000000000000000 ) ) ;
#61476=ADVANCED_FACE ( 'NONE', ( #38521 ), #43783, .T. ) ;
#61481=DIRECTION ( 'NONE',  ( -1.000000000000000000, 0.000000000000000000, 0.000000000000000000 ) ) ;
#61484=EDGE_LOOP ( 'NONE', ( #39112, #10861, #56635 ) ) ;
#61491=CIRCLE ( 'NONE', #34542, 1.000000000000000000 ) ;
#61518=EDGE_CURVE ( 'NONE', #52256, #29481, #23570, .T. ) ;
#61521=CARTESIAN_POINT ( 'NONE',  ( -10.50000000000000178, 8.000000000000000000, 4.000000000000000000 ) ) ;
#61524=DIRECTION ( 'NONE',  ( -9.376883653928687363E-17, 1.000000000000000000, -0.000000000000000000 ) ) ;
#61530=CARTESIAN_POINT ( 'NONE',  ( 22.75000000000000711, 36.75000000000000000, -3.750000000000000000 ) ) ;
#61548=CARTESIAN_POINT ( 'NONE',  ( 18.25000000000000711, 33.99999999999999289, 3.750000000000000000 ) ) ;
#61560=CARTESIAN_POINT ( 'NONE',  ( 25.00000000000000355, 36.75000000000000000, -3.000000000000000000 ) ) ;
#61564=VERTEX_POINT ( 'NONE', #36618 ) ;
#61565=ADVANCED_FACE ( 'NONE', ( #21070 ), #24957, .F. ) ;
#61569=DIRECTION ( 'NONE',  ( -0.000000000000000000, 1.000000000000000000, -0.000000000000000000 ) ) ;
#61573=DIRECTION ( 'NONE',  ( 0.000000000000000000, 0.000000000000000000, -1.000000000000000000 ) ) ;
#61577=CIRCLE ( 'NONE', #31246, 4.000000000000000000 ) ;
#61600=EDGE_CURVE ( 'NONE', #65395, #40140, #42570, .T. ) ;
#61632=CARTESIAN_POINT ( 'NONE',  ( -13.75000000000000355, 28.24999999999998934, -3.750000000000000000 ) ) ;
#61687=EDGE_CURVE ( 'NONE', #30380, #48589, #47637, .T. ) ;
#61708=CARTESIAN_POINT ( 'NONE',  ( -18.00000000000000711, 30.99999999999999289, 4.000000000000000000 ) ) ;
#61721=VERTEX_POINT ( 'NONE', #59737 ) ;
#61734=CARTESIAN_POINT ( 'NONE',  ( -4.500000000000002665, 22.24999999999998579, 3.750000000000000000 ) ) ;
#61735=DIRECTION ( 'NONE',  ( 0.000000000000000000, -1.000000000000000000, 0.000000000000000000 ) ) ;
#61736=DIRECTION ( 'NONE',  ( 0.000000000000000000, -1.000000000000000000, 0.000000000000000000 ) ) ;
#61747=DIRECTION ( 'NONE',  ( -1.000000000000000000, 0.000000000000000000, 0.000000000000000000 ) ) ;
#61748=CARTESIAN_POINT ( 'NONE',  ( 22.25000000000000711, 34.24999999999999289, -4.000000000000000000 ) ) ;
#61749=CARTESIAN_POINT ( 'NONE',  ( 19.00000000000000000, 8.000000000000000000, -3.500000000000017764 ) ) ;
#61764=CARTESIAN_POINT ( 'NONE',  ( 13.50000000000000533, 30.99999999999999289, 3.750000000000000000 ) ) ;
#61772=AXIS2_PLACEMENT_3D ( 'NONE', #9232, #30654, #36341 ) ;
#61775=VECTOR ( 'NONE', #48876, 999.9999999999998863 ) ;
#61797=EDGE_LOOP ( 'NONE', ( #15095, #21679, #41618, #54343 ) ) ;
#61828=AXIS2_PLACEMENT_3D ( 'NONE', #56001, #34899, #67609 ) ;
#61833=CARTESIAN_POINT ( 'NONE',  ( 24.00000000000000355, 36.75000000000000000, -3.000000000000000000 ) ) ;
#61840=EDGE_CURVE ( 'NONE', #55377, #5413, #7151, .T. ) ;
#61868=EDGE_CURVE ( 'NONE', #67644, #26708, #19543, .T. ) ;
#61872=LINE ( 'NONE', #13698, #15811 ) ;
#61918=CIRCLE ( 'NONE', #29366, 0.5000000000000004441 ) ;
#61919=CARTESIAN_POINT ( 'NONE',  ( 22.75000000000000711, 0.000000000000000000, 4.000000000000000000 ) ) ;
#61939=ORIENTED_EDGE ( 'NONE', *, *, #23515, .T. ) ;
#61955=AXIS2_PLACEMENT_3D ( 'NONE', #66897, #28876, #61573 ) ;
#61964=EDGE_CURVE ( 'NONE', #68501, #17294, #4943, .T. ) ;
#61974=AXIS2_PLACEMENT_3D ( 'NONE', #43167, #17777, #17100 ) ;
#61985=ORIENTED_EDGE ( 'NONE', *, *, #25548, .T. ) ;
#61992=CARTESIAN_POINT ( 'NONE',  ( -9.000000000000003553, 27.74999999999998934, -3.750000000000000000 ) ) ;
#62009=ORIENTED_EDGE ( 'NONE', *, *, #33077, .T. ) ;
#62014=EDGE_CURVE ( 'NONE', #41120, #24031, #60680, .T. ) ;
#62017=CARTESIAN_POINT ( 'NONE',  ( -4.750000000000002665, 24.99999999999998579, 4.000000000000000000 ) ) ;
#62033=VECTOR ( 'NONE', #17973, 1000.000000000000000 ) ;
#62077=EDGE_CURVE ( 'NONE', #20746, #5753, #2228, .T. ) ;
#62080=ORIENTED_EDGE ( 'NONE', *, *, #63133, .T. ) ;
#62096=ORIENTED_EDGE ( 'NONE', *, *, #9517, .F. ) ;
#62099=CARTESIAN_POINT ( 'NONE',  ( 19.00000000000000000, 8.000000000000000000, 3.500000000000003997 ) ) ;
#62106=CARTESIAN_POINT ( 'NONE',  ( -24.00000000000000000, 1.000000000000000000, -3.000000000000000000 ) ) ;
#62107=ADVANCED_FACE ( 'NONE', ( #29367 ), #2602, .T. ) ;
#62149=ORIENTED_EDGE ( 'NONE', *, *, #58444, .T. ) ;
#62153=EDGE_LOOP ( 'NONE', ( #28977, #12939, #54787, #54720 ) ) ;
#62200=FACE_OUTER_BOUND ( 'NONE', #23361, .T. ) ;
#62274=VECTOR ( 'NONE', #66545, 1000.000000000000000 ) ;
#62280=ORIENTED_EDGE ( 'NONE', *, *, #64751, .F. ) ;
#62305=CARTESIAN_POINT ( 'NONE',  ( -18.25000000000000711, 31.24999999999999289, -4.000000000000000000 ) ) ;
#62328=DIRECTION ( 'NONE',  ( 0.000000000000000000, 0.000000000000000000, -1.000000000000000000 ) ) ;
#62330=TOROIDAL_SURFACE ( 'NONE', #48925, 0.5000000000000000000, 0.2500000000000000000 ) ;
#62332=DIRECTION ( 'NONE',  ( 0.000000000000000000, 0.000000000000000000, -1.000000000000000000 ) ) ;
#62341=EDGE_CURVE ( 'NONE', #54390, #43795, #69079, .T. ) ;
#62401=ORIENTED_EDGE ( 'NONE', *, *, #26199, .F. ) ;
#62410=DIRECTION ( 'NONE',  ( -0.000000000000000000, -0.000000000000000000, -1.000000000000000000 ) ) ;
#62453=ORIENTED_EDGE ( 'NONE', *, *, #59014, .T. ) ;
#62488=CARTESIAN_POINT ( 'NONE',  ( 22.75000000000000711, 37.00000000000000000, -3.750000000000000000 ) ) ;
#62541=SPHERICAL_SURFACE ( 'NONE', #6463, 0.2500000000000000000 ) ;
#62595=CARTESIAN_POINT ( 'NONE',  ( 18.25000000000000711, 31.24999999999999289, 3.750000000000000000 ) ) ;
#62597=DIRECTION ( 'NONE',  ( 0.000000000000000000, 1.000000000000000000, 0.000000000000000000 ) ) ;
#62625=CARTESIAN_POINT ( 'NONE',  ( -17.75000000000000711, 30.99999999999999289, -3.750000000000000000 ) ) ;
#62648=VECTOR ( 'NONE', #62799, 1000.000000000000000 ) ;
#62657=CARTESIAN_POINT ( 'NONE',  ( 4.250000000000001776, 22.24999999999998579, 3.750000000000000000 ) ) ;
#62665=EDGE_LOOP ( 'NONE', ( #65632, #44729, #50440, #32248 ) ) ;
#62696=ORIENTED_EDGE ( 'NONE', *, *, #54325, .F. ) ;
#62700=DIRECTION ( 'NONE',  ( -1.000000000000000000, 0.000000000000000000, 0.000000000000000000 ) ) ;
#62711=EDGE_CURVE ( 'NONE', #6425, #21392, #64267, .T. ) ;
#62714=CARTESIAN_POINT ( 'NONE',  ( -4.500000000000002665, 22.24999999999998579, -4.000000000000000000 ) ) ;
#62727=ORIENTED_EDGE ( 'NONE', *, *, #18189, .T. ) ;
#62731=( NAMED_UNIT ( * ) SI_UNIT ( $, .STERADIAN. ) SOLID_ANGLE_UNIT ( ) );
#62738=CARTESIAN_POINT ( 'NONE',  ( 15.00000000000000000, 8.000000000000000000, 3.500000000000003997 ) ) ;
#62773=DIRECTION ( 'NONE',  ( -1.000000000000000000, 0.000000000000000000, 0.000000000000000000 ) ) ;
#62782=CARTESIAN_POINT ( 'NONE',  ( 9.000000000000003553, 27.74999999999998934, 4.000000000000000000 ) ) ;
#62799=DIRECTION ( 'NONE',  ( 0.000000000000000000, -1.000000000000000000, -0.000000000000000000 ) ) ;
#62809=DIRECTION ( 'NONE',  ( 1.000000000000000000, 0.000000000000000000, 0.000000000000000000 ) ) ;
#62825=AXIS2_PLACEMENT_3D ( 'NONE', #41320, #30357, #51861 ) ;
#62831=LINE ( 'NONE', #13017, #59103 ) ;
#62845=VERTEX_POINT ( 'NONE', #28342 ) ;
#62922=AXIS2_PLACEMENT_3D ( 'NONE', #42231, #16509, #54090 ) ;
#62927=CARTESIAN_POINT ( 'NONE',  ( -4.750000000000002665, 24.74999999999998579, 4.000000000000000000 ) ) ;
#62932=ORIENTED_EDGE ( 'NONE', *, *, #57514, .T. ) ;
#62944=ORIENTED_EDGE ( 'NONE', *, *, #15448, .T. ) ;
#62970=EDGE_CURVE ( 'NONE', #33122, #2387, #26260, .T. ) ;
#62973=PLANE ( 'NONE',  #26899 ) ;
#62982=FACE_OUTER_BOUND ( 'NONE', #69242, .T. ) ;
#62983=EDGE_CURVE ( 'NONE', #42335, #63323, #40330, .T. ) ;
#62989=CARTESIAN_POINT ( 'NONE',  ( -17.75000000000000711, 30.74999999999999289, 4.000000000000000000 ) ) ;
#63000=AXIS2_PLACEMENT_3D ( 'NONE', #20987, #10785, #68846 ) ;
#63003=CARTESIAN_POINT ( 'NONE',  ( 22.75000000000000711, 34.24999999999999289, 3.750000000000000000 ) ) ;
#63013=ORIENTED_EDGE ( 'NONE', *, *, #26056, .F. ) ;
#63018=DIRECTION ( 'NONE',  ( 0.000000000000000000, 0.000000000000000000, -1.000000000000000000 ) ) ;
#63026=DIRECTION ( 'NONE',  ( 0.000000000000000000, 0.000000000000000000, -1.000000000000000000 ) ) ;
#63062=DIRECTION ( 'NONE',  ( 0.000000000000000000, -1.000000000000000000, 0.000000000000000000 ) ) ;
#63069=AXIS2_PLACEMENT_3D ( 'NONE', #60027, #58647, #54051 ) ;
#63080=LINE ( 'NONE', #13855, #6902 ) ;
#63103=ORIENTED_EDGE ( 'NONE', *, *, #49349, .T. ) ;
#63116=VECTOR ( 'NONE', #13303, 1000.000000000000000 ) ;
#63133=EDGE_CURVE ( 'NONE', #14152, #63323, #8358, .T. ) ;
#63141=ORIENTED_EDGE ( 'NONE', *, *, #64981, .F. ) ;
#63148=ORIENTED_EDGE ( 'NONE', *, *, #48401, .F. ) ;
#63152=EDGE_CURVE ( 'NONE', #37934, #43795, #11336, .T. ) ;
#63167=EDGE_CURVE ( 'NONE', #65737, #58659, #7788, .T. ) ;
#63189=DIRECTION ( 'NONE',  ( -0.000000000000000000, -1.000000000000000000, -0.000000000000000000 ) ) ;
#63203=ORIENTED_EDGE ( 'NONE', *, *, #26199, .T. ) ;
#63214=DIRECTION ( 'NONE',  ( 1.000000000000000000, 0.000000000000000000, 0.000000000000000000 ) ) ;
#63222=CIRCLE ( 'NONE', #55324, 4.499999999999997335 ) ;
#63288=VERTEX_POINT ( 'NONE', #62305 ) ;
#63323=VERTEX_POINT ( 'NONE', #63345 ) ;
#63328=ORIENTED_EDGE ( 'NONE', *, *, #19846, .F. ) ;
#63335=ORIENTED_EDGE ( 'NONE', *, *, #25038, .T. ) ;
#63337=CARTESIAN_POINT ( 'NONE',  ( 24.00000000000000000, 1.000000000000000000, 4.000000000000000000 ) ) ;
#63345=CARTESIAN_POINT ( 'NONE',  ( 22.25000000000000711, 33.99999999999999289, -3.750000000000000000 ) ) ;
#63348=CARTESIAN_POINT ( 'NONE',  ( 4.750000000000002665, 24.74999999999998579, 3.750000000000000000 ) ) ;
#63405=DIRECTION ( 'NONE',  ( -1.000000000000000000, 0.000000000000000000, 0.000000000000000000 ) ) ;
#63417=AXIS2_PLACEMENT_3D ( 'NONE', #35509, #58334, #58015 ) ;
#63424=CIRCLE ( 'NONE', #2706, 0.2500000000000002220 ) ;
#63455=DIRECTION ( 'NONE',  ( 0.000000000000000000, 1.000000000000000000, 0.000000000000000000 ) ) ;
#63457=VERTEX_POINT ( 'NONE', #62989 ) ;
#63509=EDGE_CURVE ( 'NONE', #13443, #12003, #52262, .T. ) ;
#63538=EDGE_CURVE ( 'NONE', #47699, #55021, #11754, .T. ) ;
#63547=ORIENTED_EDGE ( 'NONE', *, *, #64532, .F. ) ;
#63583=DIRECTION ( 'NONE',  ( -0.000000000000000000, -0.000000000000000000, 1.000000000000000000 ) ) ;
#63589=CARTESIAN_POINT ( 'NONE',  ( -13.25000000000000355, 27.74999999999998934, 3.750000000000000000 ) ) ;
#63599=CARTESIAN_POINT ( 'NONE',  ( 18.25000000000000711, 33.74999999999999289, -3.750000000000000000 ) ) ;
#63626=CARTESIAN_POINT ( 'NONE',  ( 4.500000000000002665, 22.24999999999998579, -3.750000000000000000 ) ) ;
#63635=CARTESIAN_POINT ( 'NONE',  ( -4.250000000000001776, 22.24999999999998579, -3.750000000000000000 ) ) ;
#63637=CARTESIAN_POINT ( 'NONE',  ( 8.750000000000001776, 24.74999999999998579, 4.000000000000000000 ) ) ;
#63655=CARTESIAN_POINT ( 'NONE',  ( 9.000000000000003553, 25.24999999999998934, 3.750000000000000000 ) ) ;
#63664=ORIENTED_EDGE ( 'NONE', *, *, #4694, .F. ) ;
#63673=CARTESIAN_POINT ( 'NONE',  ( 25.00000000000000355, 37.00000000000000000, 4.000000000000000000 ) ) ;
#63690=CARTESIAN_POINT ( 'NONE',  ( 9.000000000000003553, 27.99999999999998934, 3.750000000000000000 ) ) ;
#63702=ORIENTED_EDGE ( 'NONE', *, *, #47719, .T. ) ;
#63710=FACE_OUTER_BOUND ( 'NONE', #7740, .T. ) ;
#63747=EDGE_LOOP ( 'NONE', ( #57443, #65735, #25498, #13292 ) ) ;
#63785=VECTOR ( 'NONE', #36085, 1000.000000000000000 ) ;
#63786=EDGE_CURVE ( 'NONE', #17866, #15233, #6137, .T. ) ;
#63798=ORIENTED_EDGE ( 'NONE', *, *, #38969, .T. ) ;
#63810=AXIS2_PLACEMENT_3D ( 'NONE', #24039, #18427, #3579 ) ;
#63811=ORIENTED_EDGE ( 'NONE', *, *, #24437, .F. ) ;
#63820=ORIENTED_EDGE ( 'NONE', *, *, #26668, .T. ) ;
#63876=ORIENTED_EDGE ( 'NONE', *, *, #25404, .F. ) ;
#63892=CARTESIAN_POINT ( 'NONE',  ( -18.25000000000000711, 33.99999999999999289, 4.000000000000000000 ) ) ;
#63920=ORIENTED_EDGE ( 'NONE', *, *, #21882, .F. ) ;
#63922=ORIENTED_EDGE ( 'NONE', *, *, #10096, .F. ) ;
#63952=AXIS2_PLACEMENT_3D ( 'NONE', #6434, #32836, #10693 ) ;
#63955=AXIS2_PLACEMENT_3D ( 'NONE', #43101, #32842, #16355 ) ;
#63999=EDGE_CURVE ( 'NONE', #42883, #529, #10708, .T. ) ;
#64000=ORIENTED_EDGE ( 'NONE', *, *, #16153, .T. ) ;
#64018=CARTESIAN_POINT ( 'NONE',  ( -22.25000000000000711, 34.24999999999999289, 4.000000000000000000 ) ) ;
#64028=CARTESIAN_POINT ( 'NONE',  ( 13.75000000000000533, 30.74999999999999289, -3.750000000000000000 ) ) ;
#64048=CARTESIAN_POINT ( 'NONE',  ( 25.00000000000000355, 37.00000000000000000, 3.750000000000000000 ) ) ;
#64056=CARTESIAN_POINT ( 'NONE',  ( 10.50000000000000178, 8.000000000000000000, 4.000000000000000000 ) ) ;
#64058=DIRECTION ( 'NONE',  ( -0.000000000000000000, -0.000000000000000000, 1.000000000000000000 ) ) ;
#64061=ORIENTED_EDGE ( 'NONE', *, *, #60170, .T. ) ;
#64064=CARTESIAN_POINT ( 'NONE',  ( -9.000000000000003553, 25.24999999999998934, -4.000000000000000000 ) ) ;
#64093=ORIENTED_EDGE ( 'NONE', *, *, #12568, .T. ) ;
#64135=CARTESIAN_POINT ( 'NONE',  ( -25.00000000000000000, 1.000000000000000000, -3.000000000000000000 ) ) ;
#64148=EDGE_CURVE ( 'NONE', #23924, #62845, #593, .T. ) ;
#64152=CARTESIAN_POINT ( 'NONE',  ( -13.74999999999998757, -7.950815931560351124E-15, 4.000000000000000000 ) ) ;
#64175=CARTESIAN_POINT ( 'NONE',  ( 13.25000000000000355, 28.24999999999998934, -3.750000000000000000 ) ) ;
#64176=CARTESIAN_POINT ( 'NONE',  ( -13.50000000000000533, 30.74999999999999289, 4.000000000000000000 ) ) ;
#64199=CYLINDRICAL_SURFACE ( 'NONE', #58354, 0.2500000000000002220 ) ;
#64226=ORIENTED_EDGE ( 'NONE', *, *, #41149, .T. ) ;
#64259=AXIS2_PLACEMENT_3D ( 'NONE', #33399, #21814, #65042 ) ;
#64267=LINE ( 'NONE', #16122, #19532 ) ;
#64274=VERTEX_POINT ( 'NONE', #58104 ) ;
#64360=CARTESIAN_POINT ( 'NONE',  ( -13.75000000000000533, 30.74999999999999289, 3.750000000000000000 ) ) ;
#64377=ORIENTED_EDGE ( 'NONE', *, *, #62711, .T. ) ;
#64382=CARTESIAN_POINT ( 'NONE',  ( -24.00000000000000355, 37.00000000000000000, -3.000000000000000000 ) ) ;
#64387=DIRECTION ( 'NONE',  ( -0.000000000000000000, -0.000000000000000000, 1.000000000000000000 ) ) ;
#64408=FACE_OUTER_BOUND ( 'NONE', #35646, .T. ) ;
#64410=VERTEX_POINT ( 'NONE', #46055 ) ;
#64423=AXIS2_PLACEMENT_3D ( 'NONE', #17293, #11279, #22535 ) ;
#64440=DIRECTION ( 'NONE',  ( 0.000000000000000000, 0.000000000000000000, -1.000000000000000000 ) ) ;
#64484=CARTESIAN_POINT ( 'NONE',  ( 22.50000000000000711, 34.24999999999999289, 3.750000000000000000 ) ) ;
#64523=DIRECTION ( 'NONE',  ( 0.000000000000000000, 0.000000000000000000, -1.000000000000000000 ) ) ;
#64525=DIRECTION ( 'NONE',  ( -0.000000000000000000, -0.000000000000000000, 1.000000000000000000 ) ) ;
#64532=EDGE_CURVE ( 'NONE', #36018, #16885, #11934, .T. ) ;
#64566=AXIS2_PLACEMENT_3D ( 'NONE', #55368, #7192, #45203 ) ;
#64570=AXIS2_PLACEMENT_3D ( 'NONE', #49377, #42757, #21593 ) ;
#64574=CARTESIAN_POINT ( 'NONE',  ( -8.750000000000001776, 24.74999999999998579, 4.000000000000000000 ) ) ;
#64603=ORIENTED_EDGE ( 'NONE', *, *, #20735, .T. ) ;
#64608=ORIENTED_EDGE ( 'NONE', *, *, #26518, .T. ) ;
#64624=ORIENTED_EDGE ( 'NONE', *, *, #65289, .F. ) ;
#64644=DIRECTION ( 'NONE',  ( 0.000000000000000000, 0.000000000000000000, -1.000000000000000000 ) ) ;
#64651=DIRECTION ( 'NONE',  ( 1.000000000000000000, 0.000000000000000000, 0.000000000000000000 ) ) ;
#64668=CYLINDRICAL_SURFACE ( 'NONE', #62922, 0.2500000000000002220 ) ;
#64692=ORIENTED_EDGE ( 'NONE', *, *, #45805, .T. ) ;
#64703=DIRECTION ( 'NONE',  ( -1.000000000000000000, 0.000000000000000000, 0.000000000000000000 ) ) ;
#64720=ORIENTED_EDGE ( 'NONE', *, *, #67595, .T. ) ;
#64751=EDGE_CURVE ( 'NONE', #40236, #7265, #67125, .T. ) ;
#64756=CYLINDRICAL_SURFACE ( 'NONE', #64423, 0.2500000000000002220 ) ;
#64790=CIRCLE ( 'NONE', #28865, 0.2500000000000002220 ) ;
#64820=DIRECTION ( 'NONE',  ( 0.000000000000000000, -0.000000000000000000, 1.000000000000000000 ) ) ;
#64856=DIRECTION ( 'NONE',  ( -1.000000000000000000, 0.000000000000000000, 0.000000000000000000 ) ) ;
#64859=EDGE_LOOP ( 'NONE', ( #8507, #52671, #5295, #41584 ) ) ;
#64868=AXIS2_PLACEMENT_3D ( 'NONE', #16486, #4127, #37951 ) ;
#64981=EDGE_CURVE ( 'NONE', #43795, #46607, #40685, .T. ) ;
#64984=EDGE_CURVE ( 'NONE', #27282, #43138, #29937, .T. ) ;
#64993=VERTEX_POINT ( 'NONE', #1912 ) ;
#64995=ORIENTED_EDGE ( 'NONE', *, *, #21273, .T. ) ;
#65002=VERTEX_POINT ( 'NONE', #62099 ) ;
#65036=AXIS2_PLACEMENT_3D ( 'NONE', #40439, #40109, #35142 ) ;
#65042=DIRECTION ( 'NONE',  ( -1.000000000000000000, 0.000000000000000000, 0.000000000000000000 ) ) ;
#65055=AXIS2_PLACEMENT_3D ( 'NONE', #45558, #50792, #60297 ) ;
#65068=CARTESIAN_POINT ( 'NONE',  ( 22.25000000000000711, 34.24999999999999289, 3.750000000000000000 ) ) ;
#65079=EDGE_LOOP ( 'NONE', ( #9192, #38691, #68799, #62696 ) ) ;
#65111=DIRECTION ( 'NONE',  ( 0.000000000000000000, 0.000000000000000000, -1.000000000000000000 ) ) ;
#65117=EDGE_CURVE ( 'NONE', #52614, #37693, #6378, .T. ) ;
#65128=CIRCLE ( 'NONE', #68563, 0.2500000000000002220 ) ;
#65139=VERTEX_POINT ( 'NONE', #9360 ) ;
#65159=DIRECTION ( 'NONE',  ( 1.000000000000000000, 0.000000000000000000, -0.000000000000000000 ) ) ;
#65209=CARTESIAN_POINT ( 'NONE',  ( 9.250000000000003553, 0.000000000000000000, 4.000000000000000000 ) ) ;
#65269=ORIENTED_EDGE ( 'NONE', *, *, #40366, .F. ) ;
#65276=CIRCLE ( 'NONE', #24740, 0.5000000000000004441 ) ;
#65282=ORIENTED_EDGE ( 'NONE', *, *, #43574, .T. ) ;
#65289=EDGE_CURVE ( 'NONE', #41931, #42883, #60305, .T. ) ;
#65301=ORIENTED_EDGE ( 'NONE', *, *, #51669, .T. ) ;
#65303=CARTESIAN_POINT ( 'NONE',  ( 11.00000000000000000, 8.000000000000000000, 4.000000000000000000 ) ) ;
#65309=CARTESIAN_POINT ( 'NONE',  ( 17.75000000000000711, 30.74999999999999289, -4.000000000000000000 ) ) ;
#65310=DIRECTION ( 'NONE',  ( 0.000000000000000000, -1.000000000000000000, 0.000000000000000000 ) ) ;
#65314=CIRCLE ( 'NONE', #42874, 0.2500000000000002220 ) ;
#65352=VECTOR ( 'NONE', #41442, 1000.000000000000000 ) ;
#65363=AXIS2_PLACEMENT_3D ( 'NONE', #68251, #34494, #16192 ) ;
#65395=VERTEX_POINT ( 'NONE', #13764 ) ;
#65396=FACE_OUTER_BOUND ( 'NONE', #52500, .T. ) ;
#65417=VERTEX_POINT ( 'NONE', #63337 ) ;
#65425=CIRCLE ( 'NONE', #4753, 0.2500000000000002220 ) ;
#65453=PLANE ( 'NONE',  #38404 ) ;
#65466=AXIS2_PLACEMENT_3D ( 'NONE', #37769, #10299, #5675 ) ;
#65478=VECTOR ( 'NONE', #31485, 1000.000000000000000 ) ;
#65481=EDGE_LOOP ( 'NONE', ( #29498, #2038, #12149, #10209 ) ) ;
#65497=CIRCLE ( 'NONE', #35168, 1.000000000000000000 ) ;
#65530=CARTESIAN_POINT ( 'NONE',  ( 22.25000000000000711, 33.74999999999999289, 4.000000000000000000 ) ) ;
#65533=DIRECTION ( 'NONE',  ( 0.000000000000000000, 1.000000000000000000, 0.000000000000000000 ) ) ;
#65544=VECTOR ( 'NONE', #46467, 1000.000000000000000 ) ;
#65563=EDGE_LOOP ( 'NONE', ( #62727, #60490, #50778, #48151 ) ) ;
#65573=DIRECTION ( 'NONE',  ( 0.000000000000000000, 0.000000000000000000, -1.000000000000000000 ) ) ;
#65574=FACE_OUTER_BOUND ( 'NONE', #53800, .T. ) ;
#65615=DIRECTION ( 'NONE',  ( 0.000000000000000000, 0.000000000000000000, -1.000000000000000000 ) ) ;
#65620=AXIS2_PLACEMENT_3D ( 'NONE', #53186, #30655, #52505 ) ;
#65625=ORIENTED_EDGE ( 'NONE', *, *, #5464, .F. ) ;
#65628=AXIS2_PLACEMENT_3D ( 'NONE', #49106, #7538, #44189 ) ;
#65632=ORIENTED_EDGE ( 'NONE', *, *, #57841, .T. ) ;
#65634=AXIS2_PLACEMENT_3D ( 'NONE', #65857, #5697, #38121 ) ;
#65650=CARTESIAN_POINT ( 'NONE',  ( 13.50000000000000533, 30.74999999999999289, 3.750000000000000000 ) ) ;
#65654=ORIENTED_EDGE ( 'NONE', *, *, #55426, .F. ) ;
#65664=ADVANCED_FACE ( 'NONE', ( #2357 ), #8411, .T. ) ;
#65694=ADVANCED_FACE ( 'NONE', ( #62200 ), #62541, .T. ) ;
#65695=DIRECTION ( 'NONE',  ( 1.000000000000000000, 0.000000000000000000, 0.000000000000000000 ) ) ;
#65708=CARTESIAN_POINT ( 'NONE',  ( -13.50000000000000355, 27.74999999999998934, -3.750000000000000000 ) ) ;
#65730=CARTESIAN_POINT ( 'NONE',  ( -22.75000000000000711, 34.24999999999999289, 3.750000000000000000 ) ) ;
#65734=LINE ( 'NONE', #34070, #37803 ) ;
#65735=ORIENTED_EDGE ( 'NONE', *, *, #34857, .F. ) ;
#65737=VERTEX_POINT ( 'NONE', #41470 ) ;
#65749=EDGE_CURVE ( 'NONE', #47479, #46287, #17702, .T. ) ;
#65750=CARTESIAN_POINT ( 'NONE',  ( -24.00000000000000000, 1.000000000000000000, -3.000000000000000000 ) ) ;
#65766=DIRECTION ( 'NONE',  ( -0.000000000000000000, -0.000000000000000000, -1.000000000000000000 ) ) ;
#65783=FACE_OUTER_BOUND ( 'NONE', #2540, .T. ) ;
#65800=LINE ( 'NONE', #39100, #51720 ) ;
#65819=EDGE_LOOP ( 'NONE', ( #44363, #1803, #19062, #55709 ) ) ;
#65827=DIRECTION ( 'NONE',  ( 0.000000000000000000, -1.000000000000000000, 0.000000000000000000 ) ) ;
#65833=CARTESIAN_POINT ( 'NONE',  ( 18.00000000000000711, 33.74999999999999289, -3.750000000000000000 ) ) ;
#65847=DIRECTION ( 'NONE',  ( 0.000000000000000000, 0.000000000000000000, -1.000000000000000000 ) ) ;
#65849=DIRECTION ( 'NONE',  ( -1.000000000000000000, 0.000000000000000000, 0.000000000000000000 ) ) ;
#65857=CARTESIAN_POINT ( 'NONE',  ( 22.25000000000000711, 34.24999999999999289, -3.750000000000000000 ) ) ;
#65862=AXIS2_PLACEMENT_3D ( 'NONE', #29460, #51277, #51982 ) ;
#65866=DIRECTION ( 'NONE',  ( 0.000000000000000000, 0.000000000000000000, 1.000000000000000000 ) ) ;
#65888=CIRCLE ( 'NONE', #5210, 4.000000000000000000 ) ;
#65904=EDGE_CURVE ( 'NONE', #63288, #30672, #14310, .T. ) ;
#65951=AXIS2_PLACEMENT_3D ( 'NONE', #14602, #24794, #65111 ) ;
#65979=CARTESIAN_POINT ( 'NONE',  ( 0.000000000000000000, 33.74999999999999289, 3.750000000000000000 ) ) ;
#65997=DIRECTION ( 'NONE',  ( 1.000000000000000000, 0.000000000000000000, 0.000000000000000000 ) ) ;
#66004=DIRECTION ( 'NONE',  ( 1.000000000000000000, 0.000000000000000000, 0.000000000000000000 ) ) ;
#66024=AXIS2_PLACEMENT_3D ( 'NONE', #7965, #56494, #30098 ) ;
#66030=ADVANCED_FACE ( 'NONE', ( #2641 ), #67066, .T. ) ;
#66039=VERTEX_POINT ( 'NONE', #61749 ) ;
#66041=DIRECTION ( 'NONE',  ( 0.000000000000000000, 0.000000000000000000, -1.000000000000000000 ) ) ;
#66046=ORIENTED_EDGE ( 'NONE', *, *, #4109, .F. ) ;
#66052=CARTESIAN_POINT ( 'NONE',  ( 24.00000000000000000, -2.250452076942884869E-15, 4.000000000000000000 ) ) ;
#66074=DIRECTION ( 'NONE',  ( 0.000000000000000000, 0.000000000000000000, -1.000000000000000000 ) ) ;
#66082=ADVANCED_FACE ( 'NONE', ( #12892 ), #14282, .T. ) ;
#66093=DIRECTION ( 'NONE',  ( 1.000000000000000000, 0.000000000000000000, 0.000000000000000000 ) ) ;
#66101=DIRECTION ( 'NONE',  ( 0.000000000000000000, 0.000000000000000000, 1.000000000000000000 ) ) ;
#66108=DIRECTION ( 'NONE',  ( 1.000000000000000000, 0.000000000000000000, 0.000000000000000000 ) ) ;
#66117=ADVANCED_FACE ( 'NONE', ( #35748 ), #2264, .F. ) ;
#66126=CARTESIAN_POINT ( 'NONE',  ( -18.25000000000000711, 0.000000000000000000, 3.750000000000000000 ) ) ;
#66127=DIRECTION ( 'NONE',  ( 1.000000000000000000, -0.000000000000000000, -0.000000000000000000 ) ) ;
#66135=EDGE_CURVE ( 'NONE', #62845, #35085, #29410, .T. ) ;
#66138=DIRECTION ( 'NONE',  ( -1.000000000000000000, 0.000000000000000000, 0.000000000000000000 ) ) ;
#66174=ORIENTED_EDGE ( 'NONE', *, *, #35110, .T. ) ;
#66180=CIRCLE ( 'NONE', #32474, 0.7499999999999997780 ) ;
#66182=DIRECTION ( 'NONE',  ( -1.000000000000000000, 0.000000000000000000, 0.000000000000000000 ) ) ;
#66183=VECTOR ( 'NONE', #46958, 1000.000000000000000 ) ;
#66188=CARTESIAN_POINT ( 'NONE',  ( -13.75000000000000533, 30.99999999999999289, 3.750000000000000000 ) ) ;
#66191=FACE_OUTER_BOUND ( 'NONE', #16275, .T. ) ;
#66194=AXIS2_PLACEMENT_3D ( 'NONE', #10672, #31, #21566 ) ;
#66201=CARTESIAN_POINT ( 'NONE',  ( -9.250000000000003553, 0.000000000000000000, 4.000000000000000000 ) ) ;
#66217=EDGE_CURVE ( 'NONE', #16875, #63288, #53324, .T. ) ;
#66235=EDGE_CURVE ( 'NONE', #63288, #6972, #59271, .T. ) ;
#66238=CYLINDRICAL_SURFACE ( 'NONE', #32968, 0.2500000000000002220 ) ;
#66275=DIRECTION ( 'NONE',  ( -1.000000000000000000, 0.000000000000000000, 0.000000000000000000 ) ) ;
#66292=EDGE_CURVE ( 'NONE', #9509, #51977, #38005, .T. ) ;
#66298=CYLINDRICAL_SURFACE ( 'NONE', #12113, 0.2500000000000002220 ) ;
#66313=VECTOR ( 'NONE', #42829, 1000.000000000000000 ) ;
#66321=DIRECTION ( 'NONE',  ( 0.000000000000000000, -1.000000000000000000, 0.000000000000000000 ) ) ;
#66327=ORIENTED_EDGE ( 'NONE', *, *, #13481, .F. ) ;
#66335=EDGE_LOOP ( 'NONE', ( #23046, #45969, #46782 ) ) ;
#66360=EDGE_LOOP ( 'NONE', ( #49547, #61939, #68237 ) ) ;
#66388=EDGE_CURVE ( 'NONE', #2387, #1595, #28261, .T. ) ;
#66411=VERTEX_POINT ( 'NONE', #17086 ) ;
#66420=DIRECTION ( 'NONE',  ( -0.000000000000000000, 1.000000000000000000, -0.000000000000000000 ) ) ;
#66421=DIRECTION ( 'NONE',  ( 0.000000000000000000, 0.000000000000000000, -1.000000000000000000 ) ) ;
#66427=DIRECTION ( 'NONE',  ( 1.000000000000000000, 0.000000000000000000, -0.000000000000000000 ) ) ;
#66484=VECTOR ( 'NONE', #1768, 1000.000000000000114 ) ;
#66487=CARTESIAN_POINT ( 'NONE',  ( -19.00000000000000000, 8.000000000000000000, -3.500000000000017764 ) ) ;
#66545=DIRECTION ( 'NONE',  ( 1.000000000000000000, -0.000000000000000000, -0.000000000000000000 ) ) ;
#66585=CONICAL_SURFACE ( 'NONE', #45279, 4.000000000000000000, 0.7853981633974482790 ) ;
#66608=VERTEX_POINT ( 'NONE', #1852 ) ;
#66609=LINE ( 'NONE', #7174, #29476 ) ;
#66615=ORIENTED_EDGE ( 'NONE', *, *, #11081, .F. ) ;
#66639=FACE_OUTER_BOUND ( 'NONE', #47040, .T. ) ;
#66668=EDGE_LOOP ( 'NONE', ( #42366, #35392, #53744, #22566 ) ) ;
#66711=CARTESIAN_POINT ( 'NONE',  ( -4.250000000000001776, 22.24999999999998579, 4.000000000000000000 ) ) ;
#66718=AXIS2_PLACEMENT_3D ( 'NONE', #6430, #27858, #17378 ) ;
#66740=CARTESIAN_POINT ( 'NONE',  ( -22.75000000000000711, 36.75000000000000000, -3.750000000000000000 ) ) ;
#66773=DIRECTION ( 'NONE',  ( 0.000000000000000000, 0.000000000000000000, -1.000000000000000000 ) ) ;
#66797=AXIS2_PLACEMENT_3D ( 'NONE', #61340, #6479, #66275 ) ;
#66816=VECTOR ( 'NONE', #13720, 1000.000000000000000 ) ;
#66820=EDGE_CURVE ( 'NONE', #50411, #23842, #42629, .T. ) ;
#66849=CARTESIAN_POINT ( 'NONE',  ( 13.50000000000000355, 28.24999999999998934, 3.750000000000000000 ) ) ;
#66855=DIRECTION ( 'NONE',  ( 0.000000000000000000, 1.000000000000000000, 0.000000000000000000 ) ) ;
#66868=ORIENTED_EDGE ( 'NONE', *, *, #59363, .T. ) ;
#66869=LINE ( 'NONE', #29912, #59949 ) ;
#66879=FACE_OUTER_BOUND ( 'NONE', #39018, .T. ) ;
#66883=VERTEX_POINT ( 'NONE', #66188 ) ;
#66897=CARTESIAN_POINT ( 'NONE',  ( 24.00000000000000355, 36.75000000000000000, 3.000000000000000000 ) ) ;
#66922=AXIS2_PLACEMENT_3D ( 'NONE', #33449, #66138, #22551 ) ;
#66924=DIRECTION ( 'NONE',  ( -1.000000000000000000, 0.000000000000000000, 0.000000000000000000 ) ) ;
#66942=CYLINDRICAL_SURFACE ( 'NONE', #42222, 0.2500000000000002220 ) ;
#66962=ORIENTED_EDGE ( 'NONE', *, *, #41098, .F. ) ;
#66969=ORIENTED_EDGE ( 'NONE', *, *, #41088, .T. ) ;
#67001=( LENGTH_UNIT ( ) NAMED_UNIT ( * ) SI_UNIT ( .MILLI., .METRE. ) );
#67008=LINE ( 'NONE', #18799, #48492 ) ;
#67020=ORIENTED_EDGE ( 'NONE', *, *, #20697, .F. ) ;
#67029=DIRECTION ( 'NONE',  ( 1.000000000000000000, 0.000000000000000000, 0.000000000000000000 ) ) ;
#67031=DIRECTION ( 'NONE',  ( -1.000000000000000000, 0.000000000000000000, 0.000000000000000000 ) ) ;
#67036=DIRECTION ( 'NONE',  ( -1.000000000000000000, 0.000000000000000000, 0.000000000000000000 ) ) ;
#67038=ORIENTED_EDGE ( 'NONE', *, *, #36163, .T. ) ;
#67057=DIRECTION ( 'NONE',  ( 0.000000000000000000, -1.000000000000000000, 0.000000000000000000 ) ) ;
#67066=CYLINDRICAL_SURFACE ( 'NONE', #49223, 1.000000000000000888 ) ;
#67082=CARTESIAN_POINT ( 'NONE',  ( 17.75000000000000711, 30.74999999999999289, 4.000000000000000000 ) ) ;
#67083=CYLINDRICAL_SURFACE ( 'NONE', #10234, 1.000000000000000000 ) ;
#67085=DIRECTION ( 'NONE',  ( -0.000000000000000000, 1.000000000000000000, -0.000000000000000000 ) ) ;
#67091=ORIENTED_EDGE ( 'NONE', *, *, #50364, .F. ) ;
#67103=ORIENTED_EDGE ( 'NONE', *, *, #22979, .F. ) ;
#67118=CYLINDRICAL_SURFACE ( 'NONE', #6561, 0.2500000000000002220 ) ;
#67125=LINE ( 'NONE', #25251, #28756 ) ;
#67128=VERTEX_POINT ( 'NONE', #61090 ) ;
#67171=EDGE_CURVE ( 'NONE', #41931, #529, #816, .T. ) ;
#67195=ORIENTED_EDGE ( 'NONE', *, *, #42075, .T. ) ;
#67216=ORIENTED_EDGE ( 'NONE', *, *, #8587, .F. ) ;
#67228=EDGE_LOOP ( 'NONE', ( #45864, #19447, #64624, #43313 ) ) ;
#67230=VECTOR ( 'NONE', #20471, 1000.000000000000000 ) ;
#67264=ORIENTED_EDGE ( 'NONE', *, *, #49196, .T. ) ;
#67281=EDGE_CURVE ( 'NONE', #67128, #55864, #40208, .T. ) ;
#67292=FACE_OUTER_BOUND ( 'NONE', #4585, .T. ) ;
#67335=( NAMED_UNIT ( * ) PLANE_ANGLE_UNIT ( ) SI_UNIT ( $, .RADIAN. ) );
#67339=FACE_OUTER_BOUND ( 'NONE', #3939, .T. ) ;
#67340=DIRECTION ( 'NONE',  ( -0.000000000000000000, -0.000000000000000000, 1.000000000000000000 ) ) ;
#67341=EDGE_LOOP ( 'NONE', ( #4545, #23394, #51760, #8967 ) ) ;
#67355=ORIENTED_EDGE ( 'NONE', *, *, #66235, .T. ) ;
#67359=ORIENTED_EDGE ( 'NONE', *, *, #50456, .T. ) ;
#67362=PLANE ( 'NONE',  #54157 ) ;
#67367=CARTESIAN_POINT ( 'NONE',  ( -9.000000000000003553, 24.99999999999998579, 3.750000000000000000 ) ) ;
#67370=VECTOR ( 'NONE', #52615, 1000.000000000000000 ) ;
#67374=ORIENTED_EDGE ( 'NONE', *, *, #18970, .F. ) ;
#67375=DIRECTION ( 'NONE',  ( 1.000000000000000000, 0.000000000000000000, 0.000000000000000000 ) ) ;
#67387=DIRECTION ( 'NONE',  ( 0.000000000000000000, 0.000000000000000000, -1.000000000000000000 ) ) ;
#67396=ORIENTED_EDGE ( 'NONE', *, *, #63133, .F. ) ;
#67406=VERTEX_POINT ( 'NONE', #42462 ) ;
#67411=FACE_OUTER_BOUND ( 'NONE', #23496, .T. ) ;
#67417=TOROIDAL_SURFACE ( 'NONE', #16889, 0.5000000000000000000, 0.2500000000000000000 ) ;
#67427=ORIENTED_EDGE ( 'NONE', *, *, #32409, .F. ) ;
#67518=VECTOR ( 'NONE', #52067, 1000.000000000000000 ) ;
#67541=CARTESIAN_POINT ( 'NONE',  ( -9.000000000000003553, 27.74999999999998934, 4.000000000000000000 ) ) ;
#67543=FACE_OUTER_BOUND ( 'NONE', #27187, .T. ) ;
#67566=EDGE_LOOP ( 'NONE', ( #30967, #6088, #36654, #42417, #26272, #67264, #1729, #60492, #53651, #25192, #40248, #37770, #48982, #42325, #18742, #7666, #57412, #67608, #18664, #21812, #27812, #21694, #67622, #49003, #43488, #64061, #68264, #7366, #24904, #69603, #28761, #38187, #36739, #48912 ) ) ;
#67569=CIRCLE ( 'NONE', #10335, 4.499999999999976019 ) ;
#67595=EDGE_CURVE ( 'NONE', #61721, #454, #43648, .T. ) ;
#67599=LINE ( 'NONE', #14140, #69616 ) ;
#67608=ORIENTED_EDGE ( 'NONE', *, *, #35017, .T. ) ;
#67609=DIRECTION ( 'NONE',  ( 0.000000000000000000, 0.000000000000000000, -1.000000000000000000 ) ) ;
#67617=CIRCLE ( 'NONE', #46315, 0.2500000000000002220 ) ;
#67622=ORIENTED_EDGE ( 'NONE', *, *, #55415, .T. ) ;
#67644=VERTEX_POINT ( 'NONE', #37462 ) ;
#67674=EDGE_CURVE ( 'NONE', #30672, #27999, #48111, .T. ) ;
#67706=DIRECTION ( 'NONE',  ( 1.000000000000000000, -0.000000000000000000, -0.000000000000000000 ) ) ;
#67713=AXIS2_PLACEMENT_3D ( 'NONE', #65750, #38376, #39056 ) ;
#67739=AXIS2_PLACEMENT_3D ( 'NONE', #4757, #9369, #9014 ) ;
#67740=CARTESIAN_POINT ( 'NONE',  ( -13.25000000000000355, 27.99999999999998934, 3.750000000000000000 ) ) ;
#67744=CARTESIAN_POINT ( 'NONE',  ( 18.25000000000000711, 0.000000000000000000, 4.000000000000000000 ) ) ;
#67753=CARTESIAN_POINT ( 'NONE',  ( -22.50000000000000711, 36.75000000000000000, -3.750000000000000000 ) ) ;
#67777=AXIS2_PLACEMENT_3D ( 'NONE', #29578, #19721, #46141 ) ;
#67815=CARTESIAN_POINT ( 'NONE',  ( 9.250000000000003553, 27.74999999999998934, -3.750000000000000000 ) ) ;
#67838=DIRECTION ( 'NONE',  ( 0.000000000000000000, -1.000000000000000000, 0.000000000000000000 ) ) ;
#67860=FACE_OUTER_BOUND ( 'NONE', #55807, .T. ) ;
#67889=ADVANCED_FACE ( 'NONE', ( #23297 ), #50383, .T. ) ;
#67901=CARTESIAN_POINT ( 'NONE',  ( -13.75000000000000533, 30.74999999999999289, -3.750000000000000000 ) ) ;
#67908=AXIS2_PLACEMENT_3D ( 'NONE', #21442, #27396, #15855 ) ;
#67939=DIRECTION ( 'NONE',  ( 1.000000000000000000, -0.000000000000000000, 0.000000000000000000 ) ) ;
#67988=EDGE_LOOP ( 'NONE', ( #56220, #36345, #27214, #54804 ) ) ;
#67991=ORIENTED_EDGE ( 'NONE', *, *, #14205, .T. ) ;
#67997=ADVANCED_FACE ( 'NONE', ( #69651 ), #53809, .F. ) ;
#68009=DIRECTION ( 'NONE',  ( 0.000000000000000000, 0.000000000000000000, 1.000000000000000000 ) ) ;
#68037=CARTESIAN_POINT ( 'NONE',  ( -24.00000000000000355, 37.00000000000000000, 3.750000000000000000 ) ) ;
#68060=DIRECTION ( 'NONE',  ( -1.000000000000000000, 0.000000000000000000, 0.000000000000000000 ) ) ;
#68061=AXIS2_PLACEMENT_3D ( 'NONE', #46703, #52970, #19896 ) ;
#68063=DIRECTION ( 'NONE',  ( 1.000000000000000000, -0.000000000000000000, -0.000000000000000000 ) ) ;
#68084=ADVANCED_FACE ( 'NONE', ( #45390 ), #31282, .F. ) ;
#68104=LINE ( 'NONE', #42105, #16245 ) ;
#68140=EDGE_CURVE ( 'NONE', #64410, #63457, #54874, .T. ) ;
#68153=AXIS2_PLACEMENT_3D ( 'NONE', #4377, #47367, #16042 ) ;
#68202=DIRECTION ( 'NONE',  ( 0.000000000000000000, 1.000000000000000000, -0.000000000000000000 ) ) ;
#68230=ORIENTED_EDGE ( 'NONE', *, *, #26904, .F. ) ;
#68237=ORIENTED_EDGE ( 'NONE', *, *, #9414, .F. ) ;
#68251=CARTESIAN_POINT ( 'NONE',  ( -8.750000000000001776, 24.74999999999998579, 3.750000000000000000 ) ) ;
#68253=DIRECTION ( 'NONE',  ( 0.000000000000000000, 0.000000000000000000, -1.000000000000000000 ) ) ;
#68259=CARTESIAN_POINT ( 'NONE',  ( 17.75000000000000711, 30.99999999999999289, 3.750000000000000000 ) ) ;
#68264=ORIENTED_EDGE ( 'NONE', *, *, #27893, .T. ) ;
#68267=DIRECTION ( 'NONE',  ( -1.000000000000000000, 0.000000000000000000, 0.000000000000000000 ) ) ;
#68287=EDGE_CURVE ( 'NONE', #5366, #55052, #41466, .T. ) ;
#68303=CIRCLE ( 'NONE', #30065, 0.2500000000000002220 ) ;
#68305=EDGE_CURVE ( 'NONE', #20640, #17311, #32273, .T. ) ;
#68313=EDGE_LOOP ( 'NONE', ( #46468, #1902, #4915, #17582 ) ) ;
#68318=AXIS2_PLACEMENT_3D ( 'NONE', #2108, #44797, #45140 ) ;
#68325=DIRECTION ( 'NONE',  ( 5.782411586589351722E-16, 1.000000000000000000, -0.000000000000000000 ) ) ;
#68367=DIRECTION ( 'NONE',  ( 0.000000000000000000, 0.000000000000000000, -1.000000000000000000 ) ) ;
#68380=SURFACE_STYLE_FILL_AREA ( #3617 ) ;
#68384=ADVANCED_FACE ( 'NONE', ( #48852 ), #26798, .T. ) ;
#68401=VERTEX_POINT ( 'NONE', #18537 ) ;
#68426=ORIENTED_EDGE ( 'NONE', *, *, #58339, .T. ) ;
#68429=DIRECTION ( 'NONE',  ( 1.000000000000000000, 9.376883653928687363E-17, -0.000000000000000000 ) ) ;
#68441=CIRCLE ( 'NONE', #65055, 0.2500000000000002220 ) ;
#68483=DIRECTION ( 'NONE',  ( -0.000000000000000000, -0.000000000000000000, -1.000000000000000000 ) ) ;
#68484=VERTEX_POINT ( 'NONE', #12540 ) ;
#68486=ORIENTED_EDGE ( 'NONE', *, *, #45328, .T. ) ;
#68490=CIRCLE ( 'NONE', #41552, 0.2500000000000002220 ) ;
#68496=ORIENTED_EDGE ( 'NONE', *, *, #24435, .T. ) ;
#68498=FACE_OUTER_BOUND ( 'NONE', #29666, .T. ) ;
#68501=VERTEX_POINT ( 'NONE', #60721 ) ;
#68529=VERTEX_POINT ( 'NONE', #22414 ) ;
#68545=CARTESIAN_POINT ( 'NONE',  ( 4.750000000000002665, 24.74999999999998579, -4.000000000000000000 ) ) ;
#68546=VECTOR ( 'NONE', #66924, 1000.000000000000000 ) ;
#68563=AXIS2_PLACEMENT_3D ( 'NONE', #49973, #39779, #39430 ) ;
#68570=FACE_OUTER_BOUND ( 'NONE', #41216, .T. ) ;
#68575=CIRCLE ( 'NONE', #13517, 1.000000000000000000 ) ;
#68591=LINE ( 'NONE', #67541, #2811 ) ;
#68617=AXIS2_PLACEMENT_3D ( 'NONE', #52049, #19309, #3806 ) ;
#68642=ADVANCED_FACE ( 'NONE', ( #58584 ), #64199, .T. ) ;
#68655=VECTOR ( 'NONE', #56348, 1000.000000000000000 ) ;
#68673=CARTESIAN_POINT ( 'NONE',  ( -22.50000000000000711, 34.24999999999999289, -4.000000000000000000 ) ) ;
#68680=EDGE_LOOP ( 'NONE', ( #14439, #21645, #42928, #61283 ) ) ;
#68726=FACE_OUTER_BOUND ( 'NONE', #10869, .T. ) ;
#68741=ADVANCED_FACE ( 'NONE', ( #26218 ), #47386, .T. ) ;
#68744=AXIS2_PLACEMENT_3D ( 'NONE', #21002, #5153, #22738 ) ;
#68750=ORIENTED_EDGE ( 'NONE', *, *, #24897, .F. ) ;
#68768=ORIENTED_EDGE ( 'NONE', *, *, #41149, .F. ) ;
#68799=ORIENTED_EDGE ( 'NONE', *, *, #18459, .F. ) ;
#68800=DIRECTION ( 'NONE',  ( 1.000000000000000000, -0.000000000000000000, -0.000000000000000000 ) ) ;
#68846=DIRECTION ( 'NONE',  ( 0.000000000000000000, 0.000000000000000000, -1.000000000000000000 ) ) ;
#68847=DIRECTION ( 'NONE',  ( 0.000000000000000000, 1.000000000000000000, 0.000000000000000000 ) ) ;
#68849=ORIENTED_EDGE ( 'NONE', *, *, #59014, .F. ) ;
#68851=DIRECTION ( 'NONE',  ( -1.000000000000000000, 0.000000000000000000, 0.000000000000000000 ) ) ;
#68982=EDGE_LOOP ( 'NONE', ( #35481, #55529, #33353, #34504 ) ) ;
#68987=ORIENTED_EDGE ( 'NONE', *, *, #41171, .F. ) ;
#69008=ORIENTED_EDGE ( 'NONE', *, *, #4516, .F. ) ;
#69019=ORIENTED_EDGE ( 'NONE', *, *, #64984, .F. ) ;
#69022=ORIENTED_EDGE ( 'NONE', *, *, #32409, .T. ) ;
#69037=EDGE_CURVE ( 'NONE', #20640, #42065, #59446, .T. ) ;
#69055=CARTESIAN_POINT ( 'NONE',  ( -9.000000000000003553, 24.99999999999998579, 4.000000000000000000 ) ) ;
#69068=AXIS2_PLACEMENT_3D ( 'NONE', #17091, #38905, #39589 ) ;
#69079=CIRCLE ( 'NONE', #7253, 0.2500000000000002220 ) ;
#69081=SPHERICAL_SURFACE ( 'NONE', #62825, 0.2500000000000000000 ) ;
#69090=DIRECTION ( 'NONE',  ( -0.000000000000000000, -0.000000000000000000, 1.000000000000000000 ) ) ;
#69100=CARTESIAN_POINT ( 'NONE',  ( 9.250000000000003553, 27.74999999999998934, -3.750000000000000000 ) ) ;
#69131=DIRECTION ( 'NONE',  ( -0.000000000000000000, -0.000000000000000000, 1.000000000000000000 ) ) ;
#69136=ORIENTED_EDGE ( 'NONE', *, *, #58370, .F. ) ;
#69170=CIRCLE ( 'NONE', #24260, 0.5000000000000004441 ) ;
#69193=EDGE_LOOP ( 'NONE', ( #6357, #3537, #63922 ) ) ;
#69216=STYLED_ITEM ( 'NONE', ( #16703 ), #49805 ) ;
#69224=DIRECTION ( 'NONE',  ( 0.000000000000000000, 0.000000000000000000, -1.000000000000000000 ) ) ;
#69226=CARTESIAN_POINT ( 'NONE',  ( 24.00000000000000000, 0.000000000000000000, 4.000000000000000000 ) ) ;
#69228=ORIENTED_EDGE ( 'NONE', *, *, #24142, .F. ) ;
#69241=AXIS2_PLACEMENT_3D ( 'NONE', #8213, #29659, #2146 ) ;
#69242=EDGE_LOOP ( 'NONE', ( #16853, #67396, #37305, #9587 ) ) ;
#69264=DIRECTION ( 'NONE',  ( -0.000000000000000000, -0.000000000000000000, 1.000000000000000000 ) ) ;
#69265=LINE ( 'NONE', #47506, #1074 ) ;
#69266=AXIS2_PLACEMENT_3D ( 'NONE', #57788, #10971, #12006 ) ;
#69271=LINE ( 'NONE', #36938, #29707 ) ;
#69290=DIRECTION ( 'NONE',  ( 1.000000000000000000, 0.000000000000000000, -0.000000000000000000 ) ) ;
#69301=ORIENTED_EDGE ( 'NONE', *, *, #23410, .T. ) ;
#69337=DIRECTION ( 'NONE',  ( -1.000000000000000000, 0.000000000000000000, 0.000000000000000000 ) ) ;
#69363=DIRECTION ( 'NONE',  ( 0.000000000000000000, 0.000000000000000000, -1.000000000000000000 ) ) ;
#69369=DIRECTION ( 'NONE',  ( -1.000000000000000000, 0.000000000000000000, 0.000000000000000000 ) ) ;
#69392=LINE ( 'NONE', #43410, #14069 ) ;
#69417=DIRECTION ( 'NONE',  ( 1.000000000000000000, 0.000000000000000000, 0.000000000000000000 ) ) ;
#69426=DIRECTION ( 'NONE',  ( -1.000000000000000000, 0.000000000000000000, 0.000000000000000000 ) ) ;
#69440=CARTESIAN_POINT ( 'NONE',  ( 9.250000000000003553, 27.99999999999998934, 3.750000000000000000 ) ) ;
#69441=CYLINDRICAL_SURFACE ( 'NONE', #64570, 0.2500000000000002220 ) ;
#69463=FACE_OUTER_BOUND ( 'NONE', #8630, .T. ) ;
#69469=ORIENTED_EDGE ( 'NONE', *, *, #65117, .F. ) ;
#69477=VERTEX_POINT ( 'NONE', #23808 ) ;
#69496=DIRECTION ( 'NONE',  ( -0.000000000000000000, -0.000000000000000000, 1.000000000000000000 ) ) ;
#69519=DIRECTION ( 'NONE',  ( -1.000000000000000000, 0.000000000000000000, 0.000000000000000000 ) ) ;
#69547=CARTESIAN_POINT ( 'NONE',  ( 13.75000000000000533, 30.74999999999999289, -4.000000000000000000 ) ) ;
#69553=ORIENTED_EDGE ( 'NONE', *, *, #36160, .F. ) ;
#69557=EDGE_CURVE ( 'NONE', #5051, #56763, #8343, .T. ) ;
#69589=EDGE_CURVE ( 'NONE', #58700, #55021, #36498, .T. ) ;
#69603=ORIENTED_EDGE ( 'NONE', *, *, #33203, .T. ) ;
#69606=ORIENTED_EDGE ( 'NONE', *, *, #18189, .F. ) ;
#69616=VECTOR ( 'NONE', #52140, 1000.000000000000000 ) ;
#69622=DIRECTION ( 'NONE',  ( -0.000000000000000000, 1.000000000000000000, -0.000000000000000000 ) ) ;
#69628=FACE_OUTER_BOUND ( 'NONE', #59322, .T. ) ;
#69629=DIRECTION ( 'NONE',  ( -0.000000000000000000, -0.000000000000000000, 1.000000000000000000 ) ) ;
#69641=VERTEX_POINT ( 'NONE', #20259 ) ;
#69651=FACE_OUTER_BOUND ( 'NONE', #53618, .T. ) ;
#69661=EDGE_CURVE ( 'NONE', #54990, #33026, #59621, .T. ) ;
#69688=CARTESIAN_POINT ( 'NONE',  ( -4.500000000000002665, 24.74999999999998579, 4.000000000000000000 ) ) ;
#69691=ORIENTED_EDGE ( 'NONE', *, *, #67281, .F. ) ;
ENDSEC;
END-ISO-10303-21;
